ISO-10303-21;
HEADER;
FILE_DESCRIPTION((''),'2;1');
FILE_NAME('Ball Spline Nut Outer Sleeve Round Flange BSLM16.step','2026-10-05T22:33:56+05:00',(''),(''),'','','');
FILE_SCHEMA (('AUTOMOTIVE_DESIGN { 1 0 10303 214 3 1 1 }'));
ENDSEC;
DATA;
#10=MECHANICAL_DESIGN_GEOMETRIC_PRESENTATION_REPRESENTATION('',(#430),#16942);
#316=TOROIDAL_SURFACE('',#8446,15.9,0.4) ;
#319=ELLIPSE('',#8347,198.783549846831,15.5) ;
#320=ELLIPSE('',#8363,16.3431626165531,15.5) ;
#321=ELLIPSE('',#8364,16.3920609727038,15.5) ;
#322=ELLIPSE('',#8367,16.4076100792785,15.5) ;
#323=ELLIPSE('',#8368,16.3701261870697,15.5) ;
#324=ELLIPSE('',#8369,177.958118605591,15.5) ;
#325=ELLIPSE('',#8370,206.510783338566,15.5) ;
#326=ELLIPSE('',#8377,16.3431623815015,15.5) ;
#327=ELLIPSE('',#8378,16.3920609727038,15.5) ;
#328=ELLIPSE('',#8381,16.4076104906839,15.5) ;
#329=ELLIPSE('',#8382,16.3701257903539,15.5) ;
#330=B_SPLINE_SURFACE_WITH_KNOTS('',2,1,((#11224,#11225),(#11226,#11227),
(#11228,#11229)),.UNSPECIFIED.,.F.,.F.,.F.,(3,3),(2,2),(0.,1.),(0.,0.0650000000000004),
 .UNSPECIFIED.) ;
#331=B_SPLINE_SURFACE_WITH_KNOTS('',2,1,((#11249,#11250),(#11251,#11252),
(#11253,#11254)),.UNSPECIFIED.,.F.,.F.,.F.,(3,3),(2,2),(0.,1.),(0.,0.0650000000000004),
 .UNSPECIFIED.) ;
#332=B_SPLINE_SURFACE_WITH_KNOTS('',2,1,((#11271,#11272),(#11273,#11274),
(#11275,#11276)),.UNSPECIFIED.,.F.,.F.,.F.,(3,3),(2,2),(0.,1.),(0.,0.0650000000000004),
 .UNSPECIFIED.) ;
#333=B_SPLINE_SURFACE_WITH_KNOTS('',2,1,((#11293,#11294),(#11295,#11296),
(#11297,#11298)),.UNSPECIFIED.,.F.,.F.,.F.,(3,3),(2,2),(0.,1.),(0.,0.0650000000000004),
 .UNSPECIFIED.) ;
#334=B_SPLINE_SURFACE_WITH_KNOTS('',2,1,((#11315,#11316),(#11317,#11318),
(#11319,#11320)),.UNSPECIFIED.,.F.,.F.,.F.,(3,3),(2,2),(0.,1.),(0.,0.0650000000000004),
 .UNSPECIFIED.) ;
#335=B_SPLINE_SURFACE_WITH_KNOTS('',2,1,((#11340,#11341),(#11342,#11343),
(#11344,#11345)),.UNSPECIFIED.,.F.,.F.,.F.,(3,3),(2,2),(0.,1.),(0.,0.0650000000000004),
 .UNSPECIFIED.) ;
#336=B_SPLINE_SURFACE_WITH_KNOTS('',2,1,((#11359,#11360),(#11361,#11362),
(#11363,#11364)),.UNSPECIFIED.,.F.,.F.,.F.,(3,3),(2,2),(0.,1.),(0.,0.0650000000000004),
 .UNSPECIFIED.) ;
#337=B_SPLINE_SURFACE_WITH_KNOTS('',2,1,((#11378,#11379),(#11380,#11381),
(#11382,#11383)),.UNSPECIFIED.,.F.,.F.,.F.,(3,3),(2,2),(0.,1.),(0.,0.0650000000000004),
 .UNSPECIFIED.) ;
#338=B_SPLINE_SURFACE_WITH_KNOTS('',2,1,((#11397,#11398),(#11399,#11400),
(#11401,#11402)),.UNSPECIFIED.,.F.,.F.,.F.,(3,3),(2,2),(0.,1.),(0.,0.0650000000000004),
 .UNSPECIFIED.) ;
#339=B_SPLINE_SURFACE_WITH_KNOTS('',2,1,((#11416,#11417),(#11418,#11419),
(#11420,#11421)),.UNSPECIFIED.,.F.,.F.,.F.,(3,3),(2,2),(0.,1.),(0.,0.0650000000000004),
 .UNSPECIFIED.) ;
#340=B_SPLINE_SURFACE_WITH_KNOTS('',2,1,((#11438,#11439),(#11440,#11441),
(#11442,#11443)),.UNSPECIFIED.,.F.,.F.,.F.,(3,3),(2,2),(0.,1.),(0.,0.0650000000000004),
 .UNSPECIFIED.) ;
#341=B_SPLINE_SURFACE_WITH_KNOTS('',2,1,((#11456,#11457),(#11458,#11459),
(#11460,#11461)),.UNSPECIFIED.,.F.,.F.,.F.,(3,3),(2,2),(0.,1.),(0.,0.0650000000000004),
 .UNSPECIFIED.) ;
#342=B_SPLINE_SURFACE_WITH_KNOTS('',2,1,((#11476,#11477),(#11478,#11479),
(#11480,#11481)),.UNSPECIFIED.,.F.,.F.,.F.,(3,3),(2,2),(0.,1.),(0.,0.0650000000000004),
 .UNSPECIFIED.) ;
#343=B_SPLINE_SURFACE_WITH_KNOTS('',2,1,((#11498,#11499),(#11500,#11501),
(#11502,#11503)),.UNSPECIFIED.,.F.,.F.,.F.,(3,3),(2,2),(0.,1.),(0.,0.0650000000000004),
 .UNSPECIFIED.) ;
#344=B_SPLINE_SURFACE_WITH_KNOTS('',2,1,((#11517,#11518),(#11519,#11520),
(#11521,#11522)),.UNSPECIFIED.,.F.,.F.,.F.,(3,3),(2,2),(0.,1.),(0.,0.0650000000000004),
 .UNSPECIFIED.) ;
#345=B_SPLINE_SURFACE_WITH_KNOTS('',2,1,((#11536,#11537),(#11538,#11539),
(#11540,#11541)),.UNSPECIFIED.,.F.,.F.,.F.,(3,3),(2,2),(0.,1.),(0.,0.0650000000000004),
 .UNSPECIFIED.) ;
#346=B_SPLINE_SURFACE_WITH_KNOTS('',2,1,((#11555,#11556),(#11557,#11558),
(#11559,#11560)),.UNSPECIFIED.,.F.,.F.,.F.,(3,3),(2,2),(0.,1.),(0.,0.0650000000000004),
 .UNSPECIFIED.) ;
#347=B_SPLINE_SURFACE_WITH_KNOTS('',2,1,((#11574,#11575),(#11576,#11577),
(#11578,#11579)),.UNSPECIFIED.,.F.,.F.,.F.,(3,3),(2,2),(0.,1.),(0.,0.0650000000000004),
 .UNSPECIFIED.) ;
#348=B_SPLINE_SURFACE_WITH_KNOTS('',2,1,((#11590,#11591),(#11592,#11593),
(#11594,#11595)),.UNSPECIFIED.,.F.,.F.,.F.,(3,3),(2,2),(0.,1.),(0.,0.0650000000000004),
 .UNSPECIFIED.) ;
#349=B_SPLINE_SURFACE_WITH_KNOTS('',2,1,((#11609,#11610),(#11611,#11612),
(#11613,#11614)),.UNSPECIFIED.,.F.,.F.,.F.,(3,3),(2,2),(0.,1.),(0.,0.0650000000000004),
 .UNSPECIFIED.) ;
#350=B_SPLINE_SURFACE_WITH_KNOTS('',2,1,((#11628,#11629),(#11630,#11631),
(#11632,#11633)),.UNSPECIFIED.,.F.,.F.,.F.,(3,3),(2,2),(0.,1.),(0.,0.0650000000000004),
 .UNSPECIFIED.) ;
#351=B_SPLINE_SURFACE_WITH_KNOTS('',2,1,((#11647,#11648),(#11649,#11650),
(#11651,#11652)),.UNSPECIFIED.,.F.,.F.,.F.,(3,3),(2,2),(0.,1.),(0.,0.0650000000000004),
 .UNSPECIFIED.) ;
#352=B_SPLINE_SURFACE_WITH_KNOTS('',2,1,((#11672,#11673),(#11674,#11675),
(#11676,#11677)),.UNSPECIFIED.,.F.,.F.,.F.,(3,3),(2,2),(0.,1.),(0.,0.0650000000000004),
 .UNSPECIFIED.) ;
#353=B_SPLINE_SURFACE_WITH_KNOTS('',2,1,((#11691,#11692),(#11693,#11694),
(#11695,#11696)),.UNSPECIFIED.,.F.,.F.,.F.,(3,3),(2,2),(0.,1.),(0.,0.0650000000000004),
 .UNSPECIFIED.) ;
#354=B_SPLINE_SURFACE_WITH_KNOTS('',2,1,((#11710,#11711),(#11712,#11713),
(#11714,#11715)),.UNSPECIFIED.,.F.,.F.,.F.,(3,3),(2,2),(0.,1.),(0.,0.0650000000000004),
 .UNSPECIFIED.) ;
#355=B_SPLINE_SURFACE_WITH_KNOTS('',2,1,((#11732,#11733),(#11734,#11735),
(#11736,#11737)),.UNSPECIFIED.,.F.,.F.,.F.,(3,3),(2,2),(0.,1.),(0.,0.0650000000000004),
 .UNSPECIFIED.) ;
#356=B_SPLINE_SURFACE_WITH_KNOTS('',2,1,((#11763,#11764),(#11765,#11766),
(#11767,#11768)),.UNSPECIFIED.,.F.,.F.,.F.,(3,3),(2,2),(0.,1.),(0.,0.0650000000000004),
 .UNSPECIFIED.) ;
#357=B_SPLINE_SURFACE_WITH_KNOTS('',2,1,((#11780,#11781),(#11782,#11783),
(#11784,#11785)),.UNSPECIFIED.,.F.,.F.,.F.,(3,3),(2,2),(0.,1.),(0.,0.0650000000000004),
 .UNSPECIFIED.) ;
#358=B_SPLINE_SURFACE_WITH_KNOTS('',2,1,((#11808,#11809),(#11810,#11811),
(#11812,#11813)),.UNSPECIFIED.,.F.,.F.,.F.,(3,3),(2,2),(0.,1.),(0.,0.0650000000000004),
 .UNSPECIFIED.) ;
#359=B_SPLINE_SURFACE_WITH_KNOTS('',2,1,((#11827,#11828),(#11829,#11830),
(#11831,#11832)),.UNSPECIFIED.,.F.,.F.,.F.,(3,3),(2,2),(0.,1.),(0.,0.0650000000000004),
 .UNSPECIFIED.) ;
#360=B_SPLINE_SURFACE_WITH_KNOTS('',2,1,((#11852,#11853),(#11854,#11855),
(#11856,#11857)),.UNSPECIFIED.,.F.,.F.,.F.,(3,3),(2,2),(0.,1.),(0.,0.0650000000000004),
 .UNSPECIFIED.) ;
#361=B_SPLINE_SURFACE_WITH_KNOTS('',2,1,((#12604,#12605),(#12606,#12607),
(#12608,#12609)),.UNSPECIFIED.,.F.,.F.,.F.,(3,3),(2,2),(0.,1.),(0.,0.0650000000000004),
 .UNSPECIFIED.) ;
#362=B_SPLINE_SURFACE_WITH_KNOTS('',2,1,((#12615,#12616),(#12617,#12618),
(#12619,#12620)),.UNSPECIFIED.,.F.,.F.,.F.,(3,3),(2,2),(0.,1.),(0.,0.0650000000000004),
 .UNSPECIFIED.) ;
#363=B_SPLINE_SURFACE_WITH_KNOTS('',2,1,((#12641,#12642),(#12643,#12644),
(#12645,#12646)),.UNSPECIFIED.,.F.,.F.,.F.,(3,3),(2,2),(0.,1.),(0.,0.0650000000000004),
 .UNSPECIFIED.) ;
#364=B_SPLINE_SURFACE_WITH_KNOTS('',2,1,((#12666,#12667),(#12668,#12669),
(#12670,#12671)),.UNSPECIFIED.,.F.,.F.,.F.,(3,3),(2,2),(0.,1.),(0.,0.0650000000000004),
 .UNSPECIFIED.) ;
#365=B_SPLINE_SURFACE_WITH_KNOTS('',2,1,((#12677,#12678),(#12679,#12680),
(#12681,#12682)),.UNSPECIFIED.,.F.,.F.,.F.,(3,3),(2,2),(0.,1.),(0.,0.0650000000000004),
 .UNSPECIFIED.) ;
#366=B_SPLINE_SURFACE_WITH_KNOTS('',2,1,((#12688,#12689),(#12690,#12691),
(#12692,#12693)),.UNSPECIFIED.,.F.,.F.,.F.,(3,3),(2,2),(0.,1.),(0.,0.0650000000000004),
 .UNSPECIFIED.) ;
#367=B_SPLINE_SURFACE_WITH_KNOTS('',2,1,((#12699,#12700),(#12701,#12702),
(#12703,#12704)),.UNSPECIFIED.,.F.,.F.,.F.,(3,3),(2,2),(0.,1.),(0.,0.0650000000000004),
 .UNSPECIFIED.) ;
#368=B_SPLINE_SURFACE_WITH_KNOTS('',2,1,((#12710,#12711),(#12712,#12713),
(#12714,#12715)),.UNSPECIFIED.,.F.,.F.,.F.,(3,3),(2,2),(0.,1.),(0.,0.0650000000000004),
 .UNSPECIFIED.) ;
#369=B_SPLINE_SURFACE_WITH_KNOTS('',2,1,((#12721,#12722),(#12723,#12724),
(#12725,#12726)),.UNSPECIFIED.,.F.,.F.,.F.,(3,3),(2,2),(0.,1.),(0.,0.0650000000000004),
 .UNSPECIFIED.) ;
#370=B_SPLINE_SURFACE_WITH_KNOTS('',2,1,((#12732,#12733),(#12734,#12735),
(#12736,#12737)),.UNSPECIFIED.,.F.,.F.,.F.,(3,3),(2,2),(0.,1.),(0.,0.0650000000000004),
 .UNSPECIFIED.) ;
#371=B_SPLINE_SURFACE_WITH_KNOTS('',2,1,((#12743,#12744),(#12745,#12746),
(#12747,#12748)),.UNSPECIFIED.,.F.,.F.,.F.,(3,3),(2,2),(0.,1.),(0.,0.0650000000000004),
 .UNSPECIFIED.) ;
#372=B_SPLINE_SURFACE_WITH_KNOTS('',2,1,((#12754,#12755),(#12756,#12757),
(#12758,#12759)),.UNSPECIFIED.,.F.,.F.,.F.,(3,3),(2,2),(0.,1.),(0.,0.0650000000000004),
 .UNSPECIFIED.) ;
#373=B_SPLINE_SURFACE_WITH_KNOTS('',2,1,((#12765,#12766),(#12767,#12768),
(#12769,#12770)),.UNSPECIFIED.,.F.,.F.,.F.,(3,3),(2,2),(0.,1.),(0.,0.0650000000000004),
 .UNSPECIFIED.) ;
#374=B_SPLINE_SURFACE_WITH_KNOTS('',2,1,((#12787,#12788),(#12789,#12790),
(#12791,#12792)),.UNSPECIFIED.,.F.,.F.,.F.,(3,3),(2,2),(0.,1.),(0.,0.0650000000000004),
 .UNSPECIFIED.) ;
#375=B_SPLINE_SURFACE_WITH_KNOTS('',2,1,((#12800,#12801),(#12802,#12803),
(#12804,#12805)),.UNSPECIFIED.,.F.,.F.,.F.,(3,3),(2,2),(0.,1.),(0.,0.0650000000000004),
 .UNSPECIFIED.) ;
#376=B_SPLINE_SURFACE_WITH_KNOTS('',2,1,((#12811,#12812),(#12813,#12814),
(#12815,#12816)),.UNSPECIFIED.,.F.,.F.,.F.,(3,3),(2,2),(0.,1.),(0.,0.0650000000000004),
 .UNSPECIFIED.) ;
#377=B_SPLINE_SURFACE_WITH_KNOTS('',2,1,((#12826,#12827),(#12828,#12829),
(#12830,#12831)),.UNSPECIFIED.,.F.,.F.,.F.,(3,3),(2,2),(0.,1.),(0.,0.0650000000000004),
 .UNSPECIFIED.) ;
#378=B_SPLINE_SURFACE_WITH_KNOTS('',2,1,((#12837,#12838),(#12839,#12840),
(#12841,#12842)),.UNSPECIFIED.,.F.,.F.,.F.,(3,3),(2,2),(0.,1.),(0.,0.0650000000000004),
 .UNSPECIFIED.) ;
#379=B_SPLINE_SURFACE_WITH_KNOTS('',2,1,((#12848,#12849),(#12850,#12851),
(#12852,#12853)),.UNSPECIFIED.,.F.,.F.,.F.,(3,3),(2,2),(0.,1.),(0.,0.0650000000000004),
 .UNSPECIFIED.) ;
#380=B_SPLINE_SURFACE_WITH_KNOTS('',2,1,((#12859,#12860),(#12861,#12862),
(#12863,#12864)),.UNSPECIFIED.,.F.,.F.,.F.,(3,3),(2,2),(0.,1.),(0.,0.0650000000000004),
 .UNSPECIFIED.) ;
#381=B_SPLINE_SURFACE_WITH_KNOTS('',2,1,((#12870,#12871),(#12872,#12873),
(#12874,#12875)),.UNSPECIFIED.,.F.,.F.,.F.,(3,3),(2,2),(0.,1.),(0.,0.0650000000000004),
 .UNSPECIFIED.) ;
#382=B_SPLINE_SURFACE_WITH_KNOTS('',2,1,((#12881,#12882),(#12883,#12884),
(#12885,#12886)),.UNSPECIFIED.,.F.,.F.,.F.,(3,3),(2,2),(0.,1.),(0.,0.0650000000000004),
 .UNSPECIFIED.) ;
#383=B_SPLINE_SURFACE_WITH_KNOTS('',2,1,((#12892,#12893),(#12894,#12895),
(#12896,#12897)),.UNSPECIFIED.,.F.,.F.,.F.,(3,3),(2,2),(0.,1.),(0.,0.0650000000000004),
 .UNSPECIFIED.) ;
#384=B_SPLINE_SURFACE_WITH_KNOTS('',2,1,((#12903,#12904),(#12905,#12906),
(#12907,#12908)),.UNSPECIFIED.,.F.,.F.,.F.,(3,3),(2,2),(0.,1.),(0.,0.0650000000000004),
 .UNSPECIFIED.) ;
#385=B_SPLINE_SURFACE_WITH_KNOTS('',2,1,((#12914,#12915),(#12916,#12917),
(#12918,#12919)),.UNSPECIFIED.,.F.,.F.,.F.,(3,3),(2,2),(0.,1.),(0.,0.0650000000000004),
 .UNSPECIFIED.) ;
#386=B_SPLINE_SURFACE_WITH_KNOTS('',2,1,((#12925,#12926),(#12927,#12928),
(#12929,#12930)),.UNSPECIFIED.,.F.,.F.,.F.,(3,3),(2,2),(0.,1.),(0.,0.0650000000000004),
 .UNSPECIFIED.) ;
#387=B_SPLINE_SURFACE_WITH_KNOTS('',2,1,((#12936,#12937),(#12938,#12939),
(#12940,#12941)),.UNSPECIFIED.,.F.,.F.,.F.,(3,3),(2,2),(0.,1.),(0.,0.0650000000000004),
 .UNSPECIFIED.) ;
#388=B_SPLINE_SURFACE_WITH_KNOTS('',2,1,((#12947,#12948),(#12949,#12950),
(#12951,#12952)),.UNSPECIFIED.,.F.,.F.,.F.,(3,3),(2,2),(0.,1.),(0.,0.0650000000000004),
 .UNSPECIFIED.) ;
#389=B_SPLINE_SURFACE_WITH_KNOTS('',2,1,((#12958,#12959),(#12960,#12961),
(#12962,#12963)),.UNSPECIFIED.,.F.,.F.,.F.,(3,3),(2,2),(0.,1.),(0.,0.0650000000000004),
 .UNSPECIFIED.) ;
#390=B_SPLINE_SURFACE_WITH_KNOTS('',2,1,((#12969,#12970),(#12971,#12972),
(#12973,#12974)),.UNSPECIFIED.,.F.,.F.,.F.,(3,3),(2,2),(0.,1.),(0.,0.0650000000000004),
 .UNSPECIFIED.) ;
#391=B_SPLINE_SURFACE_WITH_KNOTS('',2,1,((#12980,#12981),(#12982,#12983),
(#12984,#12985)),.UNSPECIFIED.,.F.,.F.,.F.,(3,3),(2,2),(0.,1.),(0.,0.0650000000000004),
 .UNSPECIFIED.) ;
#392=B_SPLINE_SURFACE_WITH_KNOTS('',2,1,((#12991,#12992),(#12993,#12994),
(#12995,#12996)),.UNSPECIFIED.,.F.,.F.,.F.,(3,3),(2,2),(0.,1.),(0.,0.0650000000000004),
 .UNSPECIFIED.) ;
#393=B_SPLINE_SURFACE_WITH_KNOTS('',2,1,((#13002,#13003),(#13004,#13005),
(#13006,#13007)),.UNSPECIFIED.,.F.,.F.,.F.,(3,3),(2,2),(0.,1.),(0.,0.0650000000000004),
 .UNSPECIFIED.) ;
#394=B_SPLINE_SURFACE_WITH_KNOTS('',2,1,((#13013,#13014),(#13015,#13016),
(#13017,#13018)),.UNSPECIFIED.,.F.,.F.,.F.,(3,3),(2,2),(0.,1.),(0.,0.0650000000000004),
 .UNSPECIFIED.) ;
#395=B_SPLINE_SURFACE_WITH_KNOTS('',2,1,((#13024,#13025),(#13026,#13027),
(#13028,#13029)),.UNSPECIFIED.,.F.,.F.,.F.,(3,3),(2,2),(0.,1.),(0.,0.0650000000000004),
 .UNSPECIFIED.) ;
#396=B_SPLINE_SURFACE_WITH_KNOTS('',2,1,((#13035,#13036),(#13037,#13038),
(#13039,#13040)),.UNSPECIFIED.,.F.,.F.,.F.,(3,3),(2,2),(0.,1.),(0.,0.0650000000000004),
 .UNSPECIFIED.) ;
#397=B_SPLINE_SURFACE_WITH_KNOTS('',2,1,((#13046,#13047),(#13048,#13049),
(#13050,#13051)),.UNSPECIFIED.,.F.,.F.,.F.,(3,3),(2,2),(0.,1.),(0.,0.0650000000000004),
 .UNSPECIFIED.) ;
#398=B_SPLINE_SURFACE_WITH_KNOTS('',2,1,((#13057,#13058),(#13059,#13060),
(#13061,#13062)),.UNSPECIFIED.,.F.,.F.,.F.,(3,3),(2,2),(0.,1.),(0.,0.0650000000000004),
 .UNSPECIFIED.) ;
#399=B_SPLINE_SURFACE_WITH_KNOTS('',2,1,((#13068,#13069),(#13070,#13071),
(#13072,#13073)),.UNSPECIFIED.,.F.,.F.,.F.,(3,3),(2,2),(0.,1.),(0.,0.0650000000000004),
 .UNSPECIFIED.) ;
#400=B_SPLINE_SURFACE_WITH_KNOTS('',2,1,((#13079,#13080),(#13081,#13082),
(#13083,#13084)),.UNSPECIFIED.,.F.,.F.,.F.,(3,3),(2,2),(0.,1.),(0.,0.0650000000000004),
 .UNSPECIFIED.) ;
#401=B_SPLINE_SURFACE_WITH_KNOTS('',2,1,((#13090,#13091),(#13092,#13093),
(#13094,#13095)),.UNSPECIFIED.,.F.,.F.,.F.,(3,3),(2,2),(0.,1.),(0.,0.0650000000000004),
 .UNSPECIFIED.) ;
#402=B_SPLINE_SURFACE_WITH_KNOTS('',2,1,((#13101,#13102),(#13103,#13104),
(#13105,#13106)),.UNSPECIFIED.,.F.,.F.,.F.,(3,3),(2,2),(0.,1.),(0.,0.0650000000000004),
 .UNSPECIFIED.) ;
#403=B_SPLINE_SURFACE_WITH_KNOTS('',2,1,((#13112,#13113),(#13114,#13115),
(#13116,#13117)),.UNSPECIFIED.,.F.,.F.,.F.,(3,3),(2,2),(0.,1.),(0.,0.0650000000000004),
 .UNSPECIFIED.) ;
#404=B_SPLINE_SURFACE_WITH_KNOTS('',2,1,((#13123,#13124),(#13125,#13126),
(#13127,#13128)),.UNSPECIFIED.,.F.,.F.,.F.,(3,3),(2,2),(0.,1.),(0.,0.0650000000000004),
 .UNSPECIFIED.) ;
#405=B_SPLINE_SURFACE_WITH_KNOTS('',2,1,((#13134,#13135),(#13136,#13137),
(#13138,#13139)),.UNSPECIFIED.,.F.,.F.,.F.,(3,3),(2,2),(0.,1.),(0.,0.0650000000000004),
 .UNSPECIFIED.) ;
#406=B_SPLINE_SURFACE_WITH_KNOTS('',2,1,((#13149,#13150),(#13151,#13152),
(#13153,#13154)),.UNSPECIFIED.,.F.,.F.,.F.,(3,3),(2,2),(0.,1.),(0.,0.0650000000000004),
 .UNSPECIFIED.) ;
#407=B_SPLINE_SURFACE_WITH_KNOTS('',2,1,((#13197,#13198),(#13199,#13200),
(#13201,#13202)),.UNSPECIFIED.,.F.,.F.,.F.,(3,3),(2,2),(0.,1.),(0.,0.0650000000000004),
 .UNSPECIFIED.) ;
#408=B_SPLINE_SURFACE_WITH_KNOTS('',2,1,((#13208,#13209),(#13210,#13211),
(#13212,#13213)),.UNSPECIFIED.,.F.,.F.,.F.,(3,3),(2,2),(0.,1.),(0.,0.0650000000000004),
 .UNSPECIFIED.) ;
#409=B_SPLINE_SURFACE_WITH_KNOTS('',3,3,((#13256,#13257,#13258,#13259,#13260,
#13261),(#13262,#13263,#13264,#13265,#13266,#13267),(#13268,#13269,#13270,
#13271,#13272,#13273),(#13274,#13275,#13276,#13277,#13278,#13279)),
 .UNSPECIFIED.,.F.,.F.,.F.,(4,4),(4,1,1,4),(0.,1.),(-1.05732256406473,-0.901937192254856,
-0.746551820444979,-0.513473762730163),.UNSPECIFIED.) ;
#410=B_SPLINE_SURFACE_WITH_KNOTS('',3,3,((#13341,#13342,#13343,#13344,#13345,
#13346),(#13347,#13348,#13349,#13350,#13351,#13352),(#13353,#13354,#13355,
#13356,#13357,#13358),(#13359,#13360,#13361,#13362,#13363,#13364)),
 .UNSPECIFIED.,.F.,.F.,.F.,(4,4),(4,1,1,4),(0.,1.),(0.513473762730164,0.746551820444979,
0.901937192254856,1.05732256406473),.UNSPECIFIED.) ;
#411=B_SPLINE_SURFACE_WITH_KNOTS('',3,3,((#13384,#13385,#13386,#13387,#13388,
#13389),(#13390,#13391,#13392,#13393,#13394,#13395),(#13396,#13397,#13398,
#13399,#13400,#13401),(#13402,#13403,#13404,#13405,#13406,#13407)),
 .UNSPECIFIED.,.F.,.F.,.F.,(4,4),(4,1,1,4),(0.,1.),(-4.19891521765453,-4.04352984584465,
-3.88814447403477,-3.65506641631996),.UNSPECIFIED.) ;
#412=B_SPLINE_SURFACE_WITH_KNOTS('',3,3,((#13427,#13428,#13429,#13430,#13431,
#13432),(#13433,#13434,#13435,#13436,#13437,#13438),(#13439,#13440,#13441,
#13442,#13443,#13444),(#13445,#13446,#13447,#13448,#13449,#13450)),
 .UNSPECIFIED.,.F.,.F.,.F.,(4,4),(4,1,1,4),(0.,1.),(-2.62811889085963,-2.39504083314481,
-2.23965546133494,-2.08427008952506),.UNSPECIFIED.) ;
#416=SHAPE_REPRESENTATION_RELATIONSHIP('SRR','None',#17020,#423) ;
#423=ADVANCED_BREP_SHAPE_REPRESENTATION('',(#437),#16936) ;
#430=STYLED_ITEM('',(#17064),#437) ;
#437=MANIFOLD_SOLID_BREP(
'Ball Spline Nut Outer Sleeve Round Flange BSLM16',#8179) ;
#459=B_SPLINE_CURVE_WITH_KNOTS('',3,(#11232,#11233,#11234,#11235,#11236,
#11237,#11238,#11239,#11240,#11241),.UNSPECIFIED.,.F.,.F.,(4,3,3,4),(0.,
0.0150000164083537,0.0240853197637074,0.0337869872272911),.UNSPECIFIED.) ;
#460=B_SPLINE_CURVE_WITH_KNOTS('',2,(#11245,#11246,#11247),
 .UNSPECIFIED.,.F.,.F.,(3,3),(0.,1.),.UNSPECIFIED.) ;
#461=B_SPLINE_CURVE_WITH_KNOTS('',3,(#11256,#11257,#11258,#11259,#11260,
#11261,#11262,#11263,#11264,#11265),.UNSPECIFIED.,.F.,.F.,(4,3,3,4),(0.,
0.0173556832409861,0.0345243876037734,0.0405769411926334),.UNSPECIFIED.) ;
#462=B_SPLINE_CURVE_WITH_KNOTS('',2,(#11267,#11268,#11269),
 .UNSPECIFIED.,.F.,.F.,(3,3),(0.,1.),.UNSPECIFIED.) ;
#463=B_SPLINE_CURVE_WITH_KNOTS('',3,(#11278,#11279,#11280,#11281,#11282,
#11283,#11284,#11285,#11286,#11287),.UNSPECIFIED.,.F.,.F.,(4,3,3,4),(0.,
0.0206625445765638,0.029902214499977,0.0388796639931611),.UNSPECIFIED.) ;
#464=B_SPLINE_CURVE_WITH_KNOTS('',2,(#11289,#11290,#11291),
 .UNSPECIFIED.,.F.,.F.,(3,3),(0.,1.),.UNSPECIFIED.) ;
#465=B_SPLINE_CURVE_WITH_KNOTS('',3,(#11300,#11301,#11302,#11303,#11304,
#11305,#11306,#11307,#11308,#11309),.UNSPECIFIED.,.F.,.F.,(4,3,3,4),(0.,
0.0163020293322635,0.0252071380218071,0.0345773972689045),.UNSPECIFIED.) ;
#466=B_SPLINE_CURVE_WITH_KNOTS('',2,(#11311,#11312,#11313),
 .UNSPECIFIED.,.F.,.F.,(3,3),(0.,1.),.UNSPECIFIED.) ;
#467=B_SPLINE_CURVE_WITH_KNOTS('',3,(#11323,#11324,#11325,#11326,#11327,
#11328,#11329,#11330,#11331,#11332),.UNSPECIFIED.,.F.,.F.,(4,3,3,4),(0.,
0.0252144119583777,0.0382782631200122,0.0519544193610427),.UNSPECIFIED.) ;
#468=B_SPLINE_CURVE_WITH_KNOTS('',2,(#11336,#11337,#11338),
 .UNSPECIFIED.,.F.,.F.,(3,3),(0.,1.),.UNSPECIFIED.) ;
#469=B_SPLINE_CURVE_WITH_KNOTS('',3,(#11347,#11348,#11349,#11350,#11351,
#11352,#11353),.UNSPECIFIED.,.F.,.F.,(4,3,4),(0.,0.0265552382096679,0.0567118210565804),
 .UNSPECIFIED.) ;
#470=B_SPLINE_CURVE_WITH_KNOTS('',2,(#11355,#11356,#11357),
 .UNSPECIFIED.,.F.,.F.,(3,3),(0.,1.),.UNSPECIFIED.) ;
#471=B_SPLINE_CURVE_WITH_KNOTS('',3,(#11366,#11367,#11368,#11369,#11370,
#11371,#11372),.UNSPECIFIED.,.F.,.F.,(4,3,4),(0.,0.0202232312434472,0.0400735848175635),
 .UNSPECIFIED.) ;
#472=B_SPLINE_CURVE_WITH_KNOTS('',2,(#11374,#11375,#11376),
 .UNSPECIFIED.,.F.,.F.,(3,3),(0.,1.),.UNSPECIFIED.) ;
#473=B_SPLINE_CURVE_WITH_KNOTS('',3,(#11385,#11386,#11387,#11388,#11389,
#11390,#11391),.UNSPECIFIED.,.F.,.F.,(4,3,4),(0.,0.0190789474349663,0.0373947557586164),
 .UNSPECIFIED.) ;
#474=B_SPLINE_CURVE_WITH_KNOTS('',2,(#11393,#11394,#11395),
 .UNSPECIFIED.,.F.,.F.,(3,3),(0.,1.),.UNSPECIFIED.) ;
#475=B_SPLINE_CURVE_WITH_KNOTS('',3,(#11404,#11405,#11406,#11407,#11408,
#11409,#11410),.UNSPECIFIED.,.F.,.F.,(4,3,4),(0.,0.0182891079019429,0.0373295492055506),
 .UNSPECIFIED.) ;
#476=B_SPLINE_CURVE_WITH_KNOTS('',2,(#11412,#11413,#11414),
 .UNSPECIFIED.,.F.,.F.,(3,3),(0.,1.),.UNSPECIFIED.) ;
#477=B_SPLINE_CURVE_WITH_KNOTS('',3,(#11423,#11424,#11425,#11426,#11427,
#11428,#11429,#11430,#11431,#11432),.UNSPECIFIED.,.F.,.F.,(4,3,3,4),(0.,
0.0297542241681086,0.0460105236800287,0.0629020224502893),.UNSPECIFIED.) ;
#478=B_SPLINE_CURVE_WITH_KNOTS('',2,(#11434,#11435,#11436),
 .UNSPECIFIED.,.F.,.F.,(3,3),(0.,1.),.UNSPECIFIED.) ;
#479=B_SPLINE_CURVE_WITH_KNOTS('',3,(#11445,#11446,#11447,#11448,#11449,
#11450),.UNSPECIFIED.,.F.,.F.,(4,2,4),(0.,0.0242893868272739,0.0842237803126408),
 .UNSPECIFIED.) ;
#480=B_SPLINE_CURVE_WITH_KNOTS('',2,(#11452,#11453,#11454),
 .UNSPECIFIED.,.F.,.F.,(3,3),(0.,1.),.UNSPECIFIED.) ;
#481=B_SPLINE_CURVE_WITH_KNOTS('',3,(#11463,#11464,#11465,#11466,#11467,
#11468,#11469,#11470),.UNSPECIFIED.,.F.,.F.,(4,2,2,4),(0.,0.0544536973145401,
0.0767040245057299,0.0963873215037275),.UNSPECIFIED.) ;
#482=B_SPLINE_CURVE_WITH_KNOTS('',2,(#11472,#11473,#11474),
 .UNSPECIFIED.,.F.,.F.,(3,3),(0.,1.),.UNSPECIFIED.) ;
#483=B_SPLINE_CURVE_WITH_KNOTS('',3,(#11483,#11484,#11485,#11486,#11487,
#11488,#11489,#11490,#11491,#11492),.UNSPECIFIED.,.F.,.F.,(4,3,3,4),(0.,
0.0271232217099323,0.0446974737911228,0.0635054039669033),.UNSPECIFIED.) ;
#484=B_SPLINE_CURVE_WITH_KNOTS('',2,(#11494,#11495,#11496),
 .UNSPECIFIED.,.F.,.F.,(3,3),(0.,1.),.UNSPECIFIED.) ;
#485=B_SPLINE_CURVE_WITH_KNOTS('',3,(#11505,#11506,#11507,#11508,#11509,
#11510,#11511),.UNSPECIFIED.,.F.,.F.,(4,3,4),(0.,0.0175478594959351,0.0350949930523616),
 .UNSPECIFIED.) ;
#486=B_SPLINE_CURVE_WITH_KNOTS('',2,(#11513,#11514,#11515),
 .UNSPECIFIED.,.F.,.F.,(3,3),(0.,1.),.UNSPECIFIED.) ;
#487=B_SPLINE_CURVE_WITH_KNOTS('',3,(#11524,#11525,#11526,#11527,#11528,
#11529,#11530),.UNSPECIFIED.,.F.,.F.,(4,3,4),(0.,0.0121019216609115,0.0237901666703287),
 .UNSPECIFIED.) ;
#488=B_SPLINE_CURVE_WITH_KNOTS('',2,(#11533,#11534,#11535),
 .UNSPECIFIED.,.F.,.F.,(3,3),(0.,1.),.UNSPECIFIED.) ;
#489=B_SPLINE_CURVE_WITH_KNOTS('',3,(#11543,#11544,#11545,#11546,#11547,
#11548,#11549),.UNSPECIFIED.,.F.,.F.,(4,3,4),(0.,0.0133863918273521,0.0260692113791466),
 .UNSPECIFIED.) ;
#490=B_SPLINE_CURVE_WITH_KNOTS('',2,(#11552,#11553,#11554),
 .UNSPECIFIED.,.F.,.F.,(3,3),(0.,1.),.UNSPECIFIED.) ;
#491=B_SPLINE_CURVE_WITH_KNOTS('',3,(#11562,#11563,#11564,#11565,#11566,
#11567,#11568),.UNSPECIFIED.,.F.,.F.,(4,3,4),(0.,0.0138210255321488,0.0277017666505464),
 .UNSPECIFIED.) ;
#492=B_SPLINE_CURVE_WITH_KNOTS('',2,(#11571,#11572,#11573),
 .UNSPECIFIED.,.F.,.F.,(3,3),(0.,1.),.UNSPECIFIED.) ;
#493=B_SPLINE_CURVE_WITH_KNOTS('',3,(#11580,#11581,#11582,#11583,#11584,
#11585,#11586),.UNSPECIFIED.,.F.,.F.,(4,3,4),(0.,0.0173843205296013,0.0380243003929434),
 .UNSPECIFIED.) ;
#494=B_SPLINE_CURVE_WITH_KNOTS('',2,(#11587,#11588,#11589),
 .UNSPECIFIED.,.F.,.F.,(3,3),(0.,1.),.UNSPECIFIED.) ;
#495=B_SPLINE_CURVE_WITH_KNOTS('',3,(#11597,#11598,#11599,#11600,#11601,
#11602,#11603),.UNSPECIFIED.,.F.,.F.,(4,3,4),(0.,0.0240652575004504,0.0463449370279219),
 .UNSPECIFIED.) ;
#496=B_SPLINE_CURVE_WITH_KNOTS('',2,(#11605,#11606,#11607),
 .UNSPECIFIED.,.F.,.F.,(3,3),(0.,1.),.UNSPECIFIED.) ;
#497=B_SPLINE_CURVE_WITH_KNOTS('',3,(#11616,#11617,#11618,#11619,#11620,
#11621,#11622),.UNSPECIFIED.,.F.,.F.,(4,3,4),(0.,0.0155188224962534,0.0308533680520038),
 .UNSPECIFIED.) ;
#498=B_SPLINE_CURVE_WITH_KNOTS('',2,(#11625,#11626,#11627),
 .UNSPECIFIED.,.F.,.F.,(3,3),(0.,1.),.UNSPECIFIED.) ;
#499=B_SPLINE_CURVE_WITH_KNOTS('',3,(#11635,#11636,#11637,#11638,#11639,
#11640,#11641),.UNSPECIFIED.,.F.,.F.,(4,3,4),(0.,0.0169672680417701,0.0330071131092539),
 .UNSPECIFIED.) ;
#500=B_SPLINE_CURVE_WITH_KNOTS('',2,(#11644,#11645,#11646),
 .UNSPECIFIED.,.F.,.F.,(3,3),(0.,1.),.UNSPECIFIED.) ;
#501=B_SPLINE_CURVE_WITH_KNOTS('',3,(#11654,#11655,#11656,#11657,#11658,
#11659,#11660,#11661,#11662,#11663,#11664,#11665,#11666),.UNSPECIFIED.,
 .F.,.F.,(4,3,3,3,4),(0.,0.011770749270626,0.0219604401624206,0.0415400615610363,
0.0508377264422704),.UNSPECIFIED.) ;
#502=B_SPLINE_CURVE_WITH_KNOTS('',2,(#11669,#11670,#11671),
 .UNSPECIFIED.,.F.,.F.,(3,3),(0.,1.),.UNSPECIFIED.) ;
#503=B_SPLINE_CURVE_WITH_KNOTS('',3,(#11679,#11680,#11681,#11682,#11683,
#11684,#11685),.UNSPECIFIED.,.F.,.F.,(4,3,4),(0.,0.0163246527969622,0.0343462180387076),
 .UNSPECIFIED.) ;
#504=B_SPLINE_CURVE_WITH_KNOTS('',2,(#11688,#11689,#11690),
 .UNSPECIFIED.,.F.,.F.,(3,3),(0.,1.),.UNSPECIFIED.) ;
#505=B_SPLINE_CURVE_WITH_KNOTS('',3,(#11698,#11699,#11700,#11701,#11702,
#11703,#11704),.UNSPECIFIED.,.F.,.F.,(4,3,4),(0.,0.0123718787780963,0.0243811015603076),
 .UNSPECIFIED.) ;
#506=B_SPLINE_CURVE_WITH_KNOTS('',2,(#11707,#11708,#11709),
 .UNSPECIFIED.,.F.,.F.,(3,3),(0.,1.),.UNSPECIFIED.) ;
#507=B_SPLINE_CURVE_WITH_KNOTS('',3,(#11717,#11718,#11719,#11720,#11721,
#11722,#11723,#11724,#11725,#11726),.UNSPECIFIED.,.F.,.F.,(4,3,3,4),(0.,
0.0148349366343986,0.0224838356253581,0.0304748092482181),.UNSPECIFIED.) ;
#508=B_SPLINE_CURVE_WITH_KNOTS('',2,(#11729,#11730,#11731),
 .UNSPECIFIED.,.F.,.F.,(3,3),(0.,1.),.UNSPECIFIED.) ;
#509=B_SPLINE_CURVE_WITH_KNOTS('',3,(#11739,#11740,#11741,#11742,#11743,
#11744,#11745,#11746,#11747,#11748,#11749,#11750,#11751),.UNSPECIFIED.,
 .F.,.F.,(4,3,3,3,4),(0.,0.0130698557907629,0.0141731149392098,0.0234680574806899,
0.0251327017063842),.UNSPECIFIED.) ;
#510=B_SPLINE_CURVE_WITH_KNOTS('',2,(#11754,#11755,#11756),
 .UNSPECIFIED.,.F.,.F.,(3,3),(0.,1.),.UNSPECIFIED.) ;
#511=B_SPLINE_CURVE_WITH_KNOTS('',3,(#11769,#11770,#11771,#11772,#11773,
#11774,#11775),.UNSPECIFIED.,.F.,.F.,(4,3,4),(0.,0.0222485092698476,0.0462903807438163),
 .UNSPECIFIED.) ;
#512=B_SPLINE_CURVE_WITH_KNOTS('',2,(#11776,#11777,#11778),
 .UNSPECIFIED.,.F.,.F.,(3,3),(0.,1.),.UNSPECIFIED.) ;
#513=B_SPLINE_CURVE_WITH_KNOTS('',3,(#11788,#11789,#11790,#11791,#11792,
#11793,#11794),.UNSPECIFIED.,.F.,.F.,(4,3,4),(0.,0.0169828382589056,0.0314916243151362),
 .UNSPECIFIED.) ;
#514=B_SPLINE_CURVE_WITH_KNOTS('',2,(#11798,#11799,#11800),
 .UNSPECIFIED.,.F.,.F.,(3,3),(0.,1.),.UNSPECIFIED.) ;
#515=B_SPLINE_CURVE_WITH_KNOTS('',3,(#11815,#11816,#11817,#11818,#11819,
#11820,#11821),.UNSPECIFIED.,.F.,.F.,(4,3,4),(0.,0.024316559375796,0.0475130234788273),
 .UNSPECIFIED.) ;
#516=B_SPLINE_CURVE_WITH_KNOTS('',2,(#11823,#11824,#11825),
 .UNSPECIFIED.,.F.,.F.,(3,3),(0.,1.),.UNSPECIFIED.) ;
#517=B_SPLINE_CURVE_WITH_KNOTS('',3,(#11834,#11835,#11836,#11837,#11838,
#11839,#11840),.UNSPECIFIED.,.F.,.F.,(4,3,4),(0.,0.0206525582993816,0.0379545073521461),
 .UNSPECIFIED.) ;
#518=B_SPLINE_CURVE_WITH_KNOTS('',2,(#11842,#11843,#11844),
 .UNSPECIFIED.,.F.,.F.,(3,3),(0.,1.),.UNSPECIFIED.) ;
#519=B_SPLINE_CURVE_WITH_KNOTS('',3,(#11859,#11860,#11861,#11862,#11863,
#11864,#11865),.UNSPECIFIED.,.F.,.F.,(4,3,4),(0.,0.014536996568322,0.0315221142844197),
 .UNSPECIFIED.) ;
#520=B_SPLINE_CURVE_WITH_KNOTS('',2,(#11868,#11869,#11870),
 .UNSPECIFIED.,.F.,.F.,(3,3),(0.,1.),.UNSPECIFIED.) ;
#521=B_SPLINE_CURVE_WITH_KNOTS('',3,(#11905,#11906,#11907,#11908,#11909,
#11910,#11911,#11912,#11913,#11914,#11915,#11916,#11917,#11918,#11919,#11920,
#11921,#11922,#11923,#11924,#11925,#11926,#11927,#11928,#11929),
 .UNSPECIFIED.,.F.,.F.,(4,3,3,3,3,3,3,3,4),(0.,0.00569194123592617,0.0112324310971198,
0.0165429389179945,0.0201111003725969,0.0242173233513949,0.0282108821611355,
0.0320493450397511,0.0344815069837439),.UNSPECIFIED.) ;
#522=B_SPLINE_CURVE_WITH_KNOTS('',3,(#11931,#11932,#11933,#11934,#11935,
#11936,#11937,#11938,#11939,#11940,#11941,#11942,#11943,#11944,#11945,#11946,
#11947,#11948,#11949,#11950,#11951,#11952,#11953,#11954,#11955),
 .UNSPECIFIED.,.F.,.F.,(4,3,3,3,3,3,3,3,4),(0.,0.00418301047252267,0.00846262474705522,
0.0129021161814928,0.0149322544938229,0.0205445093223957,0.0263037117443392,
0.0322933826159474,0.0355643359068167),.UNSPECIFIED.) ;
#523=B_SPLINE_CURVE_WITH_KNOTS('',3,(#11973,#11974,#11975,#11976,#11977,
#11978,#11979),.UNSPECIFIED.,.F.,.F.,(4,3,4),(0.,0.0212364832794801,0.0419899948755705),
 .UNSPECIFIED.) ;
#524=B_SPLINE_CURVE_WITH_KNOTS('',3,(#11981,#11982,#11983,#11984,#11985,
#11986,#11987),.UNSPECIFIED.,.F.,.F.,(4,3,4),(0.,0.0207952315113147,0.0421638470613952),
 .UNSPECIFIED.) ;
#525=B_SPLINE_CURVE_WITH_KNOTS('',3,(#11991,#11992,#11993,#11994,#11995,
#11996,#11997),.UNSPECIFIED.,.F.,.F.,(4,3,4),(0.,0.0153442120866379,0.0288161992642492),
 .UNSPECIFIED.) ;
#526=B_SPLINE_CURVE_WITH_KNOTS('',3,(#11999,#12000,#12001,#12002,#12003,
#12004,#12005),.UNSPECIFIED.,.F.,.F.,(4,3,4),(0.,0.0133416659410013,0.0284117643200023),
 .UNSPECIFIED.) ;
#527=B_SPLINE_CURVE_WITH_KNOTS('',3,(#12007,#12008,#12009,#12010,#12011,
#12012,#12013),.UNSPECIFIED.,.F.,.F.,(4,3,4),(0.,0.0167683780422157,0.034705436927841),
 .UNSPECIFIED.) ;
#528=B_SPLINE_CURVE_WITH_KNOTS('',3,(#12015,#12016,#12017,#12018,#12019,
#12020,#12021),.UNSPECIFIED.,.F.,.F.,(4,3,4),(0.,0.0157245600444115,0.0299896116808996),
 .UNSPECIFIED.) ;
#529=B_SPLINE_CURVE_WITH_KNOTS('',3,(#12023,#12024,#12025,#12026,#12027,
#12028,#12029),.UNSPECIFIED.,.F.,.F.,(4,3,4),(0.,0.0125773378818699,0.0237065110114582),
 .UNSPECIFIED.) ;
#530=B_SPLINE_CURVE_WITH_KNOTS('',3,(#12031,#12032,#12033,#12034,#12035,
#12036,#12037),.UNSPECIFIED.,.F.,.F.,(4,3,4),(0.,0.0102693084451865,0.0203354088326608),
 .UNSPECIFIED.) ;
#531=B_SPLINE_CURVE_WITH_KNOTS('',3,(#12039,#12040,#12041,#12042,#12043,
#12044,#12045),.UNSPECIFIED.,.F.,.F.,(4,3,4),(0.,0.00992200971474841,0.0195786738962378),
 .UNSPECIFIED.) ;
#532=B_SPLINE_CURVE_WITH_KNOTS('',3,(#12047,#12048,#12049,#12050,#12051,
#12052,#12053,#12054,#12055,#12056),.UNSPECIFIED.,.F.,.F.,(4,3,3,4),(0.,
0.0106013294774732,0.0222845622588424,0.023809317348732),.UNSPECIFIED.) ;
#533=B_SPLINE_CURVE_WITH_KNOTS('',3,(#12058,#12059,#12060,#12061,#12062,
#12063,#12064,#12065,#12066,#12067,#12068,#12069,#12070,#12071,#12072,#12073,
#12074,#12075,#12076),.UNSPECIFIED.,.F.,.F.,(4,3,3,3,3,3,4),(0.,0.00590422965020825,
0.00941919373558824,0.0118084593004165,0.0183919439982395,0.0279075522839463,
0.0311693981304476),.UNSPECIFIED.) ;
#534=B_SPLINE_CURVE_WITH_KNOTS('',3,(#12078,#12079,#12080,#12081,#12082,
#12083,#12084,#12085,#12086,#12087,#12088,#12089,#12090),.UNSPECIFIED.,
 .F.,.F.,(4,3,3,3,4),(0.,0.0150109515841417,0.0257666496332491,0.0333691467947793,
0.0442792551451376),.UNSPECIFIED.) ;
#535=B_SPLINE_CURVE_WITH_KNOTS('',3,(#12092,#12093,#12094,#12095,#12096,
#12097,#12098),.UNSPECIFIED.,.F.,.F.,(4,3,4),(0.,0.016591534262115,0.0315880473127885),
 .UNSPECIFIED.) ;
#536=B_SPLINE_CURVE_WITH_KNOTS('',3,(#12100,#12101,#12102,#12103,#12104,
#12105,#12106),.UNSPECIFIED.,.F.,.F.,(4,3,4),(0.,0.0143488858698759,0.0290305106878466),
 .UNSPECIFIED.) ;
#537=B_SPLINE_CURVE_WITH_KNOTS('',3,(#12108,#12109,#12110,#12111,#12112,
#12113,#12114),.UNSPECIFIED.,.F.,.F.,(4,3,4),(0.,0.0164683028045611,0.0332538948383704),
 .UNSPECIFIED.) ;
#538=B_SPLINE_CURVE_WITH_KNOTS('',3,(#12116,#12117,#12118,#12119,#12120,
#12121,#12122),.UNSPECIFIED.,.F.,.F.,(4,3,4),(0.,0.017474633999681,0.0360764640896449),
 .UNSPECIFIED.) ;
#539=B_SPLINE_CURVE_WITH_KNOTS('',3,(#12124,#12125,#12126,#12127,#12128,
#12129,#12130),.UNSPECIFIED.,.F.,.F.,(4,3,4),(0.,0.0200770342233018,0.0414114209213859),
 .UNSPECIFIED.) ;
#540=B_SPLINE_CURVE_WITH_KNOTS('',3,(#12132,#12133,#12134,#12135,#12136,
#12137,#12138),.UNSPECIFIED.,.F.,.F.,(4,3,4),(0.,0.0231080610840433,0.0441729224541179),
 .UNSPECIFIED.) ;
#541=B_SPLINE_CURVE_WITH_KNOTS('',3,(#12140,#12141,#12142,#12143,#12144,
#12145,#12146),.UNSPECIFIED.,.F.,.F.,(4,3,4),(0.,0.0193208384469699,0.037730112389279),
 .UNSPECIFIED.) ;
#542=B_SPLINE_CURVE_WITH_KNOTS('',3,(#12148,#12149,#12150,#12151,#12152,
#12153,#12154),.UNSPECIFIED.,.F.,.F.,(4,3,4),(0.,0.0182396170597861,0.0370031988263464),
 .UNSPECIFIED.) ;
#543=B_SPLINE_CURVE_WITH_KNOTS('',3,(#12158,#12159,#12160,#12161,#12162,
#12163,#12164,#12165,#12166,#12167),.UNSPECIFIED.,.F.,.F.,(4,3,3,4),(0.,
0.0190427568358624,0.0276047621343949,0.0359942554921667),.UNSPECIFIED.) ;
#544=B_SPLINE_CURVE_WITH_KNOTS('',3,(#12169,#12170,#12171,#12172,#12173,
#12174,#12175,#12176,#12177,#12178),.UNSPECIFIED.,.F.,.F.,(4,3,3,4),(0.,
0.0145175548511501,0.0262513287029716,0.0402671823708522),.UNSPECIFIED.) ;
#545=B_SPLINE_CURVE_WITH_KNOTS('',3,(#12180,#12181,#12182,#12183,#12184,
#12185,#12186,#12187,#12188,#12189,#12190,#12191,#12192),.UNSPECIFIED.,
 .F.,.F.,(4,3,3,3,4),(0.,0.0151398944763002,0.0225141408320645,0.031716815308806,
0.0398561587170203),.UNSPECIFIED.) ;
#546=B_SPLINE_CURVE_WITH_KNOTS('',3,(#12194,#12195,#12196,#12197,#12198,
#12199,#12200,#12201,#12202,#12203),.UNSPECIFIED.,.F.,.F.,(4,3,3,4),(0.,
0.0134998512216097,0.0203874514613731,0.0273913827533458),.UNSPECIFIED.) ;
#547=B_SPLINE_CURVE_WITH_KNOTS('',3,(#12205,#12206,#12207,#12208,#12209,
#12210,#12211,#12212,#12213,#12214),.UNSPECIFIED.,.F.,.F.,(4,3,3,4),(0.,
0.0107582822420351,0.016345486370408,0.0221382733736323),.UNSPECIFIED.) ;
#548=B_SPLINE_CURVE_WITH_KNOTS('',3,(#12216,#12217,#12218,#12219,#12220,
#12221,#12222,#12223,#12224,#12225,#12226,#12227,#12228,#12229,#12230,#12231),
 .UNSPECIFIED.,.F.,.F.,(4,3,3,3,3,4),(0.,0.00420466729910508,0.00633552272142135,
0.0165957853018843,0.0257546857993008,0.031100367807991),.UNSPECIFIED.) ;
#549=B_SPLINE_CURVE_WITH_KNOTS('',3,(#12233,#12234,#12235,#12236,#12237,
#12238,#12239,#12240,#12241,#12242,#12243,#12244,#12245,#12246,#12247,#12248,
#12249,#12250,#12251),.UNSPECIFIED.,.F.,.F.,(4,3,3,3,3,3,4),(0.,0.0140462067224565,
0.0254132340708786,0.0295355002228338,0.0368102718442848,0.0465126418826644,
0.0498614406746093),.UNSPECIFIED.) ;
#550=B_SPLINE_CURVE_WITH_KNOTS('',3,(#12253,#12254,#12255,#12256,#12257,
#12258,#12259),.UNSPECIFIED.,.F.,.F.,(4,3,4),(0.,0.0194616671587977,0.0366325539762354),
 .UNSPECIFIED.) ;
#551=B_SPLINE_CURVE_WITH_KNOTS('',3,(#12261,#12262,#12263,#12264,#12265,
#12266,#12267),.UNSPECIFIED.,.F.,.F.,(4,3,4),(0.,0.0163404825673663,0.0333147063175432),
 .UNSPECIFIED.) ;
#552=B_SPLINE_CURVE_WITH_KNOTS('',3,(#12269,#12270,#12271,#12272,#12273,
#12274,#12275),.UNSPECIFIED.,.F.,.F.,(4,3,4),(0.,0.0174292102142414,0.0353223313086727),
 .UNSPECIFIED.) ;
#553=B_SPLINE_CURVE_WITH_KNOTS('',3,(#12277,#12278,#12279,#12280,#12281,
#12282,#12283),.UNSPECIFIED.,.F.,.F.,(4,3,4),(0.,0.0186689879508952,0.03840958766807),
 .UNSPECIFIED.) ;
#554=B_SPLINE_CURVE_WITH_KNOTS('',3,(#12285,#12286,#12287,#12288,#12289,
#12290,#12291),.UNSPECIFIED.,.F.,.F.,(4,3,4),(0.,0.0211615752193719,0.0437139193650708),
 .UNSPECIFIED.) ;
#555=B_SPLINE_CURVE_WITH_KNOTS('',3,(#12292,#12293,#12294,#12295,#12296,
#12297,#12298),.UNSPECIFIED.,.F.,.F.,(4,3,4),(0.,0.0274003599038337,0.0509298041237331),
 .UNSPECIFIED.) ;
#556=B_SPLINE_CURVE_WITH_KNOTS('',3,(#12301,#12302,#12303,#12304,#12305,
#12306,#12307,#12308,#12309,#12310,#12311,#12312,#12313,#12314,#12315,#12316),
 .UNSPECIFIED.,.F.,.F.,(4,3,3,3,3,4),(0.,0.0119556380038084,0.0224119134293328,
0.0318321821221747,0.0533934645702515,0.0580324870841514),.UNSPECIFIED.) ;
#557=B_SPLINE_CURVE_WITH_KNOTS('',3,(#12324,#12325,#12326,#12327,#12328,
#12329,#12330,#12331,#12332,#12333,#12334,#12335,#12336),.UNSPECIFIED.,
 .F.,.F.,(4,3,3,3,4),(0.,0.0189611702963205,0.0294450271990619,0.0495973866637977,
0.0527785820105709),.UNSPECIFIED.) ;
#558=B_SPLINE_CURVE_WITH_KNOTS('',3,(#12338,#12339,#12340,#12341,#12342,
#12343,#12344),.UNSPECIFIED.,.F.,.F.,(4,3,4),(0.,0.0208854143008092,0.0428246780067487),
 .UNSPECIFIED.) ;
#559=B_SPLINE_CURVE_WITH_KNOTS('',3,(#12346,#12347,#12348,#12349,#12350,
#12351,#12352,#12353,#12354,#12355),.UNSPECIFIED.,.F.,.F.,(4,3,3,4),(0.,
0.0246117446194239,0.0505233392813415,0.0534405730663183),.UNSPECIFIED.) ;
#560=B_SPLINE_CURVE_WITH_KNOTS('',3,(#12357,#12358,#12359,#12360,#12361,
#12362,#12363),.UNSPECIFIED.,.F.,.F.,(4,3,4),(0.,0.0280864188477132,0.0520232165124005),
 .UNSPECIFIED.) ;
#561=B_SPLINE_CURVE_WITH_KNOTS('',3,(#12365,#12366,#12367,#12368,#12369,
#12370,#12371),.UNSPECIFIED.,.F.,.F.,(4,3,4),(0.,0.0215752408071767,0.0429475903985937),
 .UNSPECIFIED.) ;
#562=B_SPLINE_CURVE_WITH_KNOTS('',3,(#12373,#12374,#12375,#12376,#12377,
#12378,#12379,#12380,#12381,#12382,#12383,#12384,#12385),.UNSPECIFIED.,
 .F.,.F.,(4,3,3,3,4),(0.,0.0161321376565823,0.0244265641217521,0.0465899314620809,
0.055430671682033),.UNSPECIFIED.) ;
#563=B_SPLINE_CURVE_WITH_KNOTS('',3,(#12393,#12394,#12395,#12396,#12397,
#12398,#12399,#12400,#12401,#12402,#12403,#12404,#12405,#12406,#12407,#12408),
 .UNSPECIFIED.,.F.,.F.,(4,3,3,3,3,4),(0.,0.0114819968961422,0.0243079810619617,
0.0325847915710728,0.0396674571422663,0.0414198473083807),.UNSPECIFIED.) ;
#564=B_SPLINE_CURVE_WITH_KNOTS('',3,(#12410,#12411,#12412,#12413,#12414,
#12415,#12416),.UNSPECIFIED.,.F.,.F.,(4,3,4),(0.,0.0142419556450609,0.0286422433204278),
 .UNSPECIFIED.) ;
#565=B_SPLINE_CURVE_WITH_KNOTS('',3,(#12418,#12419,#12420,#12421,#12422,
#12423,#12424),.UNSPECIFIED.,.F.,.F.,(4,3,4),(0.,0.0155686949793599,0.0329892430022521),
 .UNSPECIFIED.) ;
#566=B_SPLINE_CURVE_WITH_KNOTS('',3,(#12425,#12426,#12427,#12428,#12429,
#12430,#12431,#12432,#12433,#12434,#12435,#12436,#12437),.UNSPECIFIED.,
 .F.,.F.,(4,3,3,3,4),(0.,0.0168788660747152,0.0272942730411942,0.0385456173339853,
0.0488240973210902),.UNSPECIFIED.) ;
#567=B_SPLINE_CURVE_WITH_KNOTS('',3,(#12450,#12451,#12452,#12453,#12454,
#12455,#12456,#12457,#12458,#12459,#12460,#12461,#12462,#12463,#12464,#12465,
#12466,#12467,#12468,#12469,#12470,#12471,#12472,#12473,#12474),
 .UNSPECIFIED.,.F.,.F.,(4,3,3,3,3,3,3,3,4),(0.,0.00569194898760575,0.01123244639831,
0.016542961918724,0.0201111017205057,0.0242173359611551,0.0282109067622345,
0.0320493831348753,0.0344815023961872),.UNSPECIFIED.) ;
#568=B_SPLINE_CURVE_WITH_KNOTS('',3,(#12476,#12477,#12478,#12479,#12480,
#12481,#12482,#12483,#12484,#12485,#12486,#12487,#12488,#12489,#12490,#12491,
#12492,#12493,#12494,#12495,#12496,#12497,#12498,#12499,#12500),
 .UNSPECIFIED.,.F.,.F.,(4,3,3,3,3,3,3,3,4),(0.,0.0041831224210667,0.00846284315641277,
0.0129024287836777,0.0149322446600846,0.0205445691292746,0.026303841906127,
0.0322935838006437,0.0355643694351932),.UNSPECIFIED.) ;
#569=B_SPLINE_CURVE_WITH_KNOTS('',2,(#12612,#12613,#12614),
 .UNSPECIFIED.,.F.,.F.,(3,3),(0.,1.),.UNSPECIFIED.) ;
#570=B_SPLINE_CURVE_WITH_KNOTS('',2,(#12623,#12624,#12625),
 .UNSPECIFIED.,.F.,.F.,(3,3),(0.,1.),.UNSPECIFIED.) ;
#571=B_SPLINE_CURVE_WITH_KNOTS('',2,(#12650,#12651,#12652),
 .UNSPECIFIED.,.F.,.F.,(3,3),(0.,1.),.UNSPECIFIED.) ;
#572=B_SPLINE_CURVE_WITH_KNOTS('',2,(#12673,#12674,#12675),
 .UNSPECIFIED.,.F.,.F.,(3,3),(0.,1.),.UNSPECIFIED.) ;
#573=B_SPLINE_CURVE_WITH_KNOTS('',2,(#12684,#12685,#12686),
 .UNSPECIFIED.,.F.,.F.,(3,3),(0.,1.),.UNSPECIFIED.) ;
#574=B_SPLINE_CURVE_WITH_KNOTS('',2,(#12695,#12696,#12697),
 .UNSPECIFIED.,.F.,.F.,(3,3),(0.,1.),.UNSPECIFIED.) ;
#575=B_SPLINE_CURVE_WITH_KNOTS('',2,(#12706,#12707,#12708),
 .UNSPECIFIED.,.F.,.F.,(3,3),(0.,1.),.UNSPECIFIED.) ;
#576=B_SPLINE_CURVE_WITH_KNOTS('',2,(#12717,#12718,#12719),
 .UNSPECIFIED.,.F.,.F.,(3,3),(0.,1.),.UNSPECIFIED.) ;
#577=B_SPLINE_CURVE_WITH_KNOTS('',2,(#12729,#12730,#12731),
 .UNSPECIFIED.,.F.,.F.,(3,3),(0.,1.),.UNSPECIFIED.) ;
#578=B_SPLINE_CURVE_WITH_KNOTS('',2,(#12740,#12741,#12742),
 .UNSPECIFIED.,.F.,.F.,(3,3),(0.,1.),.UNSPECIFIED.) ;
#579=B_SPLINE_CURVE_WITH_KNOTS('',2,(#12751,#12752,#12753),
 .UNSPECIFIED.,.F.,.F.,(3,3),(0.,1.),.UNSPECIFIED.) ;
#580=B_SPLINE_CURVE_WITH_KNOTS('',2,(#12762,#12763,#12764),
 .UNSPECIFIED.,.F.,.F.,(3,3),(0.,1.),.UNSPECIFIED.) ;
#581=B_SPLINE_CURVE_WITH_KNOTS('',2,(#12773,#12774,#12775),
 .UNSPECIFIED.,.F.,.F.,(3,3),(0.,1.),.UNSPECIFIED.) ;
#582=B_SPLINE_CURVE_WITH_KNOTS('',2,(#12796,#12797,#12798),
 .UNSPECIFIED.,.F.,.F.,(3,3),(0.,1.),.UNSPECIFIED.) ;
#583=B_SPLINE_CURVE_WITH_KNOTS('',2,(#12807,#12808,#12809),
 .UNSPECIFIED.,.F.,.F.,(3,3),(0.,1.),.UNSPECIFIED.) ;
#584=B_SPLINE_CURVE_WITH_KNOTS('',2,(#12818,#12819,#12820),
 .UNSPECIFIED.,.F.,.F.,(3,3),(0.,1.),.UNSPECIFIED.) ;
#585=B_SPLINE_CURVE_WITH_KNOTS('',2,(#12833,#12834,#12835),
 .UNSPECIFIED.,.F.,.F.,(3,3),(0.,1.),.UNSPECIFIED.) ;
#586=B_SPLINE_CURVE_WITH_KNOTS('',2,(#12844,#12845,#12846),
 .UNSPECIFIED.,.F.,.F.,(3,3),(0.,1.),.UNSPECIFIED.) ;
#587=B_SPLINE_CURVE_WITH_KNOTS('',2,(#12855,#12856,#12857),
 .UNSPECIFIED.,.F.,.F.,(3,3),(0.,1.),.UNSPECIFIED.) ;
#588=B_SPLINE_CURVE_WITH_KNOTS('',2,(#12866,#12867,#12868),
 .UNSPECIFIED.,.F.,.F.,(3,3),(0.,1.),.UNSPECIFIED.) ;
#589=B_SPLINE_CURVE_WITH_KNOTS('',2,(#12877,#12878,#12879),
 .UNSPECIFIED.,.F.,.F.,(3,3),(0.,1.),.UNSPECIFIED.) ;
#590=B_SPLINE_CURVE_WITH_KNOTS('',2,(#12888,#12889,#12890),
 .UNSPECIFIED.,.F.,.F.,(3,3),(0.,1.),.UNSPECIFIED.) ;
#591=B_SPLINE_CURVE_WITH_KNOTS('',2,(#12899,#12900,#12901),
 .UNSPECIFIED.,.F.,.F.,(3,3),(0.,1.),.UNSPECIFIED.) ;
#592=B_SPLINE_CURVE_WITH_KNOTS('',2,(#12910,#12911,#12912),
 .UNSPECIFIED.,.F.,.F.,(3,3),(0.,1.),.UNSPECIFIED.) ;
#593=B_SPLINE_CURVE_WITH_KNOTS('',2,(#12921,#12922,#12923),
 .UNSPECIFIED.,.F.,.F.,(3,3),(0.,1.),.UNSPECIFIED.) ;
#594=B_SPLINE_CURVE_WITH_KNOTS('',2,(#12932,#12933,#12934),
 .UNSPECIFIED.,.F.,.F.,(3,3),(0.,1.),.UNSPECIFIED.) ;
#595=B_SPLINE_CURVE_WITH_KNOTS('',2,(#12943,#12944,#12945),
 .UNSPECIFIED.,.F.,.F.,(3,3),(0.,1.),.UNSPECIFIED.) ;
#596=B_SPLINE_CURVE_WITH_KNOTS('',2,(#12954,#12955,#12956),
 .UNSPECIFIED.,.F.,.F.,(3,3),(0.,1.),.UNSPECIFIED.) ;
#597=B_SPLINE_CURVE_WITH_KNOTS('',2,(#12965,#12966,#12967),
 .UNSPECIFIED.,.F.,.F.,(3,3),(0.,1.),.UNSPECIFIED.) ;
#598=B_SPLINE_CURVE_WITH_KNOTS('',2,(#12976,#12977,#12978),
 .UNSPECIFIED.,.F.,.F.,(3,3),(0.,1.),.UNSPECIFIED.) ;
#599=B_SPLINE_CURVE_WITH_KNOTS('',2,(#12988,#12989,#12990),
 .UNSPECIFIED.,.F.,.F.,(3,3),(0.,1.),.UNSPECIFIED.) ;
#600=B_SPLINE_CURVE_WITH_KNOTS('',2,(#12999,#13000,#13001),
 .UNSPECIFIED.,.F.,.F.,(3,3),(0.,1.),.UNSPECIFIED.) ;
#601=B_SPLINE_CURVE_WITH_KNOTS('',2,(#13010,#13011,#13012),
 .UNSPECIFIED.,.F.,.F.,(3,3),(0.,1.),.UNSPECIFIED.) ;
#602=B_SPLINE_CURVE_WITH_KNOTS('',2,(#13021,#13022,#13023),
 .UNSPECIFIED.,.F.,.F.,(3,3),(0.,1.),.UNSPECIFIED.) ;
#603=B_SPLINE_CURVE_WITH_KNOTS('',2,(#13032,#13033,#13034),
 .UNSPECIFIED.,.F.,.F.,(3,3),(0.,1.),.UNSPECIFIED.) ;
#604=B_SPLINE_CURVE_WITH_KNOTS('',2,(#13043,#13044,#13045),
 .UNSPECIFIED.,.F.,.F.,(3,3),(0.,1.),.UNSPECIFIED.) ;
#605=B_SPLINE_CURVE_WITH_KNOTS('',2,(#13054,#13055,#13056),
 .UNSPECIFIED.,.F.,.F.,(3,3),(0.,1.),.UNSPECIFIED.) ;
#606=B_SPLINE_CURVE_WITH_KNOTS('',2,(#13065,#13066,#13067),
 .UNSPECIFIED.,.F.,.F.,(3,3),(0.,1.),.UNSPECIFIED.) ;
#607=B_SPLINE_CURVE_WITH_KNOTS('',2,(#13076,#13077,#13078),
 .UNSPECIFIED.,.F.,.F.,(3,3),(0.,1.),.UNSPECIFIED.) ;
#608=B_SPLINE_CURVE_WITH_KNOTS('',2,(#13087,#13088,#13089),
 .UNSPECIFIED.,.F.,.F.,(3,3),(0.,1.),.UNSPECIFIED.) ;
#609=B_SPLINE_CURVE_WITH_KNOTS('',2,(#13098,#13099,#13100),
 .UNSPECIFIED.,.F.,.F.,(3,3),(0.,1.),.UNSPECIFIED.) ;
#610=B_SPLINE_CURVE_WITH_KNOTS('',2,(#13109,#13110,#13111),
 .UNSPECIFIED.,.F.,.F.,(3,3),(0.,1.),.UNSPECIFIED.) ;
#611=B_SPLINE_CURVE_WITH_KNOTS('',2,(#13120,#13121,#13122),
 .UNSPECIFIED.,.F.,.F.,(3,3),(0.,1.),.UNSPECIFIED.) ;
#612=B_SPLINE_CURVE_WITH_KNOTS('',2,(#13131,#13132,#13133),
 .UNSPECIFIED.,.F.,.F.,(3,3),(0.,1.),.UNSPECIFIED.) ;
#613=B_SPLINE_CURVE_WITH_KNOTS('',2,(#13142,#13143,#13144),
 .UNSPECIFIED.,.F.,.F.,(3,3),(0.,1.),.UNSPECIFIED.) ;
#614=B_SPLINE_CURVE_WITH_KNOTS('',2,(#13155,#13156,#13157),
 .UNSPECIFIED.,.F.,.F.,(3,3),(0.,1.),.UNSPECIFIED.) ;
#615=B_SPLINE_CURVE_WITH_KNOTS('',2,(#13205,#13206,#13207),
 .UNSPECIFIED.,.F.,.F.,(3,3),(0.,1.),.UNSPECIFIED.) ;
#616=B_SPLINE_CURVE_WITH_KNOTS('',2,(#13216,#13217,#13218),
 .UNSPECIFIED.,.F.,.F.,(3,3),(0.,1.),.UNSPECIFIED.) ;
#617=B_SPLINE_CURVE_WITH_KNOTS('',3,(#13280,#13281,#13282,#13283,#13284,
#13285),.UNSPECIFIED.,.F.,.F.,(4,1,1,4),(0.513473762730163,0.746551820444979,
0.901937192254856,1.05732256406473),.UNSPECIFIED.) ;
#618=B_SPLINE_CURVE_WITH_KNOTS('',3,(#13286,#13287,#13288,#13289,#13290,
#13291),.UNSPECIFIED.,.F.,.F.,(4,1,1,4),(-1.05732256406473,-0.901937192254856,
-0.746551820444979,-0.513473762730163),.UNSPECIFIED.) ;
#619=B_SPLINE_CURVE_WITH_KNOTS('',3,(#13296,#13297,#13298,#13299,#13300,
#13301),.UNSPECIFIED.,.F.,.F.,(4,1,1,4),(2.08427008952506,2.23965546133494,
2.39504083314481,2.62811889085963),.UNSPECIFIED.) ;
#620=B_SPLINE_CURVE_WITH_KNOTS('',3,(#13305,#13306,#13307,#13308,#13309,
#13310),.UNSPECIFIED.,.F.,.F.,(4,1,1,4),(3.65506641631996,3.88814447403477,
4.04352984584465,4.19891521765453),.UNSPECIFIED.) ;
#621=B_SPLINE_CURVE_WITH_KNOTS('',3,(#13314,#13315,#13316,#13317,#13318,
#13319),.UNSPECIFIED.,.F.,.F.,(4,1,1,4),(-1.05732256406473,-0.901937192254856,
-0.746551820444979,-0.513473762730164),.UNSPECIFIED.) ;
#622=B_SPLINE_CURVE_WITH_KNOTS('',3,(#13365,#13366,#13367,#13368,#13369,
#13370),.UNSPECIFIED.,.F.,.F.,(4,1,1,4),(0.513473762730164,0.746551820444979,
0.901937192254856,1.05732256406473),.UNSPECIFIED.) ;
#623=B_SPLINE_CURVE_WITH_KNOTS('',3,(#13408,#13409,#13410,#13411,#13412,
#13413),.UNSPECIFIED.,.F.,.F.,(4,1,1,4),(-4.19891521765453,-4.04352984584465,
-3.88814447403477,-3.65506641631996),.UNSPECIFIED.) ;
#624=B_SPLINE_CURVE_WITH_KNOTS('',3,(#13451,#13452,#13453,#13454,#13455,
#13456),.UNSPECIFIED.,.F.,.F.,(4,1,1,4),(-2.62811889085963,-2.39504083314481,
-2.23965546133494,-2.08427008952506),.UNSPECIFIED.) ;
#691=FACE_BOUND('',#1573,.T.) ;
#692=FACE_BOUND('',#1585,.T.) ;
#693=FACE_BOUND('',#1586,.T.) ;
#694=FACE_BOUND('',#1587,.T.) ;
#695=FACE_BOUND('',#1588,.T.) ;
#696=FACE_BOUND('',#1589,.T.) ;
#697=FACE_BOUND('',#1590,.T.) ;
#698=FACE_BOUND('',#1591,.T.) ;
#699=FACE_BOUND('',#1592,.T.) ;
#700=FACE_BOUND('',#1691,.T.) ;
#701=FACE_BOUND('',#1693,.T.) ;
#702=FACE_BOUND('',#1709,.T.) ;
#703=FACE_BOUND('',#1711,.T.) ;
#704=FACE_BOUND('',#1713,.T.) ;
#705=FACE_BOUND('',#1715,.T.) ;
#706=FACE_BOUND('',#1725,.T.) ;
#707=FACE_BOUND('',#1731,.T.) ;
#708=FACE_BOUND('',#1734,.T.) ;
#709=FACE_BOUND('',#1737,.T.) ;
#710=FACE_BOUND('',#1740,.T.) ;
#711=FACE_BOUND('',#1743,.T.) ;
#712=FACE_BOUND('',#1746,.T.) ;
#713=FACE_BOUND('',#1749,.T.) ;
#714=FACE_BOUND('',#1750,.T.) ;
#715=FACE_BOUND('',#1751,.T.) ;
#716=FACE_BOUND('',#1752,.T.) ;
#717=FACE_BOUND('',#1753,.T.) ;
#718=FACE_BOUND('',#1759,.T.) ;
#747=PLANE('',#8346) ;
#748=PLANE('',#8348) ;
#749=PLANE('',#8349) ;
#750=PLANE('',#8351) ;
#751=PLANE('',#8352) ;
#752=PLANE('',#8354) ;
#753=PLANE('',#8355) ;
#754=PLANE('',#8357) ;
#755=PLANE('',#8387) ;
#756=PLANE('',#8388) ;
#757=PLANE('',#8389) ;
#758=PLANE('',#8390) ;
#759=PLANE('',#8391) ;
#760=PLANE('',#8392) ;
#761=PLANE('',#8393) ;
#762=PLANE('',#8394) ;
#763=PLANE('',#8395) ;
#764=PLANE('',#8396) ;
#765=PLANE('',#8397) ;
#766=PLANE('',#8398) ;
#767=PLANE('',#8399) ;
#768=PLANE('',#8400) ;
#769=PLANE('',#8401) ;
#770=PLANE('',#8402) ;
#771=PLANE('',#8403) ;
#772=PLANE('',#8404) ;
#773=PLANE('',#8405) ;
#774=PLANE('',#8406) ;
#775=PLANE('',#8407) ;
#776=PLANE('',#8408) ;
#777=PLANE('',#8409) ;
#778=PLANE('',#8410) ;
#779=PLANE('',#8411) ;
#780=PLANE('',#8412) ;
#781=PLANE('',#8413) ;
#782=PLANE('',#8414) ;
#783=PLANE('',#8415) ;
#784=PLANE('',#8416) ;
#785=PLANE('',#8417) ;
#786=PLANE('',#8418) ;
#787=PLANE('',#8419) ;
#788=PLANE('',#8420) ;
#789=PLANE('',#8421) ;
#790=PLANE('',#8422) ;
#791=PLANE('',#8423) ;
#792=PLANE('',#8424) ;
#793=PLANE('',#8425) ;
#794=PLANE('',#8426) ;
#795=PLANE('',#8427) ;
#796=PLANE('',#8428) ;
#797=PLANE('',#8429) ;
#798=PLANE('',#8430) ;
#799=PLANE('',#8431) ;
#800=PLANE('',#8432) ;
#801=PLANE('',#8433) ;
#802=PLANE('',#8434) ;
#803=PLANE('',#8438) ;
#804=PLANE('',#8440) ;
#805=PLANE('',#8475) ;
#806=PLANE('',#8477) ;
#807=PLANE('',#8479) ;
#808=PLANE('',#8481) ;
#809=PLANE('',#8503) ;
#810=PLANE('',#8517) ;
#811=PLANE('',#8520) ;
#812=PLANE('',#8525) ;
#813=PLANE('',#8529) ;
#814=PLANE('',#8534) ;
#815=PLANE('',#8538) ;
#816=PLANE('',#8541) ;
#817=PLANE('',#8550) ;
#989=CYLINDRICAL_SURFACE('',#8358,15.5) ;
#990=CYLINDRICAL_SURFACE('',#8435,15.1) ;
#991=CYLINDRICAL_SURFACE('',#8441,15.5) ;
#992=CYLINDRICAL_SURFACE('',#8455,4.) ;
#993=CYLINDRICAL_SURFACE('',#8461,4.) ;
#994=CYLINDRICAL_SURFACE('',#8467,4.) ;
#995=CYLINDRICAL_SURFACE('',#8473,4.) ;
#996=CYLINDRICAL_SURFACE('',#8483,2.25) ;
#997=CYLINDRICAL_SURFACE('',#8485,2.25) ;
#998=CYLINDRICAL_SURFACE('',#8487,2.25) ;
#999=CYLINDRICAL_SURFACE('',#8489,2.25) ;
#1000=CYLINDRICAL_SURFACE('',#8491,1.65) ;
#1001=CYLINDRICAL_SURFACE('',#8494,1.65) ;
#1002=CYLINDRICAL_SURFACE('',#8497,1.65) ;
#1003=CYLINDRICAL_SURFACE('',#8500,1.65) ;
#1004=CYLINDRICAL_SURFACE('',#8509,8.6) ;
#1005=CYLINDRICAL_SURFACE('',#8511,8.6) ;
#1006=CYLINDRICAL_SURFACE('',#8513,8.6) ;
#1007=CYLINDRICAL_SURFACE('',#8515,8.6) ;
#1008=CYLINDRICAL_SURFACE('',#8519,15.5) ;
#1009=CYLINDRICAL_SURFACE('',#8523,12.6) ;
#1010=CYLINDRICAL_SURFACE('',#8527,12.) ;
#1011=CYLINDRICAL_SURFACE('',#8532,12.6) ;
#1012=CYLINDRICAL_SURFACE('',#8536,12.) ;
#1013=CYLINDRICAL_SURFACE('',#8539,12.) ;
#1014=CYLINDRICAL_SURFACE('',#8545,25.5) ;
#1015=CYLINDRICAL_SURFACE('',#8551,12.) ;
#1097=FACE_OUTER_BOUND('',#1544,.T.) ;
#1098=FACE_OUTER_BOUND('',#1545,.T.) ;
#1099=FACE_OUTER_BOUND('',#1546,.T.) ;
#1100=FACE_OUTER_BOUND('',#1547,.T.) ;
#1101=FACE_OUTER_BOUND('',#1548,.T.) ;
#1102=FACE_OUTER_BOUND('',#1549,.T.) ;
#1103=FACE_OUTER_BOUND('',#1550,.T.) ;
#1104=FACE_OUTER_BOUND('',#1551,.T.) ;
#1105=FACE_OUTER_BOUND('',#1552,.T.) ;
#1106=FACE_OUTER_BOUND('',#1553,.T.) ;
#1107=FACE_OUTER_BOUND('',#1554,.T.) ;
#1108=FACE_OUTER_BOUND('',#1555,.T.) ;
#1109=FACE_OUTER_BOUND('',#1556,.T.) ;
#1110=FACE_OUTER_BOUND('',#1557,.T.) ;
#1111=FACE_OUTER_BOUND('',#1558,.T.) ;
#1112=FACE_OUTER_BOUND('',#1559,.T.) ;
#1113=FACE_OUTER_BOUND('',#1560,.T.) ;
#1114=FACE_OUTER_BOUND('',#1561,.T.) ;
#1115=FACE_OUTER_BOUND('',#1562,.T.) ;
#1116=FACE_OUTER_BOUND('',#1563,.T.) ;
#1117=FACE_OUTER_BOUND('',#1564,.T.) ;
#1118=FACE_OUTER_BOUND('',#1565,.T.) ;
#1119=FACE_OUTER_BOUND('',#1566,.T.) ;
#1120=FACE_OUTER_BOUND('',#1567,.T.) ;
#1121=FACE_OUTER_BOUND('',#1568,.T.) ;
#1122=FACE_OUTER_BOUND('',#1569,.T.) ;
#1123=FACE_OUTER_BOUND('',#1570,.T.) ;
#1124=FACE_OUTER_BOUND('',#1571,.T.) ;
#1125=FACE_OUTER_BOUND('',#1572,.T.) ;
#1126=FACE_OUTER_BOUND('',#1574,.T.) ;
#1127=FACE_OUTER_BOUND('',#1575,.T.) ;
#1128=FACE_OUTER_BOUND('',#1576,.T.) ;
#1129=FACE_OUTER_BOUND('',#1577,.T.) ;
#1130=FACE_OUTER_BOUND('',#1578,.T.) ;
#1131=FACE_OUTER_BOUND('',#1579,.T.) ;
#1132=FACE_OUTER_BOUND('',#1580,.T.) ;
#1133=FACE_OUTER_BOUND('',#1581,.T.) ;
#1134=FACE_OUTER_BOUND('',#1582,.T.) ;
#1135=FACE_OUTER_BOUND('',#1583,.T.) ;
#1136=FACE_OUTER_BOUND('',#1584,.T.) ;
#1137=FACE_OUTER_BOUND('',#1593,.T.) ;
#1138=FACE_OUTER_BOUND('',#1594,.T.) ;
#1139=FACE_OUTER_BOUND('',#1595,.T.) ;
#1140=FACE_OUTER_BOUND('',#1596,.T.) ;
#1141=FACE_OUTER_BOUND('',#1597,.T.) ;
#1142=FACE_OUTER_BOUND('',#1598,.T.) ;
#1143=FACE_OUTER_BOUND('',#1599,.T.) ;
#1144=FACE_OUTER_BOUND('',#1600,.T.) ;
#1145=FACE_OUTER_BOUND('',#1601,.T.) ;
#1146=FACE_OUTER_BOUND('',#1602,.T.) ;
#1147=FACE_OUTER_BOUND('',#1603,.T.) ;
#1148=FACE_OUTER_BOUND('',#1604,.T.) ;
#1149=FACE_OUTER_BOUND('',#1605,.T.) ;
#1150=FACE_OUTER_BOUND('',#1606,.T.) ;
#1151=FACE_OUTER_BOUND('',#1607,.T.) ;
#1152=FACE_OUTER_BOUND('',#1608,.T.) ;
#1153=FACE_OUTER_BOUND('',#1609,.T.) ;
#1154=FACE_OUTER_BOUND('',#1610,.T.) ;
#1155=FACE_OUTER_BOUND('',#1611,.T.) ;
#1156=FACE_OUTER_BOUND('',#1612,.T.) ;
#1157=FACE_OUTER_BOUND('',#1613,.T.) ;
#1158=FACE_OUTER_BOUND('',#1614,.T.) ;
#1159=FACE_OUTER_BOUND('',#1615,.T.) ;
#1160=FACE_OUTER_BOUND('',#1616,.T.) ;
#1161=FACE_OUTER_BOUND('',#1617,.T.) ;
#1162=FACE_OUTER_BOUND('',#1618,.T.) ;
#1163=FACE_OUTER_BOUND('',#1619,.T.) ;
#1164=FACE_OUTER_BOUND('',#1620,.T.) ;
#1165=FACE_OUTER_BOUND('',#1621,.T.) ;
#1166=FACE_OUTER_BOUND('',#1622,.T.) ;
#1167=FACE_OUTER_BOUND('',#1623,.T.) ;
#1168=FACE_OUTER_BOUND('',#1624,.T.) ;
#1169=FACE_OUTER_BOUND('',#1625,.T.) ;
#1170=FACE_OUTER_BOUND('',#1626,.T.) ;
#1171=FACE_OUTER_BOUND('',#1627,.T.) ;
#1172=FACE_OUTER_BOUND('',#1628,.T.) ;
#1173=FACE_OUTER_BOUND('',#1629,.T.) ;
#1174=FACE_OUTER_BOUND('',#1630,.T.) ;
#1175=FACE_OUTER_BOUND('',#1631,.T.) ;
#1176=FACE_OUTER_BOUND('',#1632,.T.) ;
#1177=FACE_OUTER_BOUND('',#1633,.T.) ;
#1178=FACE_OUTER_BOUND('',#1634,.T.) ;
#1179=FACE_OUTER_BOUND('',#1635,.T.) ;
#1180=FACE_OUTER_BOUND('',#1636,.T.) ;
#1181=FACE_OUTER_BOUND('',#1637,.T.) ;
#1182=FACE_OUTER_BOUND('',#1638,.T.) ;
#1183=FACE_OUTER_BOUND('',#1639,.T.) ;
#1184=FACE_OUTER_BOUND('',#1640,.T.) ;
#1185=FACE_OUTER_BOUND('',#1641,.T.) ;
#1186=FACE_OUTER_BOUND('',#1642,.T.) ;
#1187=FACE_OUTER_BOUND('',#1643,.T.) ;
#1188=FACE_OUTER_BOUND('',#1644,.T.) ;
#1189=FACE_OUTER_BOUND('',#1645,.T.) ;
#1190=FACE_OUTER_BOUND('',#1646,.T.) ;
#1191=FACE_OUTER_BOUND('',#1647,.T.) ;
#1192=FACE_OUTER_BOUND('',#1648,.T.) ;
#1193=FACE_OUTER_BOUND('',#1649,.T.) ;
#1194=FACE_OUTER_BOUND('',#1650,.T.) ;
#1195=FACE_OUTER_BOUND('',#1651,.T.) ;
#1196=FACE_OUTER_BOUND('',#1652,.T.) ;
#1197=FACE_OUTER_BOUND('',#1653,.T.) ;
#1198=FACE_OUTER_BOUND('',#1654,.T.) ;
#1199=FACE_OUTER_BOUND('',#1655,.T.) ;
#1200=FACE_OUTER_BOUND('',#1656,.T.) ;
#1201=FACE_OUTER_BOUND('',#1657,.T.) ;
#1202=FACE_OUTER_BOUND('',#1658,.T.) ;
#1203=FACE_OUTER_BOUND('',#1659,.T.) ;
#1204=FACE_OUTER_BOUND('',#1660,.T.) ;
#1205=FACE_OUTER_BOUND('',#1661,.T.) ;
#1206=FACE_OUTER_BOUND('',#1662,.T.) ;
#1207=FACE_OUTER_BOUND('',#1663,.T.) ;
#1208=FACE_OUTER_BOUND('',#1664,.T.) ;
#1209=FACE_OUTER_BOUND('',#1665,.T.) ;
#1210=FACE_OUTER_BOUND('',#1666,.T.) ;
#1211=FACE_OUTER_BOUND('',#1667,.T.) ;
#1212=FACE_OUTER_BOUND('',#1668,.T.) ;
#1213=FACE_OUTER_BOUND('',#1669,.T.) ;
#1214=FACE_OUTER_BOUND('',#1670,.T.) ;
#1215=FACE_OUTER_BOUND('',#1671,.T.) ;
#1216=FACE_OUTER_BOUND('',#1672,.T.) ;
#1217=FACE_OUTER_BOUND('',#1673,.T.) ;
#1218=FACE_OUTER_BOUND('',#1674,.T.) ;
#1219=FACE_OUTER_BOUND('',#1675,.T.) ;
#1220=FACE_OUTER_BOUND('',#1676,.T.) ;
#1221=FACE_OUTER_BOUND('',#1677,.T.) ;
#1222=FACE_OUTER_BOUND('',#1678,.T.) ;
#1223=FACE_OUTER_BOUND('',#1679,.T.) ;
#1224=FACE_OUTER_BOUND('',#1680,.T.) ;
#1225=FACE_OUTER_BOUND('',#1681,.T.) ;
#1226=FACE_OUTER_BOUND('',#1682,.T.) ;
#1227=FACE_OUTER_BOUND('',#1683,.T.) ;
#1228=FACE_OUTER_BOUND('',#1684,.T.) ;
#1229=FACE_OUTER_BOUND('',#1685,.T.) ;
#1230=FACE_OUTER_BOUND('',#1686,.T.) ;
#1231=FACE_OUTER_BOUND('',#1687,.T.) ;
#1232=FACE_OUTER_BOUND('',#1688,.T.) ;
#1233=FACE_OUTER_BOUND('',#1689,.T.) ;
#1234=FACE_OUTER_BOUND('',#1690,.T.) ;
#1235=FACE_OUTER_BOUND('',#1692,.T.) ;
#1236=FACE_OUTER_BOUND('',#1694,.T.) ;
#1237=FACE_OUTER_BOUND('',#1695,.T.) ;
#1238=FACE_OUTER_BOUND('',#1696,.T.) ;
#1239=FACE_OUTER_BOUND('',#1697,.T.) ;
#1240=FACE_OUTER_BOUND('',#1698,.T.) ;
#1241=FACE_OUTER_BOUND('',#1699,.T.) ;
#1242=FACE_OUTER_BOUND('',#1700,.T.) ;
#1243=FACE_OUTER_BOUND('',#1701,.T.) ;
#1244=FACE_OUTER_BOUND('',#1702,.T.) ;
#1245=FACE_OUTER_BOUND('',#1703,.T.) ;
#1246=FACE_OUTER_BOUND('',#1704,.T.) ;
#1247=FACE_OUTER_BOUND('',#1705,.T.) ;
#1248=FACE_OUTER_BOUND('',#1706,.T.) ;
#1249=FACE_OUTER_BOUND('',#1707,.T.) ;
#1250=FACE_OUTER_BOUND('',#1708,.T.) ;
#1251=FACE_OUTER_BOUND('',#1710,.T.) ;
#1252=FACE_OUTER_BOUND('',#1712,.T.) ;
#1253=FACE_OUTER_BOUND('',#1714,.T.) ;
#1254=FACE_OUTER_BOUND('',#1716,.T.) ;
#1255=FACE_OUTER_BOUND('',#1717,.T.) ;
#1256=FACE_OUTER_BOUND('',#1718,.T.) ;
#1257=FACE_OUTER_BOUND('',#1719,.T.) ;
#1258=FACE_OUTER_BOUND('',#1720,.T.) ;
#1259=FACE_OUTER_BOUND('',#1721,.T.) ;
#1260=FACE_OUTER_BOUND('',#1722,.T.) ;
#1261=FACE_OUTER_BOUND('',#1723,.T.) ;
#1262=FACE_OUTER_BOUND('',#1724,.T.) ;
#1263=FACE_OUTER_BOUND('',#1726,.T.) ;
#1264=FACE_OUTER_BOUND('',#1727,.T.) ;
#1265=FACE_OUTER_BOUND('',#1728,.T.) ;
#1266=FACE_OUTER_BOUND('',#1729,.T.) ;
#1267=FACE_OUTER_BOUND('',#1730,.T.) ;
#1268=FACE_OUTER_BOUND('',#1732,.T.) ;
#1269=FACE_OUTER_BOUND('',#1733,.T.) ;
#1270=FACE_OUTER_BOUND('',#1735,.T.) ;
#1271=FACE_OUTER_BOUND('',#1736,.T.) ;
#1272=FACE_OUTER_BOUND('',#1738,.T.) ;
#1273=FACE_OUTER_BOUND('',#1739,.T.) ;
#1274=FACE_OUTER_BOUND('',#1741,.T.) ;
#1275=FACE_OUTER_BOUND('',#1742,.T.) ;
#1276=FACE_OUTER_BOUND('',#1744,.T.) ;
#1277=FACE_OUTER_BOUND('',#1745,.T.) ;
#1278=FACE_OUTER_BOUND('',#1747,.T.) ;
#1279=FACE_OUTER_BOUND('',#1748,.T.) ;
#1280=FACE_OUTER_BOUND('',#1754,.T.) ;
#1281=FACE_OUTER_BOUND('',#1755,.T.) ;
#1282=FACE_OUTER_BOUND('',#1756,.T.) ;
#1283=FACE_OUTER_BOUND('',#1757,.T.) ;
#1284=FACE_OUTER_BOUND('',#1758,.T.) ;
#1285=FACE_OUTER_BOUND('',#1760,.T.) ;
#1544=EDGE_LOOP('',(#5525,#5526,#5527,#5528)) ;
#1545=EDGE_LOOP('',(#5529,#5530,#5531,#5532)) ;
#1546=EDGE_LOOP('',(#5533,#5534,#5535,#5536)) ;
#1547=EDGE_LOOP('',(#5537,#5538,#5539,#5540)) ;
#1548=EDGE_LOOP('',(#5541,#5542,#5543,#5544)) ;
#1549=EDGE_LOOP('',(#5545,#5546,#5547,#5548)) ;
#1550=EDGE_LOOP('',(#5549,#5550,#5551,#5552)) ;
#1551=EDGE_LOOP('',(#5553,#5554,#5555,#5556)) ;
#1552=EDGE_LOOP('',(#5557,#5558,#5559,#5560)) ;
#1553=EDGE_LOOP('',(#5561,#5562,#5563,#5564)) ;
#1554=EDGE_LOOP('',(#5565,#5566,#5567,#5568)) ;
#1555=EDGE_LOOP('',(#5569,#5570,#5571,#5572)) ;
#1556=EDGE_LOOP('',(#5573,#5574,#5575,#5576)) ;
#1557=EDGE_LOOP('',(#5577,#5578,#5579,#5580)) ;
#1558=EDGE_LOOP('',(#5581,#5582,#5583,#5584)) ;
#1559=EDGE_LOOP('',(#5585,#5586,#5587,#5588)) ;
#1560=EDGE_LOOP('',(#5589,#5590,#5591,#5592)) ;
#1561=EDGE_LOOP('',(#5593,#5594,#5595,#5596)) ;
#1562=EDGE_LOOP('',(#5597,#5598,#5599,#5600)) ;
#1563=EDGE_LOOP('',(#5601,#5602,#5603,#5604)) ;
#1564=EDGE_LOOP('',(#5605,#5606,#5607,#5608)) ;
#1565=EDGE_LOOP('',(#5609,#5610,#5611,#5612)) ;
#1566=EDGE_LOOP('',(#5613,#5614,#5615,#5616)) ;
#1567=EDGE_LOOP('',(#5617,#5618,#5619,#5620)) ;
#1568=EDGE_LOOP('',(#5621,#5622,#5623,#5624)) ;
#1569=EDGE_LOOP('',(#5625,#5626,#5627,#5628)) ;
#1570=EDGE_LOOP('',(#5629,#5630,#5631,#5632)) ;
#1571=EDGE_LOOP('',(#5633,#5634,#5635,#5636)) ;
#1572=EDGE_LOOP('',(#5637,#5638,#5639,#5640,#5641,#5642,#5643,#5644,#5645,
#5646,#5647,#5648,#5649,#5650,#5651,#5652,#5653,#5654,#5655)) ;
#1573=EDGE_LOOP('',(#5656,#5657,#5658,#5659,#5660,#5661,#5662,#5663,#5664)) ;
#1574=EDGE_LOOP('',(#5665,#5666,#5667,#5668)) ;
#1575=EDGE_LOOP('',(#5669,#5670,#5671,#5672)) ;
#1576=EDGE_LOOP('',(#5673,#5674,#5675,#5676)) ;
#1577=EDGE_LOOP('',(#5677,#5678,#5679,#5680)) ;
#1578=EDGE_LOOP('',(#5681,#5682,#5683,#5684)) ;
#1579=EDGE_LOOP('',(#5685,#5686,#5687,#5688)) ;
#1580=EDGE_LOOP('',(#5689,#5690,#5691,#5692)) ;
#1581=EDGE_LOOP('',(#5693,#5694,#5695,#5696)) ;
#1582=EDGE_LOOP('',(#5697,#5698,#5699,#5700)) ;
#1583=EDGE_LOOP('',(#5701,#5702,#5703,#5704,#5705,#5706,#5707,#5708,#5709)) ;
#1584=EDGE_LOOP('',(#5710,#5711,#5712,#5713)) ;
#1585=EDGE_LOOP('',(#5714,#5715,#5716,#5717,#5718,#5719,#5720,#5721,#5722,
#5723,#5724,#5725,#5726,#5727,#5728)) ;
#1586=EDGE_LOOP('',(#5729,#5730,#5731,#5732,#5733,#5734,#5735,#5736,#5737,
#5738,#5739,#5740,#5741,#5742,#5743,#5744,#5745,#5746,#5747,#5748,#5749,
#5750,#5751,#5752,#5753,#5754,#5755,#5756,#5757,#5758,#5759,#5760,#5761,
#5762,#5763)) ;
#1587=EDGE_LOOP('',(#5764,#5765,#5766,#5767,#5768,#5769,#5770,#5771,#5772,
#5773,#5774,#5775,#5776,#5777,#5778,#5779,#5780)) ;
#1588=EDGE_LOOP('',(#5781,#5782,#5783,#5784,#5785,#5786,#5787,#5788,#5789,
#5790,#5791,#5792,#5793,#5794,#5795)) ;
#1589=EDGE_LOOP('',(#5796,#5797,#5798,#5799)) ;
#1590=EDGE_LOOP('',(#5800,#5801,#5802,#5803)) ;
#1591=EDGE_LOOP('',(#5804,#5805,#5806,#5807,#5808,#5809,#5810,#5811,#5812)) ;
#1592=EDGE_LOOP('',(#5813,#5814,#5815,#5816,#5817,#5818,#5819,#5820,#5821,
#5822,#5823,#5824,#5825,#5826,#5827,#5828,#5829,#5830,#5831)) ;
#1593=EDGE_LOOP('',(#5832,#5833,#5834,#5835)) ;
#1594=EDGE_LOOP('',(#5836,#5837,#5838,#5839)) ;
#1595=EDGE_LOOP('',(#5840,#5841,#5842,#5843)) ;
#1596=EDGE_LOOP('',(#5844,#5845,#5846,#5847)) ;
#1597=EDGE_LOOP('',(#5848,#5849,#5850,#5851)) ;
#1598=EDGE_LOOP('',(#5852,#5853,#5854,#5855)) ;
#1599=EDGE_LOOP('',(#5856,#5857,#5858,#5859)) ;
#1600=EDGE_LOOP('',(#5860,#5861,#5862,#5863)) ;
#1601=EDGE_LOOP('',(#5864,#5865,#5866,#5867)) ;
#1602=EDGE_LOOP('',(#5868,#5869,#5870,#5871)) ;
#1603=EDGE_LOOP('',(#5872,#5873,#5874,#5875)) ;
#1604=EDGE_LOOP('',(#5876,#5877,#5878,#5879)) ;
#1605=EDGE_LOOP('',(#5880,#5881,#5882,#5883)) ;
#1606=EDGE_LOOP('',(#5884,#5885,#5886,#5887)) ;
#1607=EDGE_LOOP('',(#5888,#5889,#5890,#5891)) ;
#1608=EDGE_LOOP('',(#5892,#5893,#5894,#5895)) ;
#1609=EDGE_LOOP('',(#5896,#5897,#5898,#5899)) ;
#1610=EDGE_LOOP('',(#5900,#5901,#5902,#5903)) ;
#1611=EDGE_LOOP('',(#5904,#5905,#5906,#5907)) ;
#1612=EDGE_LOOP('',(#5908,#5909,#5910,#5911)) ;
#1613=EDGE_LOOP('',(#5912,#5913,#5914,#5915)) ;
#1614=EDGE_LOOP('',(#5916,#5917,#5918,#5919)) ;
#1615=EDGE_LOOP('',(#5920,#5921,#5922,#5923)) ;
#1616=EDGE_LOOP('',(#5924,#5925,#5926,#5927)) ;
#1617=EDGE_LOOP('',(#5928,#5929,#5930,#5931)) ;
#1618=EDGE_LOOP('',(#5932,#5933,#5934,#5935,#5936,#5937,#5938,#5939,#5940,
#5941,#5942,#5943,#5944,#5945,#5946)) ;
#1619=EDGE_LOOP('',(#5947,#5948,#5949,#5950)) ;
#1620=EDGE_LOOP('',(#5951,#5952,#5953,#5954)) ;
#1621=EDGE_LOOP('',(#5955,#5956,#5957,#5958)) ;
#1622=EDGE_LOOP('',(#5959,#5960,#5961,#5962)) ;
#1623=EDGE_LOOP('',(#5963,#5964,#5965,#5966)) ;
#1624=EDGE_LOOP('',(#5967,#5968,#5969,#5970)) ;
#1625=EDGE_LOOP('',(#5971,#5972,#5973,#5974)) ;
#1626=EDGE_LOOP('',(#5975,#5976,#5977,#5978)) ;
#1627=EDGE_LOOP('',(#5979,#5980,#5981,#5982)) ;
#1628=EDGE_LOOP('',(#5983,#5984,#5985,#5986)) ;
#1629=EDGE_LOOP('',(#5987,#5988,#5989,#5990)) ;
#1630=EDGE_LOOP('',(#5991,#5992,#5993,#5994)) ;
#1631=EDGE_LOOP('',(#5995,#5996,#5997,#5998)) ;
#1632=EDGE_LOOP('',(#5999,#6000,#6001,#6002)) ;
#1633=EDGE_LOOP('',(#6003,#6004,#6005,#6006)) ;
#1634=EDGE_LOOP('',(#6007,#6008,#6009,#6010)) ;
#1635=EDGE_LOOP('',(#6011,#6012,#6013,#6014)) ;
#1636=EDGE_LOOP('',(#6015,#6016,#6017,#6018,#6019,#6020,#6021,#6022,#6023,
#6024,#6025,#6026,#6027,#6028,#6029,#6030,#6031)) ;
#1637=EDGE_LOOP('',(#6032,#6033,#6034,#6035)) ;
#1638=EDGE_LOOP('',(#6036,#6037,#6038,#6039)) ;
#1639=EDGE_LOOP('',(#6040,#6041,#6042,#6043)) ;
#1640=EDGE_LOOP('',(#6044,#6045,#6046,#6047)) ;
#1641=EDGE_LOOP('',(#6048,#6049,#6050,#6051)) ;
#1642=EDGE_LOOP('',(#6052,#6053,#6054,#6055)) ;
#1643=EDGE_LOOP('',(#6056,#6057,#6058,#6059)) ;
#1644=EDGE_LOOP('',(#6060,#6061,#6062,#6063)) ;
#1645=EDGE_LOOP('',(#6064,#6065,#6066,#6067)) ;
#1646=EDGE_LOOP('',(#6068,#6069,#6070,#6071)) ;
#1647=EDGE_LOOP('',(#6072,#6073,#6074,#6075)) ;
#1648=EDGE_LOOP('',(#6076,#6077,#6078,#6079)) ;
#1649=EDGE_LOOP('',(#6080,#6081,#6082,#6083)) ;
#1650=EDGE_LOOP('',(#6084,#6085,#6086,#6087)) ;
#1651=EDGE_LOOP('',(#6088,#6089,#6090,#6091)) ;
#1652=EDGE_LOOP('',(#6092,#6093,#6094,#6095)) ;
#1653=EDGE_LOOP('',(#6096,#6097,#6098,#6099)) ;
#1654=EDGE_LOOP('',(#6100,#6101,#6102,#6103)) ;
#1655=EDGE_LOOP('',(#6104,#6105,#6106,#6107)) ;
#1656=EDGE_LOOP('',(#6108,#6109,#6110,#6111)) ;
#1657=EDGE_LOOP('',(#6112,#6113,#6114,#6115)) ;
#1658=EDGE_LOOP('',(#6116,#6117,#6118,#6119)) ;
#1659=EDGE_LOOP('',(#6120,#6121,#6122,#6123)) ;
#1660=EDGE_LOOP('',(#6124,#6125,#6126,#6127)) ;
#1661=EDGE_LOOP('',(#6128,#6129,#6130,#6131)) ;
#1662=EDGE_LOOP('',(#6132,#6133,#6134,#6135)) ;
#1663=EDGE_LOOP('',(#6136,#6137,#6138,#6139)) ;
#1664=EDGE_LOOP('',(#6140,#6141,#6142,#6143)) ;
#1665=EDGE_LOOP('',(#6144,#6145,#6146,#6147)) ;
#1666=EDGE_LOOP('',(#6148,#6149,#6150,#6151)) ;
#1667=EDGE_LOOP('',(#6152,#6153,#6154,#6155)) ;
#1668=EDGE_LOOP('',(#6156,#6157,#6158,#6159)) ;
#1669=EDGE_LOOP('',(#6160,#6161,#6162,#6163)) ;
#1670=EDGE_LOOP('',(#6164,#6165,#6166,#6167)) ;
#1671=EDGE_LOOP('',(#6168,#6169,#6170,#6171)) ;
#1672=EDGE_LOOP('',(#6172,#6173,#6174,#6175,#6176,#6177,#6178,#6179,#6180,
#6181,#6182,#6183,#6184,#6185,#6186,#6187,#6188,#6189,#6190,#6191,#6192,
#6193,#6194,#6195,#6196,#6197,#6198,#6199,#6200,#6201,#6202,#6203,#6204,
#6205,#6206)) ;
#1673=EDGE_LOOP('',(#6207,#6208,#6209,#6210)) ;
#1674=EDGE_LOOP('',(#6211,#6212,#6213,#6214)) ;
#1675=EDGE_LOOP('',(#6215,#6216,#6217,#6218)) ;
#1676=EDGE_LOOP('',(#6219,#6220,#6221,#6222)) ;
#1677=EDGE_LOOP('',(#6223,#6224,#6225,#6226)) ;
#1678=EDGE_LOOP('',(#6227,#6228,#6229,#6230)) ;
#1679=EDGE_LOOP('',(#6231,#6232,#6233,#6234)) ;
#1680=EDGE_LOOP('',(#6235,#6236,#6237,#6238)) ;
#1681=EDGE_LOOP('',(#6239,#6240,#6241,#6242)) ;
#1682=EDGE_LOOP('',(#6243,#6244,#6245,#6246)) ;
#1683=EDGE_LOOP('',(#6247,#6248,#6249,#6250)) ;
#1684=EDGE_LOOP('',(#6251,#6252,#6253,#6254)) ;
#1685=EDGE_LOOP('',(#6255,#6256,#6257,#6258)) ;
#1686=EDGE_LOOP('',(#6259,#6260,#6261,#6262)) ;
#1687=EDGE_LOOP('',(#6263,#6264,#6265,#6266)) ;
#1688=EDGE_LOOP('',(#6267,#6268,#6269,#6270,#6271,#6272,#6273,#6274,#6275,
#6276,#6277,#6278,#6279,#6280,#6281)) ;
#1689=EDGE_LOOP('',(#6282,#6283,#6284,#6285)) ;
#1690=EDGE_LOOP('',(#6286)) ;
#1691=EDGE_LOOP('',(#6287)) ;
#1692=EDGE_LOOP('',(#6288)) ;
#1693=EDGE_LOOP('',(#6289)) ;
#1694=EDGE_LOOP('',(#6290,#6291,#6292,#6293,#6294,#6295,#6296,#6297,#6298)) ;
#1695=EDGE_LOOP('',(#6299,#6300,#6301,#6302,#6303)) ;
#1696=EDGE_LOOP('',(#6304,#6305,#6306,#6307)) ;
#1697=EDGE_LOOP('',(#6308,#6309,#6310,#6311,#6312,#6313,#6314,#6315,#6316,
#6317,#6318,#6319,#6320)) ;
#1698=EDGE_LOOP('',(#6321,#6322,#6323,#6324,#6325,#6326)) ;
#1699=EDGE_LOOP('',(#6327,#6328,#6329,#6330,#6331)) ;
#1700=EDGE_LOOP('',(#6332,#6333,#6334,#6335)) ;
#1701=EDGE_LOOP('',(#6336,#6337,#6338,#6339,#6340,#6341)) ;
#1702=EDGE_LOOP('',(#6342,#6343,#6344,#6345,#6346)) ;
#1703=EDGE_LOOP('',(#6347,#6348,#6349,#6350)) ;
#1704=EDGE_LOOP('',(#6351,#6352,#6353,#6354,#6355,#6356)) ;
#1705=EDGE_LOOP('',(#6357,#6358,#6359,#6360,#6361)) ;
#1706=EDGE_LOOP('',(#6362,#6363,#6364,#6365)) ;
#1707=EDGE_LOOP('',(#6366,#6367,#6368,#6369,#6370,#6371)) ;
#1708=EDGE_LOOP('',(#6372)) ;
#1709=EDGE_LOOP('',(#6373)) ;
#1710=EDGE_LOOP('',(#6374)) ;
#1711=EDGE_LOOP('',(#6375)) ;
#1712=EDGE_LOOP('',(#6376)) ;
#1713=EDGE_LOOP('',(#6377)) ;
#1714=EDGE_LOOP('',(#6378)) ;
#1715=EDGE_LOOP('',(#6379)) ;
#1716=EDGE_LOOP('',(#6380,#6381,#6382,#6383)) ;
#1717=EDGE_LOOP('',(#6384,#6385,#6386,#6387)) ;
#1718=EDGE_LOOP('',(#6388,#6389,#6390,#6391)) ;
#1719=EDGE_LOOP('',(#6392,#6393,#6394,#6395)) ;
#1720=EDGE_LOOP('',(#6396,#6397,#6398,#6399)) ;
#1721=EDGE_LOOP('',(#6400,#6401,#6402,#6403)) ;
#1722=EDGE_LOOP('',(#6404,#6405,#6406,#6407)) ;
#1723=EDGE_LOOP('',(#6408,#6409,#6410,#6411)) ;
#1724=EDGE_LOOP('',(#6412)) ;
#1725=EDGE_LOOP('',(#6413,#6414,#6415,#6416,#6417,#6418,#6419,#6420)) ;
#1726=EDGE_LOOP('',(#6421,#6422,#6423,#6424)) ;
#1727=EDGE_LOOP('',(#6425,#6426,#6427,#6428)) ;
#1728=EDGE_LOOP('',(#6429,#6430,#6431,#6432)) ;
#1729=EDGE_LOOP('',(#6433,#6434,#6435,#6436)) ;
#1730=EDGE_LOOP('',(#6437)) ;
#1731=EDGE_LOOP('',(#6438,#6439,#6440,#6441,#6442,#6443,#6444,#6445,#6446)) ;
#1732=EDGE_LOOP('',(#6447,#6448,#6449,#6450,#6451)) ;
#1733=EDGE_LOOP('',(#6452)) ;
#1734=EDGE_LOOP('',(#6453)) ;
#1735=EDGE_LOOP('',(#6454,#6455,#6456,#6457)) ;
#1736=EDGE_LOOP('',(#6458)) ;
#1737=EDGE_LOOP('',(#6459)) ;
#1738=EDGE_LOOP('',(#6460,#6461,#6462,#6463)) ;
#1739=EDGE_LOOP('',(#6464)) ;
#1740=EDGE_LOOP('',(#6465)) ;
#1741=EDGE_LOOP('',(#6466,#6467,#6468,#6469)) ;
#1742=EDGE_LOOP('',(#6470)) ;
#1743=EDGE_LOOP('',(#6471)) ;
#1744=EDGE_LOOP('',(#6472,#6473,#6474,#6475)) ;
#1745=EDGE_LOOP('',(#6476)) ;
#1746=EDGE_LOOP('',(#6477,#6478,#6479,#6480,#6481,#6482,#6483,#6484)) ;
#1747=EDGE_LOOP('',(#6485,#6486,#6487,#6488)) ;
#1748=EDGE_LOOP('',(#6489)) ;
#1749=EDGE_LOOP('',(#6490)) ;
#1750=EDGE_LOOP('',(#6491)) ;
#1751=EDGE_LOOP('',(#6492)) ;
#1752=EDGE_LOOP('',(#6493)) ;
#1753=EDGE_LOOP('',(#6494)) ;
#1754=EDGE_LOOP('',(#6495,#6496,#6497,#6498)) ;
#1755=EDGE_LOOP('',(#6499,#6500,#6501,#6502)) ;
#1756=EDGE_LOOP('',(#6503,#6504,#6505,#6506)) ;
#1757=EDGE_LOOP('',(#6507,#6508,#6509,#6510)) ;
#1758=EDGE_LOOP('',(#6511)) ;
#1759=EDGE_LOOP('',(#6512)) ;
#1760=EDGE_LOOP('',(#6513,#6514,#6515,#6516)) ;
#2023=LINE('',#11243,#2585) ;
#2024=LINE('',#11248,#2586) ;
#2025=LINE('',#11270,#2587) ;
#2026=LINE('',#11292,#2588) ;
#2027=LINE('',#11314,#2589) ;
#2028=LINE('',#11334,#2590) ;
#2029=LINE('',#11339,#2591) ;
#2030=LINE('',#11358,#2592) ;
#2031=LINE('',#11377,#2593) ;
#2032=LINE('',#11396,#2594) ;
#2033=LINE('',#11415,#2595) ;
#2034=LINE('',#11437,#2596) ;
#2035=LINE('',#11455,#2597) ;
#2036=LINE('',#11475,#2598) ;
#2037=LINE('',#11497,#2599) ;
#2038=LINE('',#11516,#2600) ;
#2039=LINE('',#11532,#2601) ;
#2040=LINE('',#11551,#2602) ;
#2041=LINE('',#11570,#2603) ;
#2042=LINE('',#11608,#2604) ;
#2043=LINE('',#11624,#2605) ;
#2044=LINE('',#11643,#2606) ;
#2045=LINE('',#11668,#2607) ;
#2046=LINE('',#11687,#2608) ;
#2047=LINE('',#11706,#2609) ;
#2048=LINE('',#11728,#2610) ;
#2049=LINE('',#11753,#2611) ;
#2050=LINE('',#11761,#2612) ;
#2051=LINE('',#11762,#2613) ;
#2052=LINE('',#11796,#2614) ;
#2053=LINE('',#11801,#2615) ;
#2054=LINE('',#11806,#2616) ;
#2055=LINE('',#11807,#2617) ;
#2056=LINE('',#11826,#2618) ;
#2057=LINE('',#11845,#2619) ;
#2058=LINE('',#11848,#2620) ;
#2059=LINE('',#11850,#2621) ;
#2060=LINE('',#11851,#2622) ;
#2061=LINE('',#11867,#2623) ;
#2062=LINE('',#11875,#2624) ;
#2063=LINE('',#11876,#2625) ;
#2064=LINE('',#11879,#2626) ;
#2065=LINE('',#11881,#2627) ;
#2066=LINE('',#11882,#2628) ;
#2067=LINE('',#11885,#2629) ;
#2068=LINE('',#11891,#2630) ;
#2069=LINE('',#11897,#2631) ;
#2070=LINE('',#11901,#2632) ;
#2071=LINE('',#11959,#2633) ;
#2072=LINE('',#11963,#2634) ;
#2073=LINE('',#11969,#2635) ;
#2074=LINE('',#12320,#2636) ;
#2075=LINE('',#12389,#2637) ;
#2076=LINE('',#12442,#2638) ;
#2077=LINE('',#12446,#2639) ;
#2078=LINE('',#12504,#2640) ;
#2079=LINE('',#12508,#2641) ;
#2080=LINE('',#12514,#2642) ;
#2081=LINE('',#12520,#2643) ;
#2082=LINE('',#12523,#2644) ;
#2083=LINE('',#12528,#2645) ;
#2084=LINE('',#12531,#2646) ;
#2085=LINE('',#12534,#2647) ;
#2086=LINE('',#12536,#2648) ;
#2087=LINE('',#12537,#2649) ;
#2088=LINE('',#12540,#2650) ;
#2089=LINE('',#12541,#2651) ;
#2090=LINE('',#12544,#2652) ;
#2091=LINE('',#12545,#2653) ;
#2092=LINE('',#12547,#2654) ;
#2093=LINE('',#12551,#2655) ;
#2094=LINE('',#12553,#2656) ;
#2095=LINE('',#12554,#2657) ;
#2096=LINE('',#12557,#2658) ;
#2097=LINE('',#12558,#2659) ;
#2098=LINE('',#12561,#2660) ;
#2099=LINE('',#12562,#2661) ;
#2100=LINE('',#12564,#2662) ;
#2101=LINE('',#12568,#2663) ;
#2102=LINE('',#12570,#2664) ;
#2103=LINE('',#12571,#2665) ;
#2104=LINE('',#12574,#2666) ;
#2105=LINE('',#12575,#2667) ;
#2106=LINE('',#12578,#2668) ;
#2107=LINE('',#12579,#2669) ;
#2108=LINE('',#12582,#2670) ;
#2109=LINE('',#12583,#2671) ;
#2110=LINE('',#12586,#2672) ;
#2111=LINE('',#12587,#2673) ;
#2112=LINE('',#12590,#2674) ;
#2113=LINE('',#12591,#2675) ;
#2114=LINE('',#12594,#2676) ;
#2115=LINE('',#12595,#2677) ;
#2116=LINE('',#12598,#2678) ;
#2117=LINE('',#12599,#2679) ;
#2118=LINE('',#12602,#2680) ;
#2119=LINE('',#12603,#2681) ;
#2120=LINE('',#12611,#2682) ;
#2121=LINE('',#12622,#2683) ;
#2122=LINE('',#12628,#2684) ;
#2123=LINE('',#12629,#2685) ;
#2124=LINE('',#12632,#2686) ;
#2125=LINE('',#12633,#2687) ;
#2126=LINE('',#12636,#2688) ;
#2127=LINE('',#12637,#2689) ;
#2128=LINE('',#12639,#2690) ;
#2129=LINE('',#12648,#2691) ;
#2130=LINE('',#12653,#2692) ;
#2131=LINE('',#12656,#2693) ;
#2132=LINE('',#12657,#2694) ;
#2133=LINE('',#12660,#2695) ;
#2134=LINE('',#12661,#2696) ;
#2135=LINE('',#12664,#2697) ;
#2136=LINE('',#12665,#2698) ;
#2137=LINE('',#12676,#2699) ;
#2138=LINE('',#12687,#2700) ;
#2139=LINE('',#12698,#2701) ;
#2140=LINE('',#12709,#2702) ;
#2141=LINE('',#12720,#2703) ;
#2142=LINE('',#12728,#2704) ;
#2143=LINE('',#12739,#2705) ;
#2144=LINE('',#12750,#2706) ;
#2145=LINE('',#12761,#2707) ;
#2146=LINE('',#12772,#2708) ;
#2147=LINE('',#12778,#2709) ;
#2148=LINE('',#12779,#2710) ;
#2149=LINE('',#12782,#2711) ;
#2150=LINE('',#12783,#2712) ;
#2151=LINE('',#12785,#2713) ;
#2152=LINE('',#12794,#2714) ;
#2153=LINE('',#12799,#2715) ;
#2154=LINE('',#12810,#2716) ;
#2155=LINE('',#12821,#2717) ;
#2156=LINE('',#12824,#2718) ;
#2157=LINE('',#12825,#2719) ;
#2158=LINE('',#12836,#2720) ;
#2159=LINE('',#12847,#2721) ;
#2160=LINE('',#12858,#2722) ;
#2161=LINE('',#12869,#2723) ;
#2162=LINE('',#12880,#2724) ;
#2163=LINE('',#12891,#2725) ;
#2164=LINE('',#12902,#2726) ;
#2165=LINE('',#12913,#2727) ;
#2166=LINE('',#12924,#2728) ;
#2167=LINE('',#12935,#2729) ;
#2168=LINE('',#12946,#2730) ;
#2169=LINE('',#12957,#2731) ;
#2170=LINE('',#12968,#2732) ;
#2171=LINE('',#12979,#2733) ;
#2172=LINE('',#12987,#2734) ;
#2173=LINE('',#12998,#2735) ;
#2174=LINE('',#13009,#2736) ;
#2175=LINE('',#13020,#2737) ;
#2176=LINE('',#13031,#2738) ;
#2177=LINE('',#13042,#2739) ;
#2178=LINE('',#13053,#2740) ;
#2179=LINE('',#13064,#2741) ;
#2180=LINE('',#13075,#2742) ;
#2181=LINE('',#13086,#2743) ;
#2182=LINE('',#13097,#2744) ;
#2183=LINE('',#13108,#2745) ;
#2184=LINE('',#13119,#2746) ;
#2185=LINE('',#13130,#2747) ;
#2186=LINE('',#13141,#2748) ;
#2187=LINE('',#13147,#2749) ;
#2188=LINE('',#13148,#2750) ;
#2189=LINE('',#13161,#2751) ;
#2190=LINE('',#13163,#2752) ;
#2191=LINE('',#13164,#2753) ;
#2192=LINE('',#13167,#2754) ;
#2193=LINE('',#13168,#2755) ;
#2194=LINE('',#13171,#2756) ;
#2195=LINE('',#13172,#2757) ;
#2196=LINE('',#13175,#2758) ;
#2197=LINE('',#13176,#2759) ;
#2198=LINE('',#13179,#2760) ;
#2199=LINE('',#13180,#2761) ;
#2200=LINE('',#13183,#2762) ;
#2201=LINE('',#13184,#2763) ;
#2202=LINE('',#13187,#2764) ;
#2203=LINE('',#13188,#2765) ;
#2204=LINE('',#13191,#2766) ;
#2205=LINE('',#13192,#2767) ;
#2206=LINE('',#13195,#2768) ;
#2207=LINE('',#13196,#2769) ;
#2208=LINE('',#13204,#2770) ;
#2209=LINE('',#13215,#2771) ;
#2210=LINE('',#13221,#2772) ;
#2211=LINE('',#13222,#2773) ;
#2212=LINE('',#13225,#2774) ;
#2213=LINE('',#13226,#2775) ;
#2214=LINE('',#13229,#2776) ;
#2215=LINE('',#13230,#2777) ;
#2216=LINE('',#13232,#2778) ;
#2217=LINE('',#13238,#2779) ;
#2218=LINE('',#13248,#2780) ;
#2219=LINE('',#13254,#2781) ;
#2220=LINE('',#13330,#2782) ;
#2221=LINE('',#13334,#2783) ;
#2222=LINE('',#13339,#2784) ;
#2223=LINE('',#13373,#2785) ;
#2224=LINE('',#13377,#2786) ;
#2225=LINE('',#13382,#2787) ;
#2226=LINE('',#13416,#2788) ;
#2227=LINE('',#13420,#2789) ;
#2228=LINE('',#13425,#2790) ;
#2229=LINE('',#13459,#2791) ;
#2230=LINE('',#13475,#2792) ;
#2231=LINE('',#13479,#2793) ;
#2232=LINE('',#13483,#2794) ;
#2233=LINE('',#13487,#2795) ;
#2234=LINE('',#13492,#2796) ;
#2235=LINE('',#13496,#2797) ;
#2236=LINE('',#13501,#2798) ;
#2237=LINE('',#13505,#2799) ;
#2238=LINE('',#13510,#2800) ;
#2239=LINE('',#13514,#2801) ;
#2240=LINE('',#13519,#2802) ;
#2241=LINE('',#13523,#2803) ;
#2242=LINE('',#13544,#2804) ;
#2243=LINE('',#13552,#2805) ;
#2244=LINE('',#13560,#2806) ;
#2245=LINE('',#13568,#2807) ;
#2246=LINE('',#13576,#2808) ;
#2247=LINE('',#13580,#2809) ;
#2248=LINE('',#13588,#2810) ;
#2249=LINE('',#13592,#2811) ;
#2250=LINE('',#13594,#2812) ;
#2251=LINE('',#13598,#2813) ;
#2252=LINE('',#13601,#2814) ;
#2585=VECTOR('',#9165,10.) ;
#2586=VECTOR('',#9166,10.) ;
#2587=VECTOR('',#9167,10.) ;
#2588=VECTOR('',#9168,10.) ;
#2589=VECTOR('',#9169,10.) ;
#2590=VECTOR('',#9170,10.) ;
#2591=VECTOR('',#9171,10.) ;
#2592=VECTOR('',#9172,10.) ;
#2593=VECTOR('',#9173,10.) ;
#2594=VECTOR('',#9174,10.) ;
#2595=VECTOR('',#9175,10.) ;
#2596=VECTOR('',#9176,10.) ;
#2597=VECTOR('',#9177,10.) ;
#2598=VECTOR('',#9178,10.) ;
#2599=VECTOR('',#9179,10.) ;
#2600=VECTOR('',#9180,10.) ;
#2601=VECTOR('',#9181,10.) ;
#2602=VECTOR('',#9182,10.) ;
#2603=VECTOR('',#9183,10.) ;
#2604=VECTOR('',#9184,10.) ;
#2605=VECTOR('',#9185,10.) ;
#2606=VECTOR('',#9186,10.) ;
#2607=VECTOR('',#9187,10.) ;
#2608=VECTOR('',#9188,10.) ;
#2609=VECTOR('',#9189,10.) ;
#2610=VECTOR('',#9190,10.) ;
#2611=VECTOR('',#9191,10.) ;
#2612=VECTOR('',#9196,10.) ;
#2613=VECTOR('',#9197,10.) ;
#2614=VECTOR('',#9200,10.) ;
#2615=VECTOR('',#9201,10.) ;
#2616=VECTOR('',#9206,10.) ;
#2617=VECTOR('',#9207,10.) ;
#2618=VECTOR('',#9208,10.) ;
#2619=VECTOR('',#9209,10.) ;
#2620=VECTOR('',#9212,10.) ;
#2621=VECTOR('',#9213,10.) ;
#2622=VECTOR('',#9214,10.) ;
#2623=VECTOR('',#9215,10.) ;
#2624=VECTOR('',#9220,10.) ;
#2625=VECTOR('',#9221,10.) ;
#2626=VECTOR('',#9224,10.) ;
#2627=VECTOR('',#9225,10.) ;
#2628=VECTOR('',#9226,10.) ;
#2629=VECTOR('',#9231,10.) ;
#2630=VECTOR('',#9238,15.5) ;
#2631=VECTOR('',#9243,10.) ;
#2632=VECTOR('',#9246,10.) ;
#2633=VECTOR('',#9251,10.) ;
#2634=VECTOR('',#9254,10.) ;
#2635=VECTOR('',#9259,10.) ;
#2636=VECTOR('',#9268,10.) ;
#2637=VECTOR('',#9273,10.) ;
#2638=VECTOR('',#9278,10.) ;
#2639=VECTOR('',#9281,10.) ;
#2640=VECTOR('',#9286,10.) ;
#2641=VECTOR('',#9289,10.) ;
#2642=VECTOR('',#9294,10.) ;
#2643=VECTOR('',#9299,10.) ;
#2644=VECTOR('',#9302,10.) ;
#2645=VECTOR('',#9305,10.) ;
#2646=VECTOR('',#9308,10.) ;
#2647=VECTOR('',#9311,10.) ;
#2648=VECTOR('',#9312,10.) ;
#2649=VECTOR('',#9313,10.) ;
#2650=VECTOR('',#9316,10.) ;
#2651=VECTOR('',#9317,10.) ;
#2652=VECTOR('',#9320,10.) ;
#2653=VECTOR('',#9321,10.) ;
#2654=VECTOR('',#9324,10.) ;
#2655=VECTOR('',#9329,10.) ;
#2656=VECTOR('',#9330,10.) ;
#2657=VECTOR('',#9331,10.) ;
#2658=VECTOR('',#9334,10.) ;
#2659=VECTOR('',#9335,10.) ;
#2660=VECTOR('',#9338,10.) ;
#2661=VECTOR('',#9339,10.) ;
#2662=VECTOR('',#9342,10.) ;
#2663=VECTOR('',#9347,10.) ;
#2664=VECTOR('',#9348,10.) ;
#2665=VECTOR('',#9349,10.) ;
#2666=VECTOR('',#9352,10.) ;
#2667=VECTOR('',#9353,10.) ;
#2668=VECTOR('',#9356,10.) ;
#2669=VECTOR('',#9357,10.) ;
#2670=VECTOR('',#9360,10.) ;
#2671=VECTOR('',#9361,10.) ;
#2672=VECTOR('',#9364,10.) ;
#2673=VECTOR('',#9365,10.) ;
#2674=VECTOR('',#9368,10.) ;
#2675=VECTOR('',#9369,10.) ;
#2676=VECTOR('',#9372,10.) ;
#2677=VECTOR('',#9373,10.) ;
#2678=VECTOR('',#9376,10.) ;
#2679=VECTOR('',#9377,10.) ;
#2680=VECTOR('',#9380,10.) ;
#2681=VECTOR('',#9381,10.) ;
#2682=VECTOR('',#9382,10.) ;
#2683=VECTOR('',#9383,10.) ;
#2684=VECTOR('',#9386,10.) ;
#2685=VECTOR('',#9387,10.) ;
#2686=VECTOR('',#9390,10.) ;
#2687=VECTOR('',#9391,10.) ;
#2688=VECTOR('',#9394,10.) ;
#2689=VECTOR('',#9395,10.) ;
#2690=VECTOR('',#9398,10.) ;
#2691=VECTOR('',#9401,10.) ;
#2692=VECTOR('',#9402,10.) ;
#2693=VECTOR('',#9405,10.) ;
#2694=VECTOR('',#9406,10.) ;
#2695=VECTOR('',#9409,10.) ;
#2696=VECTOR('',#9410,10.) ;
#2697=VECTOR('',#9413,10.) ;
#2698=VECTOR('',#9414,10.) ;
#2699=VECTOR('',#9415,10.) ;
#2700=VECTOR('',#9416,10.) ;
#2701=VECTOR('',#9417,10.) ;
#2702=VECTOR('',#9418,10.) ;
#2703=VECTOR('',#9419,10.) ;
#2704=VECTOR('',#9420,10.) ;
#2705=VECTOR('',#9421,10.) ;
#2706=VECTOR('',#9422,10.) ;
#2707=VECTOR('',#9423,10.) ;
#2708=VECTOR('',#9424,10.) ;
#2709=VECTOR('',#9427,10.) ;
#2710=VECTOR('',#9428,10.) ;
#2711=VECTOR('',#9431,10.) ;
#2712=VECTOR('',#9432,10.) ;
#2713=VECTOR('',#9435,10.) ;
#2714=VECTOR('',#9438,10.) ;
#2715=VECTOR('',#9439,10.) ;
#2716=VECTOR('',#9440,10.) ;
#2717=VECTOR('',#9441,10.) ;
#2718=VECTOR('',#9444,10.) ;
#2719=VECTOR('',#9445,10.) ;
#2720=VECTOR('',#9446,10.) ;
#2721=VECTOR('',#9447,10.) ;
#2722=VECTOR('',#9448,10.) ;
#2723=VECTOR('',#9449,10.) ;
#2724=VECTOR('',#9450,10.) ;
#2725=VECTOR('',#9451,10.) ;
#2726=VECTOR('',#9452,10.) ;
#2727=VECTOR('',#9453,10.) ;
#2728=VECTOR('',#9454,10.) ;
#2729=VECTOR('',#9455,10.) ;
#2730=VECTOR('',#9456,10.) ;
#2731=VECTOR('',#9457,10.) ;
#2732=VECTOR('',#9458,10.) ;
#2733=VECTOR('',#9459,10.) ;
#2734=VECTOR('',#9460,10.) ;
#2735=VECTOR('',#9461,10.) ;
#2736=VECTOR('',#9462,10.) ;
#2737=VECTOR('',#9463,10.) ;
#2738=VECTOR('',#9464,10.) ;
#2739=VECTOR('',#9465,10.) ;
#2740=VECTOR('',#9466,10.) ;
#2741=VECTOR('',#9467,10.) ;
#2742=VECTOR('',#9468,10.) ;
#2743=VECTOR('',#9469,10.) ;
#2744=VECTOR('',#9470,10.) ;
#2745=VECTOR('',#9471,10.) ;
#2746=VECTOR('',#9472,10.) ;
#2747=VECTOR('',#9473,10.) ;
#2748=VECTOR('',#9474,10.) ;
#2749=VECTOR('',#9477,10.) ;
#2750=VECTOR('',#9478,10.) ;
#2751=VECTOR('',#9483,10.) ;
#2752=VECTOR('',#9484,10.) ;
#2753=VECTOR('',#9485,10.) ;
#2754=VECTOR('',#9488,10.) ;
#2755=VECTOR('',#9489,10.) ;
#2756=VECTOR('',#9492,10.) ;
#2757=VECTOR('',#9493,10.) ;
#2758=VECTOR('',#9496,10.) ;
#2759=VECTOR('',#9497,10.) ;
#2760=VECTOR('',#9500,10.) ;
#2761=VECTOR('',#9501,10.) ;
#2762=VECTOR('',#9504,10.) ;
#2763=VECTOR('',#9505,10.) ;
#2764=VECTOR('',#9508,10.) ;
#2765=VECTOR('',#9509,10.) ;
#2766=VECTOR('',#9512,10.) ;
#2767=VECTOR('',#9513,10.) ;
#2768=VECTOR('',#9516,10.) ;
#2769=VECTOR('',#9517,10.) ;
#2770=VECTOR('',#9518,10.) ;
#2771=VECTOR('',#9519,10.) ;
#2772=VECTOR('',#9522,10.) ;
#2773=VECTOR('',#9523,10.) ;
#2774=VECTOR('',#9526,10.) ;
#2775=VECTOR('',#9527,10.) ;
#2776=VECTOR('',#9530,10.) ;
#2777=VECTOR('',#9531,10.) ;
#2778=VECTOR('',#9534,10.) ;
#2779=VECTOR('',#9541,15.1) ;
#2780=VECTOR('',#9554,10.) ;
#2781=VECTOR('',#9559,10.) ;
#2782=VECTOR('',#9582,4.) ;
#2783=VECTOR('',#9587,10.) ;
#2784=VECTOR('',#9592,10.) ;
#2785=VECTOR('',#9597,4.) ;
#2786=VECTOR('',#9602,10.) ;
#2787=VECTOR('',#9607,10.) ;
#2788=VECTOR('',#9612,4.) ;
#2789=VECTOR('',#9617,10.) ;
#2790=VECTOR('',#9622,10.) ;
#2791=VECTOR('',#9627,4.) ;
#2792=VECTOR('',#9648,2.25) ;
#2793=VECTOR('',#9653,2.25) ;
#2794=VECTOR('',#9658,2.25) ;
#2795=VECTOR('',#9663,2.25) ;
#2796=VECTOR('',#9668,10.) ;
#2797=VECTOR('',#9671,10.) ;
#2798=VECTOR('',#9676,10.) ;
#2799=VECTOR('',#9679,10.) ;
#2800=VECTOR('',#9684,10.) ;
#2801=VECTOR('',#9687,10.) ;
#2802=VECTOR('',#9692,10.) ;
#2803=VECTOR('',#9695,10.) ;
#2804=VECTOR('',#9732,15.5) ;
#2805=VECTOR('',#9741,12.6) ;
#2806=VECTOR('',#9752,12.) ;
#2807=VECTOR('',#9761,12.6) ;
#2808=VECTOR('',#9772,12.) ;
#2809=VECTOR('',#9777,12.) ;
#2810=VECTOR('',#9788,25.25) ;
#2811=VECTOR('',#9793,25.5) ;
#2812=VECTOR('',#9796,25.25) ;
#2813=VECTOR('',#9801,15.25) ;
#2814=VECTOR('',#9806,12.) ;
#3164=CIRCLE('',#8350,15.5) ;
#3165=CIRCLE('',#8353,15.5) ;
#3166=CIRCLE('',#8356,15.5) ;
#3167=CIRCLE('',#8359,15.5) ;
#3168=CIRCLE('',#8360,15.5) ;
#3169=CIRCLE('',#8361,15.5) ;
#3170=CIRCLE('',#8362,15.5) ;
#3171=CIRCLE('',#8365,15.5) ;
#3172=CIRCLE('',#8366,15.5) ;
#3173=CIRCLE('',#8371,15.5) ;
#3174=CIRCLE('',#8372,15.5) ;
#3175=CIRCLE('',#8373,15.5) ;
#3176=CIRCLE('',#8374,15.5) ;
#3177=CIRCLE('',#8375,15.5) ;
#3178=CIRCLE('',#8376,15.5) ;
#3179=CIRCLE('',#8379,15.5) ;
#3180=CIRCLE('',#8380,15.5) ;
#3181=CIRCLE('',#8383,15.5) ;
#3182=CIRCLE('',#8384,15.5) ;
#3183=CIRCLE('',#8385,15.5) ;
#3184=CIRCLE('',#8386,15.5) ;
#3185=CIRCLE('',#8436,15.1) ;
#3186=CIRCLE('',#8437,15.1) ;
#3187=CIRCLE('',#8439,15.5) ;
#3188=CIRCLE('',#8443,4.) ;
#3189=CIRCLE('',#8444,4.) ;
#3190=CIRCLE('',#8445,4.3) ;
#3191=CIRCLE('',#8447,15.9) ;
#3192=CIRCLE('',#8448,15.9) ;
#3193=CIRCLE('',#8449,15.9) ;
#3194=CIRCLE('',#8450,15.9) ;
#3195=CIRCLE('',#8451,0.4) ;
#3196=CIRCLE('',#8452,15.5) ;
#3197=CIRCLE('',#8453,15.5) ;
#3198=CIRCLE('',#8454,15.9) ;
#3199=CIRCLE('',#8456,4.) ;
#3200=CIRCLE('',#8458,4.) ;
#3201=CIRCLE('',#8459,4.) ;
#3202=CIRCLE('',#8460,4.3) ;
#3203=CIRCLE('',#8462,4.) ;
#3204=CIRCLE('',#8464,4.) ;
#3205=CIRCLE('',#8465,4.) ;
#3206=CIRCLE('',#8466,4.3) ;
#3207=CIRCLE('',#8468,4.) ;
#3208=CIRCLE('',#8470,4.) ;
#3209=CIRCLE('',#8471,4.) ;
#3210=CIRCLE('',#8472,4.3) ;
#3211=CIRCLE('',#8474,4.) ;
#3212=CIRCLE('',#8476,2.25) ;
#3213=CIRCLE('',#8478,2.25) ;
#3214=CIRCLE('',#8480,2.25) ;
#3215=CIRCLE('',#8482,2.25) ;
#3216=CIRCLE('',#8484,2.25) ;
#3217=CIRCLE('',#8486,2.25) ;
#3218=CIRCLE('',#8488,2.25) ;
#3219=CIRCLE('',#8490,2.25) ;
#3220=CIRCLE('',#8492,1.65) ;
#3221=CIRCLE('',#8493,1.65) ;
#3222=CIRCLE('',#8495,1.65) ;
#3223=CIRCLE('',#8496,1.65) ;
#3224=CIRCLE('',#8498,1.65) ;
#3225=CIRCLE('',#8499,1.65) ;
#3226=CIRCLE('',#8501,1.65) ;
#3227=CIRCLE('',#8502,1.65) ;
#3228=CIRCLE('',#8504,12.) ;
#3229=CIRCLE('',#8505,8.6) ;
#3230=CIRCLE('',#8506,8.6) ;
#3231=CIRCLE('',#8507,8.6) ;
#3232=CIRCLE('',#8508,8.6) ;
#3233=CIRCLE('',#8510,8.6) ;
#3234=CIRCLE('',#8512,8.6) ;
#3235=CIRCLE('',#8514,8.6) ;
#3236=CIRCLE('',#8516,8.6) ;
#3237=CIRCLE('',#8518,25.) ;
#3238=CIRCLE('',#8521,12.6) ;
#3239=CIRCLE('',#8522,12.) ;
#3240=CIRCLE('',#8524,12.6) ;
#3241=CIRCLE('',#8526,12.) ;
#3242=CIRCLE('',#8528,12.) ;
#3243=CIRCLE('',#8530,12.6) ;
#3244=CIRCLE('',#8531,12.) ;
#3245=CIRCLE('',#8533,12.6) ;
#3246=CIRCLE('',#8535,12.) ;
#3247=CIRCLE('',#8537,12.) ;
#3248=CIRCLE('',#8540,12.) ;
#3249=CIRCLE('',#8542,25.) ;
#3250=CIRCLE('',#8544,25.5) ;
#3251=CIRCLE('',#8546,25.5) ;
#3252=CIRCLE('',#8549,15.) ;
#3456=VERTEX_POINT('',#11230) ;
#3457=VERTEX_POINT('',#11231) ;
#3458=VERTEX_POINT('',#11242) ;
#3459=VERTEX_POINT('',#11244) ;
#3460=VERTEX_POINT('',#11255) ;
#3461=VERTEX_POINT('',#11266) ;
#3462=VERTEX_POINT('',#11277) ;
#3463=VERTEX_POINT('',#11288) ;
#3464=VERTEX_POINT('',#11299) ;
#3465=VERTEX_POINT('',#11310) ;
#3466=VERTEX_POINT('',#11321) ;
#3467=VERTEX_POINT('',#11322) ;
#3468=VERTEX_POINT('',#11333) ;
#3469=VERTEX_POINT('',#11335) ;
#3470=VERTEX_POINT('',#11346) ;
#3471=VERTEX_POINT('',#11354) ;
#3472=VERTEX_POINT('',#11365) ;
#3473=VERTEX_POINT('',#11373) ;
#3474=VERTEX_POINT('',#11384) ;
#3475=VERTEX_POINT('',#11392) ;
#3476=VERTEX_POINT('',#11403) ;
#3477=VERTEX_POINT('',#11411) ;
#3478=VERTEX_POINT('',#11422) ;
#3479=VERTEX_POINT('',#11433) ;
#3480=VERTEX_POINT('',#11444) ;
#3481=VERTEX_POINT('',#11451) ;
#3482=VERTEX_POINT('',#11462) ;
#3483=VERTEX_POINT('',#11471) ;
#3484=VERTEX_POINT('',#11482) ;
#3485=VERTEX_POINT('',#11493) ;
#3486=VERTEX_POINT('',#11504) ;
#3487=VERTEX_POINT('',#11512) ;
#3488=VERTEX_POINT('',#11523) ;
#3489=VERTEX_POINT('',#11531) ;
#3490=VERTEX_POINT('',#11542) ;
#3491=VERTEX_POINT('',#11550) ;
#3492=VERTEX_POINT('',#11561) ;
#3493=VERTEX_POINT('',#11569) ;
#3494=VERTEX_POINT('',#11596) ;
#3495=VERTEX_POINT('',#11604) ;
#3496=VERTEX_POINT('',#11615) ;
#3497=VERTEX_POINT('',#11623) ;
#3498=VERTEX_POINT('',#11634) ;
#3499=VERTEX_POINT('',#11642) ;
#3500=VERTEX_POINT('',#11653) ;
#3501=VERTEX_POINT('',#11667) ;
#3502=VERTEX_POINT('',#11678) ;
#3503=VERTEX_POINT('',#11686) ;
#3504=VERTEX_POINT('',#11697) ;
#3505=VERTEX_POINT('',#11705) ;
#3506=VERTEX_POINT('',#11716) ;
#3507=VERTEX_POINT('',#11727) ;
#3508=VERTEX_POINT('',#11738) ;
#3509=VERTEX_POINT('',#11752) ;
#3510=VERTEX_POINT('',#11758) ;
#3511=VERTEX_POINT('',#11760) ;
#3512=VERTEX_POINT('',#11786) ;
#3513=VERTEX_POINT('',#11787) ;
#3514=VERTEX_POINT('',#11795) ;
#3515=VERTEX_POINT('',#11797) ;
#3516=VERTEX_POINT('',#11803) ;
#3517=VERTEX_POINT('',#11805) ;
#3518=VERTEX_POINT('',#11814) ;
#3519=VERTEX_POINT('',#11822) ;
#3520=VERTEX_POINT('',#11833) ;
#3521=VERTEX_POINT('',#11841) ;
#3522=VERTEX_POINT('',#11847) ;
#3523=VERTEX_POINT('',#11849) ;
#3524=VERTEX_POINT('',#11858) ;
#3525=VERTEX_POINT('',#11866) ;
#3526=VERTEX_POINT('',#11872) ;
#3527=VERTEX_POINT('',#11874) ;
#3528=VERTEX_POINT('',#11878) ;
#3529=VERTEX_POINT('',#11880) ;
#3530=VERTEX_POINT('',#11888) ;
#3531=VERTEX_POINT('',#11890) ;
#3532=VERTEX_POINT('',#11893) ;
#3533=VERTEX_POINT('',#11894) ;
#3534=VERTEX_POINT('',#11896) ;
#3535=VERTEX_POINT('',#11898) ;
#3536=VERTEX_POINT('',#11900) ;
#3537=VERTEX_POINT('',#11902) ;
#3538=VERTEX_POINT('',#11904) ;
#3539=VERTEX_POINT('',#11930) ;
#3540=VERTEX_POINT('',#11956) ;
#3541=VERTEX_POINT('',#11958) ;
#3542=VERTEX_POINT('',#11960) ;
#3543=VERTEX_POINT('',#11962) ;
#3544=VERTEX_POINT('',#11964) ;
#3545=VERTEX_POINT('',#11966) ;
#3546=VERTEX_POINT('',#11968) ;
#3547=VERTEX_POINT('',#11971) ;
#3548=VERTEX_POINT('',#11972) ;
#3549=VERTEX_POINT('',#11980) ;
#3550=VERTEX_POINT('',#11988) ;
#3551=VERTEX_POINT('',#11990) ;
#3552=VERTEX_POINT('',#11998) ;
#3553=VERTEX_POINT('',#12006) ;
#3554=VERTEX_POINT('',#12014) ;
#3555=VERTEX_POINT('',#12022) ;
#3556=VERTEX_POINT('',#12030) ;
#3557=VERTEX_POINT('',#12038) ;
#3558=VERTEX_POINT('',#12046) ;
#3559=VERTEX_POINT('',#12057) ;
#3560=VERTEX_POINT('',#12077) ;
#3561=VERTEX_POINT('',#12091) ;
#3562=VERTEX_POINT('',#12099) ;
#3563=VERTEX_POINT('',#12107) ;
#3564=VERTEX_POINT('',#12115) ;
#3565=VERTEX_POINT('',#12123) ;
#3566=VERTEX_POINT('',#12131) ;
#3567=VERTEX_POINT('',#12139) ;
#3568=VERTEX_POINT('',#12147) ;
#3569=VERTEX_POINT('',#12155) ;
#3570=VERTEX_POINT('',#12157) ;
#3571=VERTEX_POINT('',#12168) ;
#3572=VERTEX_POINT('',#12179) ;
#3573=VERTEX_POINT('',#12193) ;
#3574=VERTEX_POINT('',#12204) ;
#3575=VERTEX_POINT('',#12215) ;
#3576=VERTEX_POINT('',#12232) ;
#3577=VERTEX_POINT('',#12252) ;
#3578=VERTEX_POINT('',#12260) ;
#3579=VERTEX_POINT('',#12268) ;
#3580=VERTEX_POINT('',#12276) ;
#3581=VERTEX_POINT('',#12284) ;
#3582=VERTEX_POINT('',#12299) ;
#3583=VERTEX_POINT('',#12300) ;
#3584=VERTEX_POINT('',#12317) ;
#3585=VERTEX_POINT('',#12319) ;
#3586=VERTEX_POINT('',#12321) ;
#3587=VERTEX_POINT('',#12323) ;
#3588=VERTEX_POINT('',#12337) ;
#3589=VERTEX_POINT('',#12345) ;
#3590=VERTEX_POINT('',#12356) ;
#3591=VERTEX_POINT('',#12364) ;
#3592=VERTEX_POINT('',#12372) ;
#3593=VERTEX_POINT('',#12386) ;
#3594=VERTEX_POINT('',#12388) ;
#3595=VERTEX_POINT('',#12390) ;
#3596=VERTEX_POINT('',#12392) ;
#3597=VERTEX_POINT('',#12409) ;
#3598=VERTEX_POINT('',#12417) ;
#3599=VERTEX_POINT('',#12438) ;
#3600=VERTEX_POINT('',#12439) ;
#3601=VERTEX_POINT('',#12441) ;
#3602=VERTEX_POINT('',#12443) ;
#3603=VERTEX_POINT('',#12445) ;
#3604=VERTEX_POINT('',#12447) ;
#3605=VERTEX_POINT('',#12449) ;
#3606=VERTEX_POINT('',#12475) ;
#3607=VERTEX_POINT('',#12501) ;
#3608=VERTEX_POINT('',#12503) ;
#3609=VERTEX_POINT('',#12505) ;
#3610=VERTEX_POINT('',#12507) ;
#3611=VERTEX_POINT('',#12509) ;
#3612=VERTEX_POINT('',#12511) ;
#3613=VERTEX_POINT('',#12513) ;
#3614=VERTEX_POINT('',#12516) ;
#3615=VERTEX_POINT('',#12517) ;
#3616=VERTEX_POINT('',#12519) ;
#3617=VERTEX_POINT('',#12521) ;
#3618=VERTEX_POINT('',#12524) ;
#3619=VERTEX_POINT('',#12525) ;
#3620=VERTEX_POINT('',#12527) ;
#3621=VERTEX_POINT('',#12529) ;
#3622=VERTEX_POINT('',#12533) ;
#3623=VERTEX_POINT('',#12535) ;
#3624=VERTEX_POINT('',#12539) ;
#3625=VERTEX_POINT('',#12543) ;
#3626=VERTEX_POINT('',#12550) ;
#3627=VERTEX_POINT('',#12552) ;
#3628=VERTEX_POINT('',#12556) ;
#3629=VERTEX_POINT('',#12560) ;
#3630=VERTEX_POINT('',#12567) ;
#3631=VERTEX_POINT('',#12569) ;
#3632=VERTEX_POINT('',#12573) ;
#3633=VERTEX_POINT('',#12577) ;
#3634=VERTEX_POINT('',#12581) ;
#3635=VERTEX_POINT('',#12585) ;
#3636=VERTEX_POINT('',#12589) ;
#3637=VERTEX_POINT('',#12593) ;
#3638=VERTEX_POINT('',#12597) ;
#3639=VERTEX_POINT('',#12601) ;
#3640=VERTEX_POINT('',#12610) ;
#3641=VERTEX_POINT('',#12621) ;
#3642=VERTEX_POINT('',#12627) ;
#3643=VERTEX_POINT('',#12631) ;
#3644=VERTEX_POINT('',#12635) ;
#3645=VERTEX_POINT('',#12647) ;
#3646=VERTEX_POINT('',#12649) ;
#3647=VERTEX_POINT('',#12655) ;
#3648=VERTEX_POINT('',#12659) ;
#3649=VERTEX_POINT('',#12663) ;
#3650=VERTEX_POINT('',#12672) ;
#3651=VERTEX_POINT('',#12683) ;
#3652=VERTEX_POINT('',#12694) ;
#3653=VERTEX_POINT('',#12705) ;
#3654=VERTEX_POINT('',#12716) ;
#3655=VERTEX_POINT('',#12727) ;
#3656=VERTEX_POINT('',#12738) ;
#3657=VERTEX_POINT('',#12749) ;
#3658=VERTEX_POINT('',#12760) ;
#3659=VERTEX_POINT('',#12771) ;
#3660=VERTEX_POINT('',#12777) ;
#3661=VERTEX_POINT('',#12781) ;
#3662=VERTEX_POINT('',#12793) ;
#3663=VERTEX_POINT('',#12795) ;
#3664=VERTEX_POINT('',#12806) ;
#3665=VERTEX_POINT('',#12817) ;
#3666=VERTEX_POINT('',#12823) ;
#3667=VERTEX_POINT('',#12832) ;
#3668=VERTEX_POINT('',#12843) ;
#3669=VERTEX_POINT('',#12854) ;
#3670=VERTEX_POINT('',#12865) ;
#3671=VERTEX_POINT('',#12876) ;
#3672=VERTEX_POINT('',#12887) ;
#3673=VERTEX_POINT('',#12898) ;
#3674=VERTEX_POINT('',#12909) ;
#3675=VERTEX_POINT('',#12920) ;
#3676=VERTEX_POINT('',#12931) ;
#3677=VERTEX_POINT('',#12942) ;
#3678=VERTEX_POINT('',#12953) ;
#3679=VERTEX_POINT('',#12964) ;
#3680=VERTEX_POINT('',#12975) ;
#3681=VERTEX_POINT('',#12986) ;
#3682=VERTEX_POINT('',#12997) ;
#3683=VERTEX_POINT('',#13008) ;
#3684=VERTEX_POINT('',#13019) ;
#3685=VERTEX_POINT('',#13030) ;
#3686=VERTEX_POINT('',#13041) ;
#3687=VERTEX_POINT('',#13052) ;
#3688=VERTEX_POINT('',#13063) ;
#3689=VERTEX_POINT('',#13074) ;
#3690=VERTEX_POINT('',#13085) ;
#3691=VERTEX_POINT('',#13096) ;
#3692=VERTEX_POINT('',#13107) ;
#3693=VERTEX_POINT('',#13118) ;
#3694=VERTEX_POINT('',#13129) ;
#3695=VERTEX_POINT('',#13140) ;
#3696=VERTEX_POINT('',#13146) ;
#3697=VERTEX_POINT('',#13160) ;
#3698=VERTEX_POINT('',#13162) ;
#3699=VERTEX_POINT('',#13166) ;
#3700=VERTEX_POINT('',#13170) ;
#3701=VERTEX_POINT('',#13174) ;
#3702=VERTEX_POINT('',#13178) ;
#3703=VERTEX_POINT('',#13182) ;
#3704=VERTEX_POINT('',#13186) ;
#3705=VERTEX_POINT('',#13190) ;
#3706=VERTEX_POINT('',#13194) ;
#3707=VERTEX_POINT('',#13203) ;
#3708=VERTEX_POINT('',#13214) ;
#3709=VERTEX_POINT('',#13220) ;
#3710=VERTEX_POINT('',#13224) ;
#3711=VERTEX_POINT('',#13228) ;
#3712=VERTEX_POINT('',#13235) ;
#3713=VERTEX_POINT('',#13237) ;
#3714=VERTEX_POINT('',#13241) ;
#3715=VERTEX_POINT('',#13246) ;
#3716=VERTEX_POINT('',#13247) ;
#3717=VERTEX_POINT('',#13249) ;
#3718=VERTEX_POINT('',#13251) ;
#3719=VERTEX_POINT('',#13253) ;
#3720=VERTEX_POINT('',#13293) ;
#3721=VERTEX_POINT('',#13295) ;
#3722=VERTEX_POINT('',#13302) ;
#3723=VERTEX_POINT('',#13304) ;
#3724=VERTEX_POINT('',#13311) ;
#3725=VERTEX_POINT('',#13313) ;
#3726=VERTEX_POINT('',#13320) ;
#3727=VERTEX_POINT('',#13322) ;
#3728=VERTEX_POINT('',#13324) ;
#3729=VERTEX_POINT('',#13329) ;
#3730=VERTEX_POINT('',#13333) ;
#3731=VERTEX_POINT('',#13335) ;
#3732=VERTEX_POINT('',#13337) ;
#3733=VERTEX_POINT('',#13372) ;
#3734=VERTEX_POINT('',#13376) ;
#3735=VERTEX_POINT('',#13378) ;
#3736=VERTEX_POINT('',#13380) ;
#3737=VERTEX_POINT('',#13415) ;
#3738=VERTEX_POINT('',#13419) ;
#3739=VERTEX_POINT('',#13421) ;
#3740=VERTEX_POINT('',#13423) ;
#3741=VERTEX_POINT('',#13458) ;
#3742=VERTEX_POINT('',#13462) ;
#3743=VERTEX_POINT('',#13465) ;
#3744=VERTEX_POINT('',#13468) ;
#3745=VERTEX_POINT('',#13471) ;
#3746=VERTEX_POINT('',#13474) ;
#3747=VERTEX_POINT('',#13478) ;
#3748=VERTEX_POINT('',#13482) ;
#3749=VERTEX_POINT('',#13486) ;
#3750=VERTEX_POINT('',#13490) ;
#3751=VERTEX_POINT('',#13491) ;
#3752=VERTEX_POINT('',#13493) ;
#3753=VERTEX_POINT('',#13495) ;
#3754=VERTEX_POINT('',#13499) ;
#3755=VERTEX_POINT('',#13500) ;
#3756=VERTEX_POINT('',#13502) ;
#3757=VERTEX_POINT('',#13504) ;
#3758=VERTEX_POINT('',#13508) ;
#3759=VERTEX_POINT('',#13509) ;
#3760=VERTEX_POINT('',#13511) ;
#3761=VERTEX_POINT('',#13513) ;
#3762=VERTEX_POINT('',#13517) ;
#3763=VERTEX_POINT('',#13518) ;
#3764=VERTEX_POINT('',#13520) ;
#3765=VERTEX_POINT('',#13522) ;
#3766=VERTEX_POINT('',#13526) ;
#3767=VERTEX_POINT('',#13541) ;
#3768=VERTEX_POINT('',#13546) ;
#3769=VERTEX_POINT('',#13548) ;
#3770=VERTEX_POINT('',#13551) ;
#3771=VERTEX_POINT('',#13555) ;
#3772=VERTEX_POINT('',#13558) ;
#3773=VERTEX_POINT('',#13562) ;
#3774=VERTEX_POINT('',#13564) ;
#3775=VERTEX_POINT('',#13567) ;
#3776=VERTEX_POINT('',#13571) ;
#3777=VERTEX_POINT('',#13574) ;
#3778=VERTEX_POINT('',#13579) ;
#3779=VERTEX_POINT('',#13583) ;
#3780=VERTEX_POINT('',#13586) ;
#3781=VERTEX_POINT('',#13590) ;
#3782=VERTEX_POINT('',#13596) ;
#4260=EDGE_CURVE('',#3456,#3457,#459,.T.) ;
#4261=EDGE_CURVE('',#3456,#3458,#2023,.T.) ;
#4262=EDGE_CURVE('',#3458,#3459,#460,.T.) ;
#4263=EDGE_CURVE('',#3457,#3459,#2024,.T.) ;
#4264=EDGE_CURVE('',#3457,#3460,#461,.T.) ;
#4265=EDGE_CURVE('',#3459,#3461,#462,.T.) ;
#4266=EDGE_CURVE('',#3460,#3461,#2025,.T.) ;
#4267=EDGE_CURVE('',#3460,#3462,#463,.T.) ;
#4268=EDGE_CURVE('',#3461,#3463,#464,.T.) ;
#4269=EDGE_CURVE('',#3462,#3463,#2026,.T.) ;
#4270=EDGE_CURVE('',#3462,#3464,#465,.T.) ;
#4271=EDGE_CURVE('',#3463,#3465,#466,.T.) ;
#4272=EDGE_CURVE('',#3464,#3465,#2027,.T.) ;
#4273=EDGE_CURVE('',#3466,#3467,#467,.T.) ;
#4274=EDGE_CURVE('',#3466,#3468,#2028,.T.) ;
#4275=EDGE_CURVE('',#3468,#3469,#468,.T.) ;
#4276=EDGE_CURVE('',#3467,#3469,#2029,.T.) ;
#4277=EDGE_CURVE('',#3467,#3470,#469,.T.) ;
#4278=EDGE_CURVE('',#3469,#3471,#470,.T.) ;
#4279=EDGE_CURVE('',#3470,#3471,#2030,.T.) ;
#4280=EDGE_CURVE('',#3470,#3472,#471,.T.) ;
#4281=EDGE_CURVE('',#3471,#3473,#472,.T.) ;
#4282=EDGE_CURVE('',#3472,#3473,#2031,.T.) ;
#4283=EDGE_CURVE('',#3472,#3474,#473,.T.) ;
#4284=EDGE_CURVE('',#3473,#3475,#474,.T.) ;
#4285=EDGE_CURVE('',#3474,#3475,#2032,.T.) ;
#4286=EDGE_CURVE('',#3474,#3476,#475,.T.) ;
#4287=EDGE_CURVE('',#3475,#3477,#476,.T.) ;
#4288=EDGE_CURVE('',#3476,#3477,#2033,.T.) ;
#4289=EDGE_CURVE('',#3476,#3478,#477,.T.) ;
#4290=EDGE_CURVE('',#3477,#3479,#478,.T.) ;
#4291=EDGE_CURVE('',#3478,#3479,#2034,.T.) ;
#4292=EDGE_CURVE('',#3478,#3480,#479,.T.) ;
#4293=EDGE_CURVE('',#3479,#3481,#480,.T.) ;
#4294=EDGE_CURVE('',#3480,#3481,#2035,.T.) ;
#4295=EDGE_CURVE('',#3480,#3482,#481,.T.) ;
#4296=EDGE_CURVE('',#3481,#3483,#482,.T.) ;
#4297=EDGE_CURVE('',#3482,#3483,#2036,.T.) ;
#4298=EDGE_CURVE('',#3482,#3484,#483,.T.) ;
#4299=EDGE_CURVE('',#3483,#3485,#484,.T.) ;
#4300=EDGE_CURVE('',#3484,#3485,#2037,.T.) ;
#4301=EDGE_CURVE('',#3464,#3486,#485,.T.) ;
#4302=EDGE_CURVE('',#3465,#3487,#486,.T.) ;
#4303=EDGE_CURVE('',#3486,#3487,#2038,.T.) ;
#4304=EDGE_CURVE('',#3488,#3456,#487,.T.) ;
#4305=EDGE_CURVE('',#3488,#3489,#2039,.T.) ;
#4306=EDGE_CURVE('',#3489,#3458,#488,.T.) ;
#4307=EDGE_CURVE('',#3490,#3488,#489,.T.) ;
#4308=EDGE_CURVE('',#3490,#3491,#2040,.T.) ;
#4309=EDGE_CURVE('',#3491,#3489,#490,.T.) ;
#4310=EDGE_CURVE('',#3492,#3490,#491,.T.) ;
#4311=EDGE_CURVE('',#3492,#3493,#2041,.T.) ;
#4312=EDGE_CURVE('',#3493,#3491,#492,.T.) ;
#4313=EDGE_CURVE('',#3486,#3492,#493,.T.) ;
#4314=EDGE_CURVE('',#3487,#3493,#494,.T.) ;
#4315=EDGE_CURVE('',#3484,#3494,#495,.T.) ;
#4316=EDGE_CURVE('',#3485,#3495,#496,.T.) ;
#4317=EDGE_CURVE('',#3494,#3495,#2042,.T.) ;
#4318=EDGE_CURVE('',#3496,#3466,#497,.T.) ;
#4319=EDGE_CURVE('',#3496,#3497,#2043,.T.) ;
#4320=EDGE_CURVE('',#3497,#3468,#498,.T.) ;
#4321=EDGE_CURVE('',#3498,#3496,#499,.T.) ;
#4322=EDGE_CURVE('',#3498,#3499,#2044,.T.) ;
#4323=EDGE_CURVE('',#3499,#3497,#500,.T.) ;
#4324=EDGE_CURVE('',#3500,#3498,#501,.T.) ;
#4325=EDGE_CURVE('',#3500,#3501,#2045,.T.) ;
#4326=EDGE_CURVE('',#3501,#3499,#502,.T.) ;
#4327=EDGE_CURVE('',#3502,#3500,#503,.T.) ;
#4328=EDGE_CURVE('',#3502,#3503,#2046,.T.) ;
#4329=EDGE_CURVE('',#3503,#3501,#504,.T.) ;
#4330=EDGE_CURVE('',#3504,#3502,#505,.T.) ;
#4331=EDGE_CURVE('',#3504,#3505,#2047,.T.) ;
#4332=EDGE_CURVE('',#3505,#3503,#506,.T.) ;
#4333=EDGE_CURVE('',#3506,#3504,#507,.T.) ;
#4334=EDGE_CURVE('',#3506,#3507,#2048,.T.) ;
#4335=EDGE_CURVE('',#3507,#3505,#508,.T.) ;
#4336=EDGE_CURVE('',#3508,#3506,#509,.T.) ;
#4337=EDGE_CURVE('',#3508,#3509,#2049,.T.) ;
#4338=EDGE_CURVE('',#3509,#3507,#510,.T.) ;
#4339=EDGE_CURVE('',#3510,#3508,#319,.T.) ;
#4340=EDGE_CURVE('',#3510,#3511,#2050,.T.) ;
#4341=EDGE_CURVE('',#3511,#3509,#2051,.T.) ;
#4342=EDGE_CURVE('',#3494,#3510,#511,.T.) ;
#4343=EDGE_CURVE('',#3495,#3511,#512,.T.) ;
#4344=EDGE_CURVE('',#3512,#3513,#513,.T.) ;
#4345=EDGE_CURVE('',#3512,#3514,#2052,.T.) ;
#4346=EDGE_CURVE('',#3514,#3515,#514,.T.) ;
#4347=EDGE_CURVE('',#3513,#3515,#2053,.T.) ;
#4348=EDGE_CURVE('',#3513,#3516,#3164,.T.) ;
#4349=EDGE_CURVE('',#3515,#3517,#2054,.T.) ;
#4350=EDGE_CURVE('',#3516,#3517,#2055,.T.) ;
#4351=EDGE_CURVE('',#3516,#3518,#515,.T.) ;
#4352=EDGE_CURVE('',#3517,#3519,#516,.T.) ;
#4353=EDGE_CURVE('',#3518,#3519,#2056,.T.) ;
#4354=EDGE_CURVE('',#3518,#3520,#517,.T.) ;
#4355=EDGE_CURVE('',#3519,#3521,#518,.T.) ;
#4356=EDGE_CURVE('',#3520,#3521,#2057,.T.) ;
#4357=EDGE_CURVE('',#3520,#3522,#2058,.T.) ;
#4358=EDGE_CURVE('',#3521,#3523,#2059,.T.) ;
#4359=EDGE_CURVE('',#3522,#3523,#2060,.T.) ;
#4360=EDGE_CURVE('',#3524,#3512,#519,.T.) ;
#4361=EDGE_CURVE('',#3524,#3525,#2061,.T.) ;
#4362=EDGE_CURVE('',#3525,#3514,#520,.T.) ;
#4363=EDGE_CURVE('',#3526,#3524,#3165,.T.) ;
#4364=EDGE_CURVE('',#3526,#3527,#2062,.T.) ;
#4365=EDGE_CURVE('',#3527,#3525,#2063,.T.) ;
#4366=EDGE_CURVE('',#3528,#3526,#2064,.T.) ;
#4367=EDGE_CURVE('',#3528,#3529,#2065,.T.) ;
#4368=EDGE_CURVE('',#3529,#3527,#2066,.T.) ;
#4369=EDGE_CURVE('',#3522,#3528,#3166,.T.) ;
#4370=EDGE_CURVE('',#3523,#3529,#2067,.T.) ;
#4371=EDGE_CURVE('',#3530,#3530,#3167,.T.) ;
#4372=EDGE_CURVE('',#3530,#3531,#2068,.T.) ;
#4373=EDGE_CURVE('',#3531,#3531,#3168,.T.) ;
#4374=EDGE_CURVE('',#3532,#3533,#3169,.T.) ;
#4375=EDGE_CURVE('',#3533,#3534,#2069,.T.) ;
#4376=EDGE_CURVE('',#3534,#3535,#3170,.T.) ;
#4377=EDGE_CURVE('',#3535,#3536,#2070,.T.) ;
#4378=EDGE_CURVE('',#3536,#3537,#320,.T.) ;
#4379=EDGE_CURVE('',#3537,#3538,#521,.T.) ;
#4380=EDGE_CURVE('',#3538,#3539,#522,.T.) ;
#4381=EDGE_CURVE('',#3539,#3540,#321,.T.) ;
#4382=EDGE_CURVE('',#3540,#3541,#2071,.T.) ;
#4383=EDGE_CURVE('',#3541,#3542,#3171,.T.) ;
#4384=EDGE_CURVE('',#3542,#3543,#2072,.T.) ;
#4385=EDGE_CURVE('',#3543,#3544,#3172,.T.) ;
#4386=EDGE_CURVE('',#3544,#3545,#322,.T.) ;
#4387=EDGE_CURVE('',#3545,#3546,#2073,.T.) ;
#4388=EDGE_CURVE('',#3546,#3532,#323,.T.) ;
#4389=EDGE_CURVE('',#3547,#3548,#523,.T.) ;
#4390=EDGE_CURVE('',#3548,#3549,#524,.T.) ;
#4391=EDGE_CURVE('',#3549,#3550,#324,.T.) ;
#4392=EDGE_CURVE('',#3550,#3551,#525,.T.) ;
#4393=EDGE_CURVE('',#3551,#3552,#526,.T.) ;
#4394=EDGE_CURVE('',#3552,#3553,#527,.T.) ;
#4395=EDGE_CURVE('',#3553,#3554,#528,.T.) ;
#4396=EDGE_CURVE('',#3554,#3555,#529,.T.) ;
#4397=EDGE_CURVE('',#3555,#3556,#530,.T.) ;
#4398=EDGE_CURVE('',#3556,#3557,#531,.T.) ;
#4399=EDGE_CURVE('',#3557,#3558,#532,.T.) ;
#4400=EDGE_CURVE('',#3558,#3559,#533,.T.) ;
#4401=EDGE_CURVE('',#3559,#3560,#534,.T.) ;
#4402=EDGE_CURVE('',#3560,#3561,#535,.T.) ;
#4403=EDGE_CURVE('',#3561,#3562,#536,.T.) ;
#4404=EDGE_CURVE('',#3562,#3563,#537,.T.) ;
#4405=EDGE_CURVE('',#3563,#3564,#538,.T.) ;
#4406=EDGE_CURVE('',#3564,#3565,#539,.T.) ;
#4407=EDGE_CURVE('',#3565,#3566,#540,.T.) ;
#4408=EDGE_CURVE('',#3566,#3567,#541,.T.) ;
#4409=EDGE_CURVE('',#3567,#3568,#542,.T.) ;
#4410=EDGE_CURVE('',#3568,#3569,#325,.T.) ;
#4411=EDGE_CURVE('',#3569,#3570,#543,.T.) ;
#4412=EDGE_CURVE('',#3570,#3571,#544,.T.) ;
#4413=EDGE_CURVE('',#3571,#3572,#545,.T.) ;
#4414=EDGE_CURVE('',#3572,#3573,#546,.T.) ;
#4415=EDGE_CURVE('',#3573,#3574,#547,.T.) ;
#4416=EDGE_CURVE('',#3574,#3575,#548,.T.) ;
#4417=EDGE_CURVE('',#3575,#3576,#549,.T.) ;
#4418=EDGE_CURVE('',#3576,#3577,#550,.T.) ;
#4419=EDGE_CURVE('',#3577,#3578,#551,.T.) ;
#4420=EDGE_CURVE('',#3578,#3579,#552,.T.) ;
#4421=EDGE_CURVE('',#3579,#3580,#553,.T.) ;
#4422=EDGE_CURVE('',#3580,#3581,#554,.T.) ;
#4423=EDGE_CURVE('',#3581,#3547,#555,.T.) ;
#4424=EDGE_CURVE('',#3582,#3583,#556,.T.) ;
#4425=EDGE_CURVE('',#3583,#3584,#3173,.T.) ;
#4426=EDGE_CURVE('',#3584,#3585,#2074,.T.) ;
#4427=EDGE_CURVE('',#3585,#3586,#3174,.T.) ;
#4428=EDGE_CURVE('',#3586,#3587,#557,.T.) ;
#4429=EDGE_CURVE('',#3587,#3588,#558,.T.) ;
#4430=EDGE_CURVE('',#3588,#3589,#559,.T.) ;
#4431=EDGE_CURVE('',#3589,#3590,#560,.T.) ;
#4432=EDGE_CURVE('',#3590,#3591,#561,.T.) ;
#4433=EDGE_CURVE('',#3591,#3592,#562,.T.) ;
#4434=EDGE_CURVE('',#3592,#3593,#3175,.T.) ;
#4435=EDGE_CURVE('',#3593,#3594,#2075,.T.) ;
#4436=EDGE_CURVE('',#3594,#3595,#3176,.T.) ;
#4437=EDGE_CURVE('',#3595,#3596,#563,.T.) ;
#4438=EDGE_CURVE('',#3596,#3597,#564,.T.) ;
#4439=EDGE_CURVE('',#3597,#3598,#565,.T.) ;
#4440=EDGE_CURVE('',#3598,#3582,#566,.T.) ;
#4441=EDGE_CURVE('',#3599,#3600,#3177,.T.) ;
#4442=EDGE_CURVE('',#3600,#3601,#2076,.T.) ;
#4443=EDGE_CURVE('',#3601,#3602,#3178,.T.) ;
#4444=EDGE_CURVE('',#3602,#3603,#2077,.T.) ;
#4445=EDGE_CURVE('',#3603,#3604,#326,.T.) ;
#4446=EDGE_CURVE('',#3604,#3605,#567,.T.) ;
#4447=EDGE_CURVE('',#3605,#3606,#568,.T.) ;
#4448=EDGE_CURVE('',#3606,#3607,#327,.T.) ;
#4449=EDGE_CURVE('',#3607,#3608,#2078,.T.) ;
#4450=EDGE_CURVE('',#3608,#3609,#3179,.T.) ;
#4451=EDGE_CURVE('',#3609,#3610,#2079,.T.) ;
#4452=EDGE_CURVE('',#3610,#3611,#3180,.T.) ;
#4453=EDGE_CURVE('',#3611,#3612,#328,.T.) ;
#4454=EDGE_CURVE('',#3612,#3613,#2080,.T.) ;
#4455=EDGE_CURVE('',#3613,#3599,#329,.T.) ;
#4456=EDGE_CURVE('',#3614,#3615,#3181,.T.) ;
#4457=EDGE_CURVE('',#3615,#3616,#2081,.T.) ;
#4458=EDGE_CURVE('',#3616,#3617,#3182,.T.) ;
#4459=EDGE_CURVE('',#3617,#3614,#2082,.T.) ;
#4460=EDGE_CURVE('',#3618,#3619,#3183,.T.) ;
#4461=EDGE_CURVE('',#3619,#3620,#2083,.T.) ;
#4462=EDGE_CURVE('',#3620,#3621,#3184,.T.) ;
#4463=EDGE_CURVE('',#3621,#3618,#2084,.T.) ;
#4464=EDGE_CURVE('',#3620,#3622,#2085,.T.) ;
#4465=EDGE_CURVE('',#3622,#3623,#2086,.T.) ;
#4466=EDGE_CURVE('',#3621,#3623,#2087,.T.) ;
#4467=EDGE_CURVE('',#3623,#3624,#2088,.T.) ;
#4468=EDGE_CURVE('',#3618,#3624,#2089,.T.) ;
#4469=EDGE_CURVE('',#3624,#3625,#2090,.T.) ;
#4470=EDGE_CURVE('',#3619,#3625,#2091,.T.) ;
#4471=EDGE_CURVE('',#3625,#3622,#2092,.T.) ;
#4472=EDGE_CURVE('',#3616,#3626,#2093,.T.) ;
#4473=EDGE_CURVE('',#3626,#3627,#2094,.T.) ;
#4474=EDGE_CURVE('',#3617,#3627,#2095,.T.) ;
#4475=EDGE_CURVE('',#3627,#3628,#2096,.T.) ;
#4476=EDGE_CURVE('',#3614,#3628,#2097,.T.) ;
#4477=EDGE_CURVE('',#3628,#3629,#2098,.T.) ;
#4478=EDGE_CURVE('',#3615,#3629,#2099,.T.) ;
#4479=EDGE_CURVE('',#3629,#3626,#2100,.T.) ;
#4480=EDGE_CURVE('',#3607,#3630,#2101,.T.) ;
#4481=EDGE_CURVE('',#3630,#3631,#2102,.T.) ;
#4482=EDGE_CURVE('',#3608,#3631,#2103,.T.) ;
#4483=EDGE_CURVE('',#3631,#3632,#2104,.T.) ;
#4484=EDGE_CURVE('',#3609,#3632,#2105,.T.) ;
#4485=EDGE_CURVE('',#3632,#3633,#2106,.T.) ;
#4486=EDGE_CURVE('',#3610,#3633,#2107,.T.) ;
#4487=EDGE_CURVE('',#3633,#3634,#2108,.T.) ;
#4488=EDGE_CURVE('',#3611,#3634,#2109,.T.) ;
#4489=EDGE_CURVE('',#3634,#3635,#2110,.T.) ;
#4490=EDGE_CURVE('',#3612,#3635,#2111,.T.) ;
#4491=EDGE_CURVE('',#3635,#3636,#2112,.T.) ;
#4492=EDGE_CURVE('',#3613,#3636,#2113,.T.) ;
#4493=EDGE_CURVE('',#3636,#3637,#2114,.T.) ;
#4494=EDGE_CURVE('',#3599,#3637,#2115,.T.) ;
#4495=EDGE_CURVE('',#3637,#3638,#2116,.T.) ;
#4496=EDGE_CURVE('',#3600,#3638,#2117,.T.) ;
#4497=EDGE_CURVE('',#3606,#3639,#2118,.T.) ;
#4498=EDGE_CURVE('',#3639,#3630,#2119,.T.) ;
#4499=EDGE_CURVE('',#3605,#3640,#2120,.T.) ;
#4500=EDGE_CURVE('',#3640,#3639,#569,.T.) ;
#4501=EDGE_CURVE('',#3604,#3641,#2121,.T.) ;
#4502=EDGE_CURVE('',#3641,#3640,#570,.T.) ;
#4503=EDGE_CURVE('',#3603,#3642,#2122,.T.) ;
#4504=EDGE_CURVE('',#3642,#3641,#2123,.T.) ;
#4505=EDGE_CURVE('',#3602,#3643,#2124,.T.) ;
#4506=EDGE_CURVE('',#3643,#3642,#2125,.T.) ;
#4507=EDGE_CURVE('',#3601,#3644,#2126,.T.) ;
#4508=EDGE_CURVE('',#3644,#3643,#2127,.T.) ;
#4509=EDGE_CURVE('',#3638,#3644,#2128,.T.) ;
#4510=EDGE_CURVE('',#3591,#3645,#2129,.T.) ;
#4511=EDGE_CURVE('',#3645,#3646,#571,.T.) ;
#4512=EDGE_CURVE('',#3592,#3646,#2130,.T.) ;
#4513=EDGE_CURVE('',#3646,#3647,#2131,.T.) ;
#4514=EDGE_CURVE('',#3593,#3647,#2132,.T.) ;
#4515=EDGE_CURVE('',#3647,#3648,#2133,.T.) ;
#4516=EDGE_CURVE('',#3594,#3648,#2134,.T.) ;
#4517=EDGE_CURVE('',#3648,#3649,#2135,.T.) ;
#4518=EDGE_CURVE('',#3595,#3649,#2136,.T.) ;
#4519=EDGE_CURVE('',#3649,#3650,#572,.T.) ;
#4520=EDGE_CURVE('',#3596,#3650,#2137,.T.) ;
#4521=EDGE_CURVE('',#3650,#3651,#573,.T.) ;
#4522=EDGE_CURVE('',#3597,#3651,#2138,.T.) ;
#4523=EDGE_CURVE('',#3651,#3652,#574,.T.) ;
#4524=EDGE_CURVE('',#3598,#3652,#2139,.T.) ;
#4525=EDGE_CURVE('',#3652,#3653,#575,.T.) ;
#4526=EDGE_CURVE('',#3582,#3653,#2140,.T.) ;
#4527=EDGE_CURVE('',#3653,#3654,#576,.T.) ;
#4528=EDGE_CURVE('',#3583,#3654,#2141,.T.) ;
#4529=EDGE_CURVE('',#3590,#3655,#2142,.T.) ;
#4530=EDGE_CURVE('',#3655,#3645,#577,.T.) ;
#4531=EDGE_CURVE('',#3589,#3656,#2143,.T.) ;
#4532=EDGE_CURVE('',#3656,#3655,#578,.T.) ;
#4533=EDGE_CURVE('',#3588,#3657,#2144,.T.) ;
#4534=EDGE_CURVE('',#3657,#3656,#579,.T.) ;
#4535=EDGE_CURVE('',#3587,#3658,#2145,.T.) ;
#4536=EDGE_CURVE('',#3658,#3657,#580,.T.) ;
#4537=EDGE_CURVE('',#3586,#3659,#2146,.T.) ;
#4538=EDGE_CURVE('',#3659,#3658,#581,.T.) ;
#4539=EDGE_CURVE('',#3585,#3660,#2147,.T.) ;
#4540=EDGE_CURVE('',#3660,#3659,#2148,.T.) ;
#4541=EDGE_CURVE('',#3584,#3661,#2149,.T.) ;
#4542=EDGE_CURVE('',#3661,#3660,#2150,.T.) ;
#4543=EDGE_CURVE('',#3654,#3661,#2151,.T.) ;
#4544=EDGE_CURVE('',#3565,#3662,#2152,.T.) ;
#4545=EDGE_CURVE('',#3662,#3663,#582,.T.) ;
#4546=EDGE_CURVE('',#3566,#3663,#2153,.T.) ;
#4547=EDGE_CURVE('',#3663,#3664,#583,.T.) ;
#4548=EDGE_CURVE('',#3567,#3664,#2154,.T.) ;
#4549=EDGE_CURVE('',#3664,#3665,#584,.T.) ;
#4550=EDGE_CURVE('',#3568,#3665,#2155,.T.) ;
#4551=EDGE_CURVE('',#3665,#3666,#2156,.T.) ;
#4552=EDGE_CURVE('',#3569,#3666,#2157,.T.) ;
#4553=EDGE_CURVE('',#3666,#3667,#585,.T.) ;
#4554=EDGE_CURVE('',#3570,#3667,#2158,.T.) ;
#4555=EDGE_CURVE('',#3667,#3668,#586,.T.) ;
#4556=EDGE_CURVE('',#3571,#3668,#2159,.T.) ;
#4557=EDGE_CURVE('',#3668,#3669,#587,.T.) ;
#4558=EDGE_CURVE('',#3572,#3669,#2160,.T.) ;
#4559=EDGE_CURVE('',#3669,#3670,#588,.T.) ;
#4560=EDGE_CURVE('',#3573,#3670,#2161,.T.) ;
#4561=EDGE_CURVE('',#3670,#3671,#589,.T.) ;
#4562=EDGE_CURVE('',#3574,#3671,#2162,.T.) ;
#4563=EDGE_CURVE('',#3671,#3672,#590,.T.) ;
#4564=EDGE_CURVE('',#3575,#3672,#2163,.T.) ;
#4565=EDGE_CURVE('',#3672,#3673,#591,.T.) ;
#4566=EDGE_CURVE('',#3576,#3673,#2164,.T.) ;
#4567=EDGE_CURVE('',#3673,#3674,#592,.T.) ;
#4568=EDGE_CURVE('',#3577,#3674,#2165,.T.) ;
#4569=EDGE_CURVE('',#3674,#3675,#593,.T.) ;
#4570=EDGE_CURVE('',#3578,#3675,#2166,.T.) ;
#4571=EDGE_CURVE('',#3675,#3676,#594,.T.) ;
#4572=EDGE_CURVE('',#3579,#3676,#2167,.T.) ;
#4573=EDGE_CURVE('',#3676,#3677,#595,.T.) ;
#4574=EDGE_CURVE('',#3580,#3677,#2168,.T.) ;
#4575=EDGE_CURVE('',#3677,#3678,#596,.T.) ;
#4576=EDGE_CURVE('',#3581,#3678,#2169,.T.) ;
#4577=EDGE_CURVE('',#3678,#3679,#597,.T.) ;
#4578=EDGE_CURVE('',#3547,#3679,#2170,.T.) ;
#4579=EDGE_CURVE('',#3679,#3680,#598,.T.) ;
#4580=EDGE_CURVE('',#3548,#3680,#2171,.T.) ;
#4581=EDGE_CURVE('',#3564,#3681,#2172,.T.) ;
#4582=EDGE_CURVE('',#3681,#3662,#599,.T.) ;
#4583=EDGE_CURVE('',#3563,#3682,#2173,.T.) ;
#4584=EDGE_CURVE('',#3682,#3681,#600,.T.) ;
#4585=EDGE_CURVE('',#3562,#3683,#2174,.T.) ;
#4586=EDGE_CURVE('',#3683,#3682,#601,.T.) ;
#4587=EDGE_CURVE('',#3561,#3684,#2175,.T.) ;
#4588=EDGE_CURVE('',#3684,#3683,#602,.T.) ;
#4589=EDGE_CURVE('',#3560,#3685,#2176,.T.) ;
#4590=EDGE_CURVE('',#3685,#3684,#603,.T.) ;
#4591=EDGE_CURVE('',#3559,#3686,#2177,.T.) ;
#4592=EDGE_CURVE('',#3686,#3685,#604,.T.) ;
#4593=EDGE_CURVE('',#3558,#3687,#2178,.T.) ;
#4594=EDGE_CURVE('',#3687,#3686,#605,.T.) ;
#4595=EDGE_CURVE('',#3557,#3688,#2179,.T.) ;
#4596=EDGE_CURVE('',#3688,#3687,#606,.T.) ;
#4597=EDGE_CURVE('',#3556,#3689,#2180,.T.) ;
#4598=EDGE_CURVE('',#3689,#3688,#607,.T.) ;
#4599=EDGE_CURVE('',#3555,#3690,#2181,.T.) ;
#4600=EDGE_CURVE('',#3690,#3689,#608,.T.) ;
#4601=EDGE_CURVE('',#3554,#3691,#2182,.T.) ;
#4602=EDGE_CURVE('',#3691,#3690,#609,.T.) ;
#4603=EDGE_CURVE('',#3553,#3692,#2183,.T.) ;
#4604=EDGE_CURVE('',#3692,#3691,#610,.T.) ;
#4605=EDGE_CURVE('',#3552,#3693,#2184,.T.) ;
#4606=EDGE_CURVE('',#3693,#3692,#611,.T.) ;
#4607=EDGE_CURVE('',#3551,#3694,#2185,.T.) ;
#4608=EDGE_CURVE('',#3694,#3693,#612,.T.) ;
#4609=EDGE_CURVE('',#3550,#3695,#2186,.T.) ;
#4610=EDGE_CURVE('',#3695,#3694,#613,.T.) ;
#4611=EDGE_CURVE('',#3549,#3696,#2187,.T.) ;
#4612=EDGE_CURVE('',#3696,#3695,#2188,.T.) ;
#4613=EDGE_CURVE('',#3680,#3696,#614,.T.) ;
#4614=EDGE_CURVE('',#3540,#3697,#2189,.T.) ;
#4615=EDGE_CURVE('',#3697,#3698,#2190,.T.) ;
#4616=EDGE_CURVE('',#3541,#3698,#2191,.T.) ;
#4617=EDGE_CURVE('',#3698,#3699,#2192,.T.) ;
#4618=EDGE_CURVE('',#3542,#3699,#2193,.T.) ;
#4619=EDGE_CURVE('',#3699,#3700,#2194,.T.) ;
#4620=EDGE_CURVE('',#3543,#3700,#2195,.T.) ;
#4621=EDGE_CURVE('',#3700,#3701,#2196,.T.) ;
#4622=EDGE_CURVE('',#3544,#3701,#2197,.T.) ;
#4623=EDGE_CURVE('',#3701,#3702,#2198,.T.) ;
#4624=EDGE_CURVE('',#3545,#3702,#2199,.T.) ;
#4625=EDGE_CURVE('',#3702,#3703,#2200,.T.) ;
#4626=EDGE_CURVE('',#3546,#3703,#2201,.T.) ;
#4627=EDGE_CURVE('',#3703,#3704,#2202,.T.) ;
#4628=EDGE_CURVE('',#3532,#3704,#2203,.T.) ;
#4629=EDGE_CURVE('',#3704,#3705,#2204,.T.) ;
#4630=EDGE_CURVE('',#3533,#3705,#2205,.T.) ;
#4631=EDGE_CURVE('',#3539,#3706,#2206,.T.) ;
#4632=EDGE_CURVE('',#3706,#3697,#2207,.T.) ;
#4633=EDGE_CURVE('',#3538,#3707,#2208,.T.) ;
#4634=EDGE_CURVE('',#3707,#3706,#615,.T.) ;
#4635=EDGE_CURVE('',#3537,#3708,#2209,.T.) ;
#4636=EDGE_CURVE('',#3708,#3707,#616,.T.) ;
#4637=EDGE_CURVE('',#3536,#3709,#2210,.T.) ;
#4638=EDGE_CURVE('',#3709,#3708,#2211,.T.) ;
#4639=EDGE_CURVE('',#3535,#3710,#2212,.T.) ;
#4640=EDGE_CURVE('',#3710,#3709,#2213,.T.) ;
#4641=EDGE_CURVE('',#3534,#3711,#2214,.T.) ;
#4642=EDGE_CURVE('',#3711,#3710,#2215,.T.) ;
#4643=EDGE_CURVE('',#3705,#3711,#2216,.T.) ;
#4644=EDGE_CURVE('',#3712,#3712,#3185,.T.) ;
#4645=EDGE_CURVE('',#3712,#3713,#2217,.T.) ;
#4646=EDGE_CURVE('',#3713,#3713,#3186,.T.) ;
#4647=EDGE_CURVE('',#3714,#3714,#3187,.T.) ;
#4648=EDGE_CURVE('',#3715,#3716,#2218,.T.) ;
#4649=EDGE_CURVE('',#3716,#3717,#3188,.T.) ;
#4650=EDGE_CURVE('',#3717,#3718,#3189,.T.) ;
#4651=EDGE_CURVE('',#3718,#3719,#2219,.T.) ;
#4652=EDGE_CURVE('',#3719,#3715,#3190,.T.) ;
#4653=EDGE_CURVE('',#3715,#3719,#617,.T.) ;
#4654=EDGE_CURVE('',#3718,#3716,#618,.T.) ;
#4655=EDGE_CURVE('',#3715,#3720,#3191,.T.) ;
#4656=EDGE_CURVE('',#3721,#3720,#619,.T.) ;
#4657=EDGE_CURVE('',#3721,#3722,#3192,.T.) ;
#4658=EDGE_CURVE('',#3723,#3722,#620,.T.) ;
#4659=EDGE_CURVE('',#3723,#3724,#3193,.T.) ;
#4660=EDGE_CURVE('',#3725,#3724,#621,.T.) ;
#4661=EDGE_CURVE('',#3725,#3726,#3194,.T.) ;
#4662=EDGE_CURVE('',#3726,#3727,#3195,.T.) ;
#4663=EDGE_CURVE('',#3727,#3728,#3196,.T.) ;
#4664=EDGE_CURVE('',#3728,#3727,#3197,.T.) ;
#4665=EDGE_CURVE('',#3726,#3719,#3198,.T.) ;
#4666=EDGE_CURVE('',#3717,#3729,#2220,.T.) ;
#4667=EDGE_CURVE('',#3729,#3729,#3199,.T.) ;
#4668=EDGE_CURVE('',#3725,#3730,#2221,.T.) ;
#4669=EDGE_CURVE('',#3730,#3731,#3200,.T.) ;
#4670=EDGE_CURVE('',#3731,#3732,#3201,.T.) ;
#4671=EDGE_CURVE('',#3732,#3724,#2222,.T.) ;
#4672=EDGE_CURVE('',#3724,#3725,#3202,.T.) ;
#4673=EDGE_CURVE('',#3732,#3730,#622,.T.) ;
#4674=EDGE_CURVE('',#3731,#3733,#2223,.T.) ;
#4675=EDGE_CURVE('',#3733,#3733,#3203,.T.) ;
#4676=EDGE_CURVE('',#3723,#3734,#2224,.T.) ;
#4677=EDGE_CURVE('',#3734,#3735,#3204,.T.) ;
#4678=EDGE_CURVE('',#3735,#3736,#3205,.T.) ;
#4679=EDGE_CURVE('',#3736,#3722,#2225,.T.) ;
#4680=EDGE_CURVE('',#3722,#3723,#3206,.T.) ;
#4681=EDGE_CURVE('',#3736,#3734,#623,.T.) ;
#4682=EDGE_CURVE('',#3735,#3737,#2226,.T.) ;
#4683=EDGE_CURVE('',#3737,#3737,#3207,.T.) ;
#4684=EDGE_CURVE('',#3721,#3738,#2227,.T.) ;
#4685=EDGE_CURVE('',#3738,#3739,#3208,.T.) ;
#4686=EDGE_CURVE('',#3739,#3740,#3209,.T.) ;
#4687=EDGE_CURVE('',#3740,#3720,#2228,.T.) ;
#4688=EDGE_CURVE('',#3720,#3721,#3210,.T.) ;
#4689=EDGE_CURVE('',#3740,#3738,#624,.T.) ;
#4690=EDGE_CURVE('',#3739,#3741,#2229,.T.) ;
#4691=EDGE_CURVE('',#3741,#3741,#3211,.T.) ;
#4692=EDGE_CURVE('',#3742,#3742,#3212,.T.) ;
#4693=EDGE_CURVE('',#3743,#3743,#3213,.T.) ;
#4694=EDGE_CURVE('',#3744,#3744,#3214,.T.) ;
#4695=EDGE_CURVE('',#3745,#3745,#3215,.T.) ;
#4696=EDGE_CURVE('',#3742,#3746,#2230,.T.) ;
#4697=EDGE_CURVE('',#3746,#3746,#3216,.T.) ;
#4698=EDGE_CURVE('',#3743,#3747,#2231,.T.) ;
#4699=EDGE_CURVE('',#3747,#3747,#3217,.T.) ;
#4700=EDGE_CURVE('',#3744,#3748,#2232,.T.) ;
#4701=EDGE_CURVE('',#3748,#3748,#3218,.T.) ;
#4702=EDGE_CURVE('',#3745,#3749,#2233,.T.) ;
#4703=EDGE_CURVE('',#3749,#3749,#3219,.T.) ;
#4704=EDGE_CURVE('',#3750,#3751,#2234,.T.) ;
#4705=EDGE_CURVE('',#3752,#3750,#3220,.T.) ;
#4706=EDGE_CURVE('',#3753,#3752,#2235,.T.) ;
#4707=EDGE_CURVE('',#3751,#3753,#3221,.T.) ;
#4708=EDGE_CURVE('',#3754,#3755,#2236,.T.) ;
#4709=EDGE_CURVE('',#3756,#3754,#3222,.T.) ;
#4710=EDGE_CURVE('',#3757,#3756,#2237,.T.) ;
#4711=EDGE_CURVE('',#3755,#3757,#3223,.T.) ;
#4712=EDGE_CURVE('',#3758,#3759,#2238,.T.) ;
#4713=EDGE_CURVE('',#3760,#3758,#3224,.T.) ;
#4714=EDGE_CURVE('',#3761,#3760,#2239,.T.) ;
#4715=EDGE_CURVE('',#3759,#3761,#3225,.T.) ;
#4716=EDGE_CURVE('',#3762,#3763,#2240,.T.) ;
#4717=EDGE_CURVE('',#3764,#3762,#3226,.T.) ;
#4718=EDGE_CURVE('',#3765,#3764,#2241,.T.) ;
#4719=EDGE_CURVE('',#3763,#3765,#3227,.T.) ;
#4720=EDGE_CURVE('',#3766,#3766,#3228,.T.) ;
#4721=EDGE_CURVE('',#3764,#3753,#3229,.T.) ;
#4722=EDGE_CURVE('',#3760,#3762,#3230,.T.) ;
#4723=EDGE_CURVE('',#3755,#3758,#3231,.T.) ;
#4724=EDGE_CURVE('',#3751,#3757,#3232,.T.) ;
#4725=EDGE_CURVE('',#3761,#3763,#3233,.T.) ;
#4726=EDGE_CURVE('',#3754,#3759,#3234,.T.) ;
#4727=EDGE_CURVE('',#3765,#3752,#3235,.T.) ;
#4728=EDGE_CURVE('',#3750,#3756,#3236,.T.) ;
#4729=EDGE_CURVE('',#3767,#3767,#3237,.T.) ;
#4730=EDGE_CURVE('',#3714,#3728,#2242,.T.) ;
#4731=EDGE_CURVE('',#3768,#3768,#3238,.T.) ;
#4732=EDGE_CURVE('',#3769,#3769,#3239,.T.) ;
#4733=EDGE_CURVE('',#3768,#3770,#2243,.T.) ;
#4734=EDGE_CURVE('',#3770,#3770,#3240,.T.) ;
#4735=EDGE_CURVE('',#3771,#3771,#3241,.T.) ;
#4736=EDGE_CURVE('',#3772,#3772,#3242,.T.) ;
#4737=EDGE_CURVE('',#3772,#3771,#2244,.T.) ;
#4738=EDGE_CURVE('',#3773,#3773,#3243,.T.) ;
#4739=EDGE_CURVE('',#3774,#3774,#3244,.T.) ;
#4740=EDGE_CURVE('',#3773,#3775,#2245,.T.) ;
#4741=EDGE_CURVE('',#3775,#3775,#3245,.T.) ;
#4742=EDGE_CURVE('',#3776,#3776,#3246,.T.) ;
#4743=EDGE_CURVE('',#3777,#3777,#3247,.T.) ;
#4744=EDGE_CURVE('',#3777,#3776,#2246,.T.) ;
#4745=EDGE_CURVE('',#3774,#3778,#2247,.T.) ;
#4746=EDGE_CURVE('',#3778,#3778,#3248,.T.) ;
#4747=EDGE_CURVE('',#3779,#3779,#3249,.T.) ;
#4748=EDGE_CURVE('',#3780,#3780,#3250,.T.) ;
#4749=EDGE_CURVE('',#3780,#3779,#2248,.T.) ;
#4750=EDGE_CURVE('',#3781,#3781,#3251,.T.) ;
#4751=EDGE_CURVE('',#3781,#3780,#2249,.T.) ;
#4752=EDGE_CURVE('',#3767,#3781,#2250,.T.) ;
#4753=EDGE_CURVE('',#3782,#3782,#3252,.T.) ;
#4754=EDGE_CURVE('',#3782,#3530,#2251,.T.) ;
#4755=EDGE_CURVE('',#3769,#3766,#2252,.T.) ;
#5525=ORIENTED_EDGE('',*,*,#4260,.F.) ;
#5526=ORIENTED_EDGE('',*,*,#4261,.T.) ;
#5527=ORIENTED_EDGE('',*,*,#4262,.T.) ;
#5528=ORIENTED_EDGE('',*,*,#4263,.F.) ;
#5529=ORIENTED_EDGE('',*,*,#4264,.F.) ;
#5530=ORIENTED_EDGE('',*,*,#4263,.T.) ;
#5531=ORIENTED_EDGE('',*,*,#4265,.T.) ;
#5532=ORIENTED_EDGE('',*,*,#4266,.F.) ;
#5533=ORIENTED_EDGE('',*,*,#4267,.F.) ;
#5534=ORIENTED_EDGE('',*,*,#4266,.T.) ;
#5535=ORIENTED_EDGE('',*,*,#4268,.T.) ;
#5536=ORIENTED_EDGE('',*,*,#4269,.F.) ;
#5537=ORIENTED_EDGE('',*,*,#4270,.F.) ;
#5538=ORIENTED_EDGE('',*,*,#4269,.T.) ;
#5539=ORIENTED_EDGE('',*,*,#4271,.T.) ;
#5540=ORIENTED_EDGE('',*,*,#4272,.F.) ;
#5541=ORIENTED_EDGE('',*,*,#4273,.F.) ;
#5542=ORIENTED_EDGE('',*,*,#4274,.T.) ;
#5543=ORIENTED_EDGE('',*,*,#4275,.T.) ;
#5544=ORIENTED_EDGE('',*,*,#4276,.F.) ;
#5545=ORIENTED_EDGE('',*,*,#4277,.F.) ;
#5546=ORIENTED_EDGE('',*,*,#4276,.T.) ;
#5547=ORIENTED_EDGE('',*,*,#4278,.T.) ;
#5548=ORIENTED_EDGE('',*,*,#4279,.F.) ;
#5549=ORIENTED_EDGE('',*,*,#4280,.F.) ;
#5550=ORIENTED_EDGE('',*,*,#4279,.T.) ;
#5551=ORIENTED_EDGE('',*,*,#4281,.T.) ;
#5552=ORIENTED_EDGE('',*,*,#4282,.F.) ;
#5553=ORIENTED_EDGE('',*,*,#4283,.F.) ;
#5554=ORIENTED_EDGE('',*,*,#4282,.T.) ;
#5555=ORIENTED_EDGE('',*,*,#4284,.T.) ;
#5556=ORIENTED_EDGE('',*,*,#4285,.F.) ;
#5557=ORIENTED_EDGE('',*,*,#4286,.F.) ;
#5558=ORIENTED_EDGE('',*,*,#4285,.T.) ;
#5559=ORIENTED_EDGE('',*,*,#4287,.T.) ;
#5560=ORIENTED_EDGE('',*,*,#4288,.F.) ;
#5561=ORIENTED_EDGE('',*,*,#4289,.F.) ;
#5562=ORIENTED_EDGE('',*,*,#4288,.T.) ;
#5563=ORIENTED_EDGE('',*,*,#4290,.T.) ;
#5564=ORIENTED_EDGE('',*,*,#4291,.F.) ;
#5565=ORIENTED_EDGE('',*,*,#4292,.F.) ;
#5566=ORIENTED_EDGE('',*,*,#4291,.T.) ;
#5567=ORIENTED_EDGE('',*,*,#4293,.T.) ;
#5568=ORIENTED_EDGE('',*,*,#4294,.F.) ;
#5569=ORIENTED_EDGE('',*,*,#4295,.F.) ;
#5570=ORIENTED_EDGE('',*,*,#4294,.T.) ;
#5571=ORIENTED_EDGE('',*,*,#4296,.T.) ;
#5572=ORIENTED_EDGE('',*,*,#4297,.F.) ;
#5573=ORIENTED_EDGE('',*,*,#4298,.F.) ;
#5574=ORIENTED_EDGE('',*,*,#4297,.T.) ;
#5575=ORIENTED_EDGE('',*,*,#4299,.T.) ;
#5576=ORIENTED_EDGE('',*,*,#4300,.F.) ;
#5577=ORIENTED_EDGE('',*,*,#4301,.F.) ;
#5578=ORIENTED_EDGE('',*,*,#4272,.T.) ;
#5579=ORIENTED_EDGE('',*,*,#4302,.T.) ;
#5580=ORIENTED_EDGE('',*,*,#4303,.F.) ;
#5581=ORIENTED_EDGE('',*,*,#4304,.F.) ;
#5582=ORIENTED_EDGE('',*,*,#4305,.T.) ;
#5583=ORIENTED_EDGE('',*,*,#4306,.T.) ;
#5584=ORIENTED_EDGE('',*,*,#4261,.F.) ;
#5585=ORIENTED_EDGE('',*,*,#4307,.F.) ;
#5586=ORIENTED_EDGE('',*,*,#4308,.T.) ;
#5587=ORIENTED_EDGE('',*,*,#4309,.T.) ;
#5588=ORIENTED_EDGE('',*,*,#4305,.F.) ;
#5589=ORIENTED_EDGE('',*,*,#4310,.F.) ;
#5590=ORIENTED_EDGE('',*,*,#4311,.T.) ;
#5591=ORIENTED_EDGE('',*,*,#4312,.T.) ;
#5592=ORIENTED_EDGE('',*,*,#4308,.F.) ;
#5593=ORIENTED_EDGE('',*,*,#4313,.F.) ;
#5594=ORIENTED_EDGE('',*,*,#4303,.T.) ;
#5595=ORIENTED_EDGE('',*,*,#4314,.T.) ;
#5596=ORIENTED_EDGE('',*,*,#4311,.F.) ;
#5597=ORIENTED_EDGE('',*,*,#4315,.F.) ;
#5598=ORIENTED_EDGE('',*,*,#4300,.T.) ;
#5599=ORIENTED_EDGE('',*,*,#4316,.T.) ;
#5600=ORIENTED_EDGE('',*,*,#4317,.F.) ;
#5601=ORIENTED_EDGE('',*,*,#4318,.F.) ;
#5602=ORIENTED_EDGE('',*,*,#4319,.T.) ;
#5603=ORIENTED_EDGE('',*,*,#4320,.T.) ;
#5604=ORIENTED_EDGE('',*,*,#4274,.F.) ;
#5605=ORIENTED_EDGE('',*,*,#4321,.F.) ;
#5606=ORIENTED_EDGE('',*,*,#4322,.T.) ;
#5607=ORIENTED_EDGE('',*,*,#4323,.T.) ;
#5608=ORIENTED_EDGE('',*,*,#4319,.F.) ;
#5609=ORIENTED_EDGE('',*,*,#4324,.F.) ;
#5610=ORIENTED_EDGE('',*,*,#4325,.T.) ;
#5611=ORIENTED_EDGE('',*,*,#4326,.T.) ;
#5612=ORIENTED_EDGE('',*,*,#4322,.F.) ;
#5613=ORIENTED_EDGE('',*,*,#4327,.F.) ;
#5614=ORIENTED_EDGE('',*,*,#4328,.T.) ;
#5615=ORIENTED_EDGE('',*,*,#4329,.T.) ;
#5616=ORIENTED_EDGE('',*,*,#4325,.F.) ;
#5617=ORIENTED_EDGE('',*,*,#4330,.F.) ;
#5618=ORIENTED_EDGE('',*,*,#4331,.T.) ;
#5619=ORIENTED_EDGE('',*,*,#4332,.T.) ;
#5620=ORIENTED_EDGE('',*,*,#4328,.F.) ;
#5621=ORIENTED_EDGE('',*,*,#4333,.F.) ;
#5622=ORIENTED_EDGE('',*,*,#4334,.T.) ;
#5623=ORIENTED_EDGE('',*,*,#4335,.T.) ;
#5624=ORIENTED_EDGE('',*,*,#4331,.F.) ;
#5625=ORIENTED_EDGE('',*,*,#4336,.F.) ;
#5626=ORIENTED_EDGE('',*,*,#4337,.T.) ;
#5627=ORIENTED_EDGE('',*,*,#4338,.T.) ;
#5628=ORIENTED_EDGE('',*,*,#4334,.F.) ;
#5629=ORIENTED_EDGE('',*,*,#4339,.F.) ;
#5630=ORIENTED_EDGE('',*,*,#4340,.T.) ;
#5631=ORIENTED_EDGE('',*,*,#4341,.T.) ;
#5632=ORIENTED_EDGE('',*,*,#4337,.F.) ;
#5633=ORIENTED_EDGE('',*,*,#4342,.F.) ;
#5634=ORIENTED_EDGE('',*,*,#4317,.T.) ;
#5635=ORIENTED_EDGE('',*,*,#4343,.T.) ;
#5636=ORIENTED_EDGE('',*,*,#4340,.F.) ;
#5637=ORIENTED_EDGE('',*,*,#4343,.F.) ;
#5638=ORIENTED_EDGE('',*,*,#4316,.F.) ;
#5639=ORIENTED_EDGE('',*,*,#4299,.F.) ;
#5640=ORIENTED_EDGE('',*,*,#4296,.F.) ;
#5641=ORIENTED_EDGE('',*,*,#4293,.F.) ;
#5642=ORIENTED_EDGE('',*,*,#4290,.F.) ;
#5643=ORIENTED_EDGE('',*,*,#4287,.F.) ;
#5644=ORIENTED_EDGE('',*,*,#4284,.F.) ;
#5645=ORIENTED_EDGE('',*,*,#4281,.F.) ;
#5646=ORIENTED_EDGE('',*,*,#4278,.F.) ;
#5647=ORIENTED_EDGE('',*,*,#4275,.F.) ;
#5648=ORIENTED_EDGE('',*,*,#4320,.F.) ;
#5649=ORIENTED_EDGE('',*,*,#4323,.F.) ;
#5650=ORIENTED_EDGE('',*,*,#4326,.F.) ;
#5651=ORIENTED_EDGE('',*,*,#4329,.F.) ;
#5652=ORIENTED_EDGE('',*,*,#4332,.F.) ;
#5653=ORIENTED_EDGE('',*,*,#4335,.F.) ;
#5654=ORIENTED_EDGE('',*,*,#4338,.F.) ;
#5655=ORIENTED_EDGE('',*,*,#4341,.F.) ;
#5656=ORIENTED_EDGE('',*,*,#4314,.F.) ;
#5657=ORIENTED_EDGE('',*,*,#4302,.F.) ;
#5658=ORIENTED_EDGE('',*,*,#4271,.F.) ;
#5659=ORIENTED_EDGE('',*,*,#4268,.F.) ;
#5660=ORIENTED_EDGE('',*,*,#4265,.F.) ;
#5661=ORIENTED_EDGE('',*,*,#4262,.F.) ;
#5662=ORIENTED_EDGE('',*,*,#4306,.F.) ;
#5663=ORIENTED_EDGE('',*,*,#4309,.F.) ;
#5664=ORIENTED_EDGE('',*,*,#4312,.F.) ;
#5665=ORIENTED_EDGE('',*,*,#4344,.F.) ;
#5666=ORIENTED_EDGE('',*,*,#4345,.T.) ;
#5667=ORIENTED_EDGE('',*,*,#4346,.T.) ;
#5668=ORIENTED_EDGE('',*,*,#4347,.F.) ;
#5669=ORIENTED_EDGE('',*,*,#4348,.F.) ;
#5670=ORIENTED_EDGE('',*,*,#4347,.T.) ;
#5671=ORIENTED_EDGE('',*,*,#4349,.T.) ;
#5672=ORIENTED_EDGE('',*,*,#4350,.F.) ;
#5673=ORIENTED_EDGE('',*,*,#4351,.F.) ;
#5674=ORIENTED_EDGE('',*,*,#4350,.T.) ;
#5675=ORIENTED_EDGE('',*,*,#4352,.T.) ;
#5676=ORIENTED_EDGE('',*,*,#4353,.F.) ;
#5677=ORIENTED_EDGE('',*,*,#4354,.F.) ;
#5678=ORIENTED_EDGE('',*,*,#4353,.T.) ;
#5679=ORIENTED_EDGE('',*,*,#4355,.T.) ;
#5680=ORIENTED_EDGE('',*,*,#4356,.F.) ;
#5681=ORIENTED_EDGE('',*,*,#4357,.F.) ;
#5682=ORIENTED_EDGE('',*,*,#4356,.T.) ;
#5683=ORIENTED_EDGE('',*,*,#4358,.T.) ;
#5684=ORIENTED_EDGE('',*,*,#4359,.F.) ;
#5685=ORIENTED_EDGE('',*,*,#4360,.F.) ;
#5686=ORIENTED_EDGE('',*,*,#4361,.T.) ;
#5687=ORIENTED_EDGE('',*,*,#4362,.T.) ;
#5688=ORIENTED_EDGE('',*,*,#4345,.F.) ;
#5689=ORIENTED_EDGE('',*,*,#4363,.F.) ;
#5690=ORIENTED_EDGE('',*,*,#4364,.T.) ;
#5691=ORIENTED_EDGE('',*,*,#4365,.T.) ;
#5692=ORIENTED_EDGE('',*,*,#4361,.F.) ;
#5693=ORIENTED_EDGE('',*,*,#4366,.F.) ;
#5694=ORIENTED_EDGE('',*,*,#4367,.T.) ;
#5695=ORIENTED_EDGE('',*,*,#4368,.T.) ;
#5696=ORIENTED_EDGE('',*,*,#4364,.F.) ;
#5697=ORIENTED_EDGE('',*,*,#4369,.F.) ;
#5698=ORIENTED_EDGE('',*,*,#4359,.T.) ;
#5699=ORIENTED_EDGE('',*,*,#4370,.T.) ;
#5700=ORIENTED_EDGE('',*,*,#4367,.F.) ;
#5701=ORIENTED_EDGE('',*,*,#4370,.F.) ;
#5702=ORIENTED_EDGE('',*,*,#4358,.F.) ;
#5703=ORIENTED_EDGE('',*,*,#4355,.F.) ;
#5704=ORIENTED_EDGE('',*,*,#4352,.F.) ;
#5705=ORIENTED_EDGE('',*,*,#4349,.F.) ;
#5706=ORIENTED_EDGE('',*,*,#4346,.F.) ;
#5707=ORIENTED_EDGE('',*,*,#4362,.F.) ;
#5708=ORIENTED_EDGE('',*,*,#4365,.F.) ;
#5709=ORIENTED_EDGE('',*,*,#4368,.F.) ;
#5710=ORIENTED_EDGE('',*,*,#4371,.F.) ;
#5711=ORIENTED_EDGE('',*,*,#4372,.T.) ;
#5712=ORIENTED_EDGE('',*,*,#4373,.T.) ;
#5713=ORIENTED_EDGE('',*,*,#4372,.F.) ;
#5714=ORIENTED_EDGE('',*,*,#4374,.T.) ;
#5715=ORIENTED_EDGE('',*,*,#4375,.T.) ;
#5716=ORIENTED_EDGE('',*,*,#4376,.T.) ;
#5717=ORIENTED_EDGE('',*,*,#4377,.T.) ;
#5718=ORIENTED_EDGE('',*,*,#4378,.T.) ;
#5719=ORIENTED_EDGE('',*,*,#4379,.T.) ;
#5720=ORIENTED_EDGE('',*,*,#4380,.T.) ;
#5721=ORIENTED_EDGE('',*,*,#4381,.T.) ;
#5722=ORIENTED_EDGE('',*,*,#4382,.T.) ;
#5723=ORIENTED_EDGE('',*,*,#4383,.T.) ;
#5724=ORIENTED_EDGE('',*,*,#4384,.T.) ;
#5725=ORIENTED_EDGE('',*,*,#4385,.T.) ;
#5726=ORIENTED_EDGE('',*,*,#4386,.T.) ;
#5727=ORIENTED_EDGE('',*,*,#4387,.T.) ;
#5728=ORIENTED_EDGE('',*,*,#4388,.T.) ;
#5729=ORIENTED_EDGE('',*,*,#4389,.T.) ;
#5730=ORIENTED_EDGE('',*,*,#4390,.T.) ;
#5731=ORIENTED_EDGE('',*,*,#4391,.T.) ;
#5732=ORIENTED_EDGE('',*,*,#4392,.T.) ;
#5733=ORIENTED_EDGE('',*,*,#4393,.T.) ;
#5734=ORIENTED_EDGE('',*,*,#4394,.T.) ;
#5735=ORIENTED_EDGE('',*,*,#4395,.T.) ;
#5736=ORIENTED_EDGE('',*,*,#4396,.T.) ;
#5737=ORIENTED_EDGE('',*,*,#4397,.T.) ;
#5738=ORIENTED_EDGE('',*,*,#4398,.T.) ;
#5739=ORIENTED_EDGE('',*,*,#4399,.T.) ;
#5740=ORIENTED_EDGE('',*,*,#4400,.T.) ;
#5741=ORIENTED_EDGE('',*,*,#4401,.T.) ;
#5742=ORIENTED_EDGE('',*,*,#4402,.T.) ;
#5743=ORIENTED_EDGE('',*,*,#4403,.T.) ;
#5744=ORIENTED_EDGE('',*,*,#4404,.T.) ;
#5745=ORIENTED_EDGE('',*,*,#4405,.T.) ;
#5746=ORIENTED_EDGE('',*,*,#4406,.T.) ;
#5747=ORIENTED_EDGE('',*,*,#4407,.T.) ;
#5748=ORIENTED_EDGE('',*,*,#4408,.T.) ;
#5749=ORIENTED_EDGE('',*,*,#4409,.T.) ;
#5750=ORIENTED_EDGE('',*,*,#4410,.T.) ;
#5751=ORIENTED_EDGE('',*,*,#4411,.T.) ;
#5752=ORIENTED_EDGE('',*,*,#4412,.T.) ;
#5753=ORIENTED_EDGE('',*,*,#4413,.T.) ;
#5754=ORIENTED_EDGE('',*,*,#4414,.T.) ;
#5755=ORIENTED_EDGE('',*,*,#4415,.T.) ;
#5756=ORIENTED_EDGE('',*,*,#4416,.T.) ;
#5757=ORIENTED_EDGE('',*,*,#4417,.T.) ;
#5758=ORIENTED_EDGE('',*,*,#4418,.T.) ;
#5759=ORIENTED_EDGE('',*,*,#4419,.T.) ;
#5760=ORIENTED_EDGE('',*,*,#4420,.T.) ;
#5761=ORIENTED_EDGE('',*,*,#4421,.T.) ;
#5762=ORIENTED_EDGE('',*,*,#4422,.T.) ;
#5763=ORIENTED_EDGE('',*,*,#4423,.T.) ;
#5764=ORIENTED_EDGE('',*,*,#4424,.T.) ;
#5765=ORIENTED_EDGE('',*,*,#4425,.T.) ;
#5766=ORIENTED_EDGE('',*,*,#4426,.T.) ;
#5767=ORIENTED_EDGE('',*,*,#4427,.T.) ;
#5768=ORIENTED_EDGE('',*,*,#4428,.T.) ;
#5769=ORIENTED_EDGE('',*,*,#4429,.T.) ;
#5770=ORIENTED_EDGE('',*,*,#4430,.T.) ;
#5771=ORIENTED_EDGE('',*,*,#4431,.T.) ;
#5772=ORIENTED_EDGE('',*,*,#4432,.T.) ;
#5773=ORIENTED_EDGE('',*,*,#4433,.T.) ;
#5774=ORIENTED_EDGE('',*,*,#4434,.T.) ;
#5775=ORIENTED_EDGE('',*,*,#4435,.T.) ;
#5776=ORIENTED_EDGE('',*,*,#4436,.T.) ;
#5777=ORIENTED_EDGE('',*,*,#4437,.T.) ;
#5778=ORIENTED_EDGE('',*,*,#4438,.T.) ;
#5779=ORIENTED_EDGE('',*,*,#4439,.T.) ;
#5780=ORIENTED_EDGE('',*,*,#4440,.T.) ;
#5781=ORIENTED_EDGE('',*,*,#4441,.T.) ;
#5782=ORIENTED_EDGE('',*,*,#4442,.T.) ;
#5783=ORIENTED_EDGE('',*,*,#4443,.T.) ;
#5784=ORIENTED_EDGE('',*,*,#4444,.T.) ;
#5785=ORIENTED_EDGE('',*,*,#4445,.T.) ;
#5786=ORIENTED_EDGE('',*,*,#4446,.T.) ;
#5787=ORIENTED_EDGE('',*,*,#4447,.T.) ;
#5788=ORIENTED_EDGE('',*,*,#4448,.T.) ;
#5789=ORIENTED_EDGE('',*,*,#4449,.T.) ;
#5790=ORIENTED_EDGE('',*,*,#4450,.T.) ;
#5791=ORIENTED_EDGE('',*,*,#4451,.T.) ;
#5792=ORIENTED_EDGE('',*,*,#4452,.T.) ;
#5793=ORIENTED_EDGE('',*,*,#4453,.T.) ;
#5794=ORIENTED_EDGE('',*,*,#4454,.T.) ;
#5795=ORIENTED_EDGE('',*,*,#4455,.T.) ;
#5796=ORIENTED_EDGE('',*,*,#4456,.T.) ;
#5797=ORIENTED_EDGE('',*,*,#4457,.T.) ;
#5798=ORIENTED_EDGE('',*,*,#4458,.T.) ;
#5799=ORIENTED_EDGE('',*,*,#4459,.T.) ;
#5800=ORIENTED_EDGE('',*,*,#4460,.T.) ;
#5801=ORIENTED_EDGE('',*,*,#4461,.T.) ;
#5802=ORIENTED_EDGE('',*,*,#4462,.T.) ;
#5803=ORIENTED_EDGE('',*,*,#4463,.T.) ;
#5804=ORIENTED_EDGE('',*,*,#4357,.T.) ;
#5805=ORIENTED_EDGE('',*,*,#4369,.T.) ;
#5806=ORIENTED_EDGE('',*,*,#4366,.T.) ;
#5807=ORIENTED_EDGE('',*,*,#4363,.T.) ;
#5808=ORIENTED_EDGE('',*,*,#4360,.T.) ;
#5809=ORIENTED_EDGE('',*,*,#4344,.T.) ;
#5810=ORIENTED_EDGE('',*,*,#4348,.T.) ;
#5811=ORIENTED_EDGE('',*,*,#4351,.T.) ;
#5812=ORIENTED_EDGE('',*,*,#4354,.T.) ;
#5813=ORIENTED_EDGE('',*,*,#4315,.T.) ;
#5814=ORIENTED_EDGE('',*,*,#4342,.T.) ;
#5815=ORIENTED_EDGE('',*,*,#4339,.T.) ;
#5816=ORIENTED_EDGE('',*,*,#4336,.T.) ;
#5817=ORIENTED_EDGE('',*,*,#4333,.T.) ;
#5818=ORIENTED_EDGE('',*,*,#4330,.T.) ;
#5819=ORIENTED_EDGE('',*,*,#4327,.T.) ;
#5820=ORIENTED_EDGE('',*,*,#4324,.T.) ;
#5821=ORIENTED_EDGE('',*,*,#4321,.T.) ;
#5822=ORIENTED_EDGE('',*,*,#4318,.T.) ;
#5823=ORIENTED_EDGE('',*,*,#4273,.T.) ;
#5824=ORIENTED_EDGE('',*,*,#4277,.T.) ;
#5825=ORIENTED_EDGE('',*,*,#4280,.T.) ;
#5826=ORIENTED_EDGE('',*,*,#4283,.T.) ;
#5827=ORIENTED_EDGE('',*,*,#4286,.T.) ;
#5828=ORIENTED_EDGE('',*,*,#4289,.T.) ;
#5829=ORIENTED_EDGE('',*,*,#4292,.T.) ;
#5830=ORIENTED_EDGE('',*,*,#4295,.T.) ;
#5831=ORIENTED_EDGE('',*,*,#4298,.T.) ;
#5832=ORIENTED_EDGE('',*,*,#4462,.F.) ;
#5833=ORIENTED_EDGE('',*,*,#4464,.T.) ;
#5834=ORIENTED_EDGE('',*,*,#4465,.T.) ;
#5835=ORIENTED_EDGE('',*,*,#4466,.F.) ;
#5836=ORIENTED_EDGE('',*,*,#4463,.F.) ;
#5837=ORIENTED_EDGE('',*,*,#4466,.T.) ;
#5838=ORIENTED_EDGE('',*,*,#4467,.T.) ;
#5839=ORIENTED_EDGE('',*,*,#4468,.F.) ;
#5840=ORIENTED_EDGE('',*,*,#4460,.F.) ;
#5841=ORIENTED_EDGE('',*,*,#4468,.T.) ;
#5842=ORIENTED_EDGE('',*,*,#4469,.T.) ;
#5843=ORIENTED_EDGE('',*,*,#4470,.F.) ;
#5844=ORIENTED_EDGE('',*,*,#4461,.F.) ;
#5845=ORIENTED_EDGE('',*,*,#4470,.T.) ;
#5846=ORIENTED_EDGE('',*,*,#4471,.T.) ;
#5847=ORIENTED_EDGE('',*,*,#4464,.F.) ;
#5848=ORIENTED_EDGE('',*,*,#4471,.F.) ;
#5849=ORIENTED_EDGE('',*,*,#4469,.F.) ;
#5850=ORIENTED_EDGE('',*,*,#4467,.F.) ;
#5851=ORIENTED_EDGE('',*,*,#4465,.F.) ;
#5852=ORIENTED_EDGE('',*,*,#4458,.F.) ;
#5853=ORIENTED_EDGE('',*,*,#4472,.T.) ;
#5854=ORIENTED_EDGE('',*,*,#4473,.T.) ;
#5855=ORIENTED_EDGE('',*,*,#4474,.F.) ;
#5856=ORIENTED_EDGE('',*,*,#4459,.F.) ;
#5857=ORIENTED_EDGE('',*,*,#4474,.T.) ;
#5858=ORIENTED_EDGE('',*,*,#4475,.T.) ;
#5859=ORIENTED_EDGE('',*,*,#4476,.F.) ;
#5860=ORIENTED_EDGE('',*,*,#4456,.F.) ;
#5861=ORIENTED_EDGE('',*,*,#4476,.T.) ;
#5862=ORIENTED_EDGE('',*,*,#4477,.T.) ;
#5863=ORIENTED_EDGE('',*,*,#4478,.F.) ;
#5864=ORIENTED_EDGE('',*,*,#4457,.F.) ;
#5865=ORIENTED_EDGE('',*,*,#4478,.T.) ;
#5866=ORIENTED_EDGE('',*,*,#4479,.T.) ;
#5867=ORIENTED_EDGE('',*,*,#4472,.F.) ;
#5868=ORIENTED_EDGE('',*,*,#4479,.F.) ;
#5869=ORIENTED_EDGE('',*,*,#4477,.F.) ;
#5870=ORIENTED_EDGE('',*,*,#4475,.F.) ;
#5871=ORIENTED_EDGE('',*,*,#4473,.F.) ;
#5872=ORIENTED_EDGE('',*,*,#4449,.F.) ;
#5873=ORIENTED_EDGE('',*,*,#4480,.T.) ;
#5874=ORIENTED_EDGE('',*,*,#4481,.T.) ;
#5875=ORIENTED_EDGE('',*,*,#4482,.F.) ;
#5876=ORIENTED_EDGE('',*,*,#4450,.F.) ;
#5877=ORIENTED_EDGE('',*,*,#4482,.T.) ;
#5878=ORIENTED_EDGE('',*,*,#4483,.T.) ;
#5879=ORIENTED_EDGE('',*,*,#4484,.F.) ;
#5880=ORIENTED_EDGE('',*,*,#4451,.F.) ;
#5881=ORIENTED_EDGE('',*,*,#4484,.T.) ;
#5882=ORIENTED_EDGE('',*,*,#4485,.T.) ;
#5883=ORIENTED_EDGE('',*,*,#4486,.F.) ;
#5884=ORIENTED_EDGE('',*,*,#4452,.F.) ;
#5885=ORIENTED_EDGE('',*,*,#4486,.T.) ;
#5886=ORIENTED_EDGE('',*,*,#4487,.T.) ;
#5887=ORIENTED_EDGE('',*,*,#4488,.F.) ;
#5888=ORIENTED_EDGE('',*,*,#4453,.F.) ;
#5889=ORIENTED_EDGE('',*,*,#4488,.T.) ;
#5890=ORIENTED_EDGE('',*,*,#4489,.T.) ;
#5891=ORIENTED_EDGE('',*,*,#4490,.F.) ;
#5892=ORIENTED_EDGE('',*,*,#4454,.F.) ;
#5893=ORIENTED_EDGE('',*,*,#4490,.T.) ;
#5894=ORIENTED_EDGE('',*,*,#4491,.T.) ;
#5895=ORIENTED_EDGE('',*,*,#4492,.F.) ;
#5896=ORIENTED_EDGE('',*,*,#4455,.F.) ;
#5897=ORIENTED_EDGE('',*,*,#4492,.T.) ;
#5898=ORIENTED_EDGE('',*,*,#4493,.T.) ;
#5899=ORIENTED_EDGE('',*,*,#4494,.F.) ;
#5900=ORIENTED_EDGE('',*,*,#4441,.F.) ;
#5901=ORIENTED_EDGE('',*,*,#4494,.T.) ;
#5902=ORIENTED_EDGE('',*,*,#4495,.T.) ;
#5903=ORIENTED_EDGE('',*,*,#4496,.F.) ;
#5904=ORIENTED_EDGE('',*,*,#4448,.F.) ;
#5905=ORIENTED_EDGE('',*,*,#4497,.T.) ;
#5906=ORIENTED_EDGE('',*,*,#4498,.T.) ;
#5907=ORIENTED_EDGE('',*,*,#4480,.F.) ;
#5908=ORIENTED_EDGE('',*,*,#4447,.F.) ;
#5909=ORIENTED_EDGE('',*,*,#4499,.T.) ;
#5910=ORIENTED_EDGE('',*,*,#4500,.T.) ;
#5911=ORIENTED_EDGE('',*,*,#4497,.F.) ;
#5912=ORIENTED_EDGE('',*,*,#4446,.F.) ;
#5913=ORIENTED_EDGE('',*,*,#4501,.T.) ;
#5914=ORIENTED_EDGE('',*,*,#4502,.T.) ;
#5915=ORIENTED_EDGE('',*,*,#4499,.F.) ;
#5916=ORIENTED_EDGE('',*,*,#4445,.F.) ;
#5917=ORIENTED_EDGE('',*,*,#4503,.T.) ;
#5918=ORIENTED_EDGE('',*,*,#4504,.T.) ;
#5919=ORIENTED_EDGE('',*,*,#4501,.F.) ;
#5920=ORIENTED_EDGE('',*,*,#4444,.F.) ;
#5921=ORIENTED_EDGE('',*,*,#4505,.T.) ;
#5922=ORIENTED_EDGE('',*,*,#4506,.T.) ;
#5923=ORIENTED_EDGE('',*,*,#4503,.F.) ;
#5924=ORIENTED_EDGE('',*,*,#4443,.F.) ;
#5925=ORIENTED_EDGE('',*,*,#4507,.T.) ;
#5926=ORIENTED_EDGE('',*,*,#4508,.T.) ;
#5927=ORIENTED_EDGE('',*,*,#4505,.F.) ;
#5928=ORIENTED_EDGE('',*,*,#4442,.F.) ;
#5929=ORIENTED_EDGE('',*,*,#4496,.T.) ;
#5930=ORIENTED_EDGE('',*,*,#4509,.T.) ;
#5931=ORIENTED_EDGE('',*,*,#4507,.F.) ;
#5932=ORIENTED_EDGE('',*,*,#4509,.F.) ;
#5933=ORIENTED_EDGE('',*,*,#4495,.F.) ;
#5934=ORIENTED_EDGE('',*,*,#4493,.F.) ;
#5935=ORIENTED_EDGE('',*,*,#4491,.F.) ;
#5936=ORIENTED_EDGE('',*,*,#4489,.F.) ;
#5937=ORIENTED_EDGE('',*,*,#4487,.F.) ;
#5938=ORIENTED_EDGE('',*,*,#4485,.F.) ;
#5939=ORIENTED_EDGE('',*,*,#4483,.F.) ;
#5940=ORIENTED_EDGE('',*,*,#4481,.F.) ;
#5941=ORIENTED_EDGE('',*,*,#4498,.F.) ;
#5942=ORIENTED_EDGE('',*,*,#4500,.F.) ;
#5943=ORIENTED_EDGE('',*,*,#4502,.F.) ;
#5944=ORIENTED_EDGE('',*,*,#4504,.F.) ;
#5945=ORIENTED_EDGE('',*,*,#4506,.F.) ;
#5946=ORIENTED_EDGE('',*,*,#4508,.F.) ;
#5947=ORIENTED_EDGE('',*,*,#4433,.F.) ;
#5948=ORIENTED_EDGE('',*,*,#4510,.T.) ;
#5949=ORIENTED_EDGE('',*,*,#4511,.T.) ;
#5950=ORIENTED_EDGE('',*,*,#4512,.F.) ;
#5951=ORIENTED_EDGE('',*,*,#4434,.F.) ;
#5952=ORIENTED_EDGE('',*,*,#4512,.T.) ;
#5953=ORIENTED_EDGE('',*,*,#4513,.T.) ;
#5954=ORIENTED_EDGE('',*,*,#4514,.F.) ;
#5955=ORIENTED_EDGE('',*,*,#4435,.F.) ;
#5956=ORIENTED_EDGE('',*,*,#4514,.T.) ;
#5957=ORIENTED_EDGE('',*,*,#4515,.T.) ;
#5958=ORIENTED_EDGE('',*,*,#4516,.F.) ;
#5959=ORIENTED_EDGE('',*,*,#4436,.F.) ;
#5960=ORIENTED_EDGE('',*,*,#4516,.T.) ;
#5961=ORIENTED_EDGE('',*,*,#4517,.T.) ;
#5962=ORIENTED_EDGE('',*,*,#4518,.F.) ;
#5963=ORIENTED_EDGE('',*,*,#4437,.F.) ;
#5964=ORIENTED_EDGE('',*,*,#4518,.T.) ;
#5965=ORIENTED_EDGE('',*,*,#4519,.T.) ;
#5966=ORIENTED_EDGE('',*,*,#4520,.F.) ;
#5967=ORIENTED_EDGE('',*,*,#4438,.F.) ;
#5968=ORIENTED_EDGE('',*,*,#4520,.T.) ;
#5969=ORIENTED_EDGE('',*,*,#4521,.T.) ;
#5970=ORIENTED_EDGE('',*,*,#4522,.F.) ;
#5971=ORIENTED_EDGE('',*,*,#4439,.F.) ;
#5972=ORIENTED_EDGE('',*,*,#4522,.T.) ;
#5973=ORIENTED_EDGE('',*,*,#4523,.T.) ;
#5974=ORIENTED_EDGE('',*,*,#4524,.F.) ;
#5975=ORIENTED_EDGE('',*,*,#4440,.F.) ;
#5976=ORIENTED_EDGE('',*,*,#4524,.T.) ;
#5977=ORIENTED_EDGE('',*,*,#4525,.T.) ;
#5978=ORIENTED_EDGE('',*,*,#4526,.F.) ;
#5979=ORIENTED_EDGE('',*,*,#4424,.F.) ;
#5980=ORIENTED_EDGE('',*,*,#4526,.T.) ;
#5981=ORIENTED_EDGE('',*,*,#4527,.T.) ;
#5982=ORIENTED_EDGE('',*,*,#4528,.F.) ;
#5983=ORIENTED_EDGE('',*,*,#4432,.F.) ;
#5984=ORIENTED_EDGE('',*,*,#4529,.T.) ;
#5985=ORIENTED_EDGE('',*,*,#4530,.T.) ;
#5986=ORIENTED_EDGE('',*,*,#4510,.F.) ;
#5987=ORIENTED_EDGE('',*,*,#4431,.F.) ;
#5988=ORIENTED_EDGE('',*,*,#4531,.T.) ;
#5989=ORIENTED_EDGE('',*,*,#4532,.T.) ;
#5990=ORIENTED_EDGE('',*,*,#4529,.F.) ;
#5991=ORIENTED_EDGE('',*,*,#4430,.F.) ;
#5992=ORIENTED_EDGE('',*,*,#4533,.T.) ;
#5993=ORIENTED_EDGE('',*,*,#4534,.T.) ;
#5994=ORIENTED_EDGE('',*,*,#4531,.F.) ;
#5995=ORIENTED_EDGE('',*,*,#4429,.F.) ;
#5996=ORIENTED_EDGE('',*,*,#4535,.T.) ;
#5997=ORIENTED_EDGE('',*,*,#4536,.T.) ;
#5998=ORIENTED_EDGE('',*,*,#4533,.F.) ;
#5999=ORIENTED_EDGE('',*,*,#4428,.F.) ;
#6000=ORIENTED_EDGE('',*,*,#4537,.T.) ;
#6001=ORIENTED_EDGE('',*,*,#4538,.T.) ;
#6002=ORIENTED_EDGE('',*,*,#4535,.F.) ;
#6003=ORIENTED_EDGE('',*,*,#4427,.F.) ;
#6004=ORIENTED_EDGE('',*,*,#4539,.T.) ;
#6005=ORIENTED_EDGE('',*,*,#4540,.T.) ;
#6006=ORIENTED_EDGE('',*,*,#4537,.F.) ;
#6007=ORIENTED_EDGE('',*,*,#4426,.F.) ;
#6008=ORIENTED_EDGE('',*,*,#4541,.T.) ;
#6009=ORIENTED_EDGE('',*,*,#4542,.T.) ;
#6010=ORIENTED_EDGE('',*,*,#4539,.F.) ;
#6011=ORIENTED_EDGE('',*,*,#4425,.F.) ;
#6012=ORIENTED_EDGE('',*,*,#4528,.T.) ;
#6013=ORIENTED_EDGE('',*,*,#4543,.T.) ;
#6014=ORIENTED_EDGE('',*,*,#4541,.F.) ;
#6015=ORIENTED_EDGE('',*,*,#4543,.F.) ;
#6016=ORIENTED_EDGE('',*,*,#4527,.F.) ;
#6017=ORIENTED_EDGE('',*,*,#4525,.F.) ;
#6018=ORIENTED_EDGE('',*,*,#4523,.F.) ;
#6019=ORIENTED_EDGE('',*,*,#4521,.F.) ;
#6020=ORIENTED_EDGE('',*,*,#4519,.F.) ;
#6021=ORIENTED_EDGE('',*,*,#4517,.F.) ;
#6022=ORIENTED_EDGE('',*,*,#4515,.F.) ;
#6023=ORIENTED_EDGE('',*,*,#4513,.F.) ;
#6024=ORIENTED_EDGE('',*,*,#4511,.F.) ;
#6025=ORIENTED_EDGE('',*,*,#4530,.F.) ;
#6026=ORIENTED_EDGE('',*,*,#4532,.F.) ;
#6027=ORIENTED_EDGE('',*,*,#4534,.F.) ;
#6028=ORIENTED_EDGE('',*,*,#4536,.F.) ;
#6029=ORIENTED_EDGE('',*,*,#4538,.F.) ;
#6030=ORIENTED_EDGE('',*,*,#4540,.F.) ;
#6031=ORIENTED_EDGE('',*,*,#4542,.F.) ;
#6032=ORIENTED_EDGE('',*,*,#4407,.F.) ;
#6033=ORIENTED_EDGE('',*,*,#4544,.T.) ;
#6034=ORIENTED_EDGE('',*,*,#4545,.T.) ;
#6035=ORIENTED_EDGE('',*,*,#4546,.F.) ;
#6036=ORIENTED_EDGE('',*,*,#4408,.F.) ;
#6037=ORIENTED_EDGE('',*,*,#4546,.T.) ;
#6038=ORIENTED_EDGE('',*,*,#4547,.T.) ;
#6039=ORIENTED_EDGE('',*,*,#4548,.F.) ;
#6040=ORIENTED_EDGE('',*,*,#4409,.F.) ;
#6041=ORIENTED_EDGE('',*,*,#4548,.T.) ;
#6042=ORIENTED_EDGE('',*,*,#4549,.T.) ;
#6043=ORIENTED_EDGE('',*,*,#4550,.F.) ;
#6044=ORIENTED_EDGE('',*,*,#4410,.F.) ;
#6045=ORIENTED_EDGE('',*,*,#4550,.T.) ;
#6046=ORIENTED_EDGE('',*,*,#4551,.T.) ;
#6047=ORIENTED_EDGE('',*,*,#4552,.F.) ;
#6048=ORIENTED_EDGE('',*,*,#4411,.F.) ;
#6049=ORIENTED_EDGE('',*,*,#4552,.T.) ;
#6050=ORIENTED_EDGE('',*,*,#4553,.T.) ;
#6051=ORIENTED_EDGE('',*,*,#4554,.F.) ;
#6052=ORIENTED_EDGE('',*,*,#4412,.F.) ;
#6053=ORIENTED_EDGE('',*,*,#4554,.T.) ;
#6054=ORIENTED_EDGE('',*,*,#4555,.T.) ;
#6055=ORIENTED_EDGE('',*,*,#4556,.F.) ;
#6056=ORIENTED_EDGE('',*,*,#4413,.F.) ;
#6057=ORIENTED_EDGE('',*,*,#4556,.T.) ;
#6058=ORIENTED_EDGE('',*,*,#4557,.T.) ;
#6059=ORIENTED_EDGE('',*,*,#4558,.F.) ;
#6060=ORIENTED_EDGE('',*,*,#4414,.F.) ;
#6061=ORIENTED_EDGE('',*,*,#4558,.T.) ;
#6062=ORIENTED_EDGE('',*,*,#4559,.T.) ;
#6063=ORIENTED_EDGE('',*,*,#4560,.F.) ;
#6064=ORIENTED_EDGE('',*,*,#4415,.F.) ;
#6065=ORIENTED_EDGE('',*,*,#4560,.T.) ;
#6066=ORIENTED_EDGE('',*,*,#4561,.T.) ;
#6067=ORIENTED_EDGE('',*,*,#4562,.F.) ;
#6068=ORIENTED_EDGE('',*,*,#4416,.F.) ;
#6069=ORIENTED_EDGE('',*,*,#4562,.T.) ;
#6070=ORIENTED_EDGE('',*,*,#4563,.T.) ;
#6071=ORIENTED_EDGE('',*,*,#4564,.F.) ;
#6072=ORIENTED_EDGE('',*,*,#4417,.F.) ;
#6073=ORIENTED_EDGE('',*,*,#4564,.T.) ;
#6074=ORIENTED_EDGE('',*,*,#4565,.T.) ;
#6075=ORIENTED_EDGE('',*,*,#4566,.F.) ;
#6076=ORIENTED_EDGE('',*,*,#4418,.F.) ;
#6077=ORIENTED_EDGE('',*,*,#4566,.T.) ;
#6078=ORIENTED_EDGE('',*,*,#4567,.T.) ;
#6079=ORIENTED_EDGE('',*,*,#4568,.F.) ;
#6080=ORIENTED_EDGE('',*,*,#4419,.F.) ;
#6081=ORIENTED_EDGE('',*,*,#4568,.T.) ;
#6082=ORIENTED_EDGE('',*,*,#4569,.T.) ;
#6083=ORIENTED_EDGE('',*,*,#4570,.F.) ;
#6084=ORIENTED_EDGE('',*,*,#4420,.F.) ;
#6085=ORIENTED_EDGE('',*,*,#4570,.T.) ;
#6086=ORIENTED_EDGE('',*,*,#4571,.T.) ;
#6087=ORIENTED_EDGE('',*,*,#4572,.F.) ;
#6088=ORIENTED_EDGE('',*,*,#4421,.F.) ;
#6089=ORIENTED_EDGE('',*,*,#4572,.T.) ;
#6090=ORIENTED_EDGE('',*,*,#4573,.T.) ;
#6091=ORIENTED_EDGE('',*,*,#4574,.F.) ;
#6092=ORIENTED_EDGE('',*,*,#4422,.F.) ;
#6093=ORIENTED_EDGE('',*,*,#4574,.T.) ;
#6094=ORIENTED_EDGE('',*,*,#4575,.T.) ;
#6095=ORIENTED_EDGE('',*,*,#4576,.F.) ;
#6096=ORIENTED_EDGE('',*,*,#4423,.F.) ;
#6097=ORIENTED_EDGE('',*,*,#4576,.T.) ;
#6098=ORIENTED_EDGE('',*,*,#4577,.T.) ;
#6099=ORIENTED_EDGE('',*,*,#4578,.F.) ;
#6100=ORIENTED_EDGE('',*,*,#4389,.F.) ;
#6101=ORIENTED_EDGE('',*,*,#4578,.T.) ;
#6102=ORIENTED_EDGE('',*,*,#4579,.T.) ;
#6103=ORIENTED_EDGE('',*,*,#4580,.F.) ;
#6104=ORIENTED_EDGE('',*,*,#4406,.F.) ;
#6105=ORIENTED_EDGE('',*,*,#4581,.T.) ;
#6106=ORIENTED_EDGE('',*,*,#4582,.T.) ;
#6107=ORIENTED_EDGE('',*,*,#4544,.F.) ;
#6108=ORIENTED_EDGE('',*,*,#4405,.F.) ;
#6109=ORIENTED_EDGE('',*,*,#4583,.T.) ;
#6110=ORIENTED_EDGE('',*,*,#4584,.T.) ;
#6111=ORIENTED_EDGE('',*,*,#4581,.F.) ;
#6112=ORIENTED_EDGE('',*,*,#4404,.F.) ;
#6113=ORIENTED_EDGE('',*,*,#4585,.T.) ;
#6114=ORIENTED_EDGE('',*,*,#4586,.T.) ;
#6115=ORIENTED_EDGE('',*,*,#4583,.F.) ;
#6116=ORIENTED_EDGE('',*,*,#4403,.F.) ;
#6117=ORIENTED_EDGE('',*,*,#4587,.T.) ;
#6118=ORIENTED_EDGE('',*,*,#4588,.T.) ;
#6119=ORIENTED_EDGE('',*,*,#4585,.F.) ;
#6120=ORIENTED_EDGE('',*,*,#4402,.F.) ;
#6121=ORIENTED_EDGE('',*,*,#4589,.T.) ;
#6122=ORIENTED_EDGE('',*,*,#4590,.T.) ;
#6123=ORIENTED_EDGE('',*,*,#4587,.F.) ;
#6124=ORIENTED_EDGE('',*,*,#4401,.F.) ;
#6125=ORIENTED_EDGE('',*,*,#4591,.T.) ;
#6126=ORIENTED_EDGE('',*,*,#4592,.T.) ;
#6127=ORIENTED_EDGE('',*,*,#4589,.F.) ;
#6128=ORIENTED_EDGE('',*,*,#4400,.F.) ;
#6129=ORIENTED_EDGE('',*,*,#4593,.T.) ;
#6130=ORIENTED_EDGE('',*,*,#4594,.T.) ;
#6131=ORIENTED_EDGE('',*,*,#4591,.F.) ;
#6132=ORIENTED_EDGE('',*,*,#4399,.F.) ;
#6133=ORIENTED_EDGE('',*,*,#4595,.T.) ;
#6134=ORIENTED_EDGE('',*,*,#4596,.T.) ;
#6135=ORIENTED_EDGE('',*,*,#4593,.F.) ;
#6136=ORIENTED_EDGE('',*,*,#4398,.F.) ;
#6137=ORIENTED_EDGE('',*,*,#4597,.T.) ;
#6138=ORIENTED_EDGE('',*,*,#4598,.T.) ;
#6139=ORIENTED_EDGE('',*,*,#4595,.F.) ;
#6140=ORIENTED_EDGE('',*,*,#4397,.F.) ;
#6141=ORIENTED_EDGE('',*,*,#4599,.T.) ;
#6142=ORIENTED_EDGE('',*,*,#4600,.T.) ;
#6143=ORIENTED_EDGE('',*,*,#4597,.F.) ;
#6144=ORIENTED_EDGE('',*,*,#4396,.F.) ;
#6145=ORIENTED_EDGE('',*,*,#4601,.T.) ;
#6146=ORIENTED_EDGE('',*,*,#4602,.T.) ;
#6147=ORIENTED_EDGE('',*,*,#4599,.F.) ;
#6148=ORIENTED_EDGE('',*,*,#4395,.F.) ;
#6149=ORIENTED_EDGE('',*,*,#4603,.T.) ;
#6150=ORIENTED_EDGE('',*,*,#4604,.T.) ;
#6151=ORIENTED_EDGE('',*,*,#4601,.F.) ;
#6152=ORIENTED_EDGE('',*,*,#4394,.F.) ;
#6153=ORIENTED_EDGE('',*,*,#4605,.T.) ;
#6154=ORIENTED_EDGE('',*,*,#4606,.T.) ;
#6155=ORIENTED_EDGE('',*,*,#4603,.F.) ;
#6156=ORIENTED_EDGE('',*,*,#4393,.F.) ;
#6157=ORIENTED_EDGE('',*,*,#4607,.T.) ;
#6158=ORIENTED_EDGE('',*,*,#4608,.T.) ;
#6159=ORIENTED_EDGE('',*,*,#4605,.F.) ;
#6160=ORIENTED_EDGE('',*,*,#4392,.F.) ;
#6161=ORIENTED_EDGE('',*,*,#4609,.T.) ;
#6162=ORIENTED_EDGE('',*,*,#4610,.T.) ;
#6163=ORIENTED_EDGE('',*,*,#4607,.F.) ;
#6164=ORIENTED_EDGE('',*,*,#4391,.F.) ;
#6165=ORIENTED_EDGE('',*,*,#4611,.T.) ;
#6166=ORIENTED_EDGE('',*,*,#4612,.T.) ;
#6167=ORIENTED_EDGE('',*,*,#4609,.F.) ;
#6168=ORIENTED_EDGE('',*,*,#4390,.F.) ;
#6169=ORIENTED_EDGE('',*,*,#4580,.T.) ;
#6170=ORIENTED_EDGE('',*,*,#4613,.T.) ;
#6171=ORIENTED_EDGE('',*,*,#4611,.F.) ;
#6172=ORIENTED_EDGE('',*,*,#4613,.F.) ;
#6173=ORIENTED_EDGE('',*,*,#4579,.F.) ;
#6174=ORIENTED_EDGE('',*,*,#4577,.F.) ;
#6175=ORIENTED_EDGE('',*,*,#4575,.F.) ;
#6176=ORIENTED_EDGE('',*,*,#4573,.F.) ;
#6177=ORIENTED_EDGE('',*,*,#4571,.F.) ;
#6178=ORIENTED_EDGE('',*,*,#4569,.F.) ;
#6179=ORIENTED_EDGE('',*,*,#4567,.F.) ;
#6180=ORIENTED_EDGE('',*,*,#4565,.F.) ;
#6181=ORIENTED_EDGE('',*,*,#4563,.F.) ;
#6182=ORIENTED_EDGE('',*,*,#4561,.F.) ;
#6183=ORIENTED_EDGE('',*,*,#4559,.F.) ;
#6184=ORIENTED_EDGE('',*,*,#4557,.F.) ;
#6185=ORIENTED_EDGE('',*,*,#4555,.F.) ;
#6186=ORIENTED_EDGE('',*,*,#4553,.F.) ;
#6187=ORIENTED_EDGE('',*,*,#4551,.F.) ;
#6188=ORIENTED_EDGE('',*,*,#4549,.F.) ;
#6189=ORIENTED_EDGE('',*,*,#4547,.F.) ;
#6190=ORIENTED_EDGE('',*,*,#4545,.F.) ;
#6191=ORIENTED_EDGE('',*,*,#4582,.F.) ;
#6192=ORIENTED_EDGE('',*,*,#4584,.F.) ;
#6193=ORIENTED_EDGE('',*,*,#4586,.F.) ;
#6194=ORIENTED_EDGE('',*,*,#4588,.F.) ;
#6195=ORIENTED_EDGE('',*,*,#4590,.F.) ;
#6196=ORIENTED_EDGE('',*,*,#4592,.F.) ;
#6197=ORIENTED_EDGE('',*,*,#4594,.F.) ;
#6198=ORIENTED_EDGE('',*,*,#4596,.F.) ;
#6199=ORIENTED_EDGE('',*,*,#4598,.F.) ;
#6200=ORIENTED_EDGE('',*,*,#4600,.F.) ;
#6201=ORIENTED_EDGE('',*,*,#4602,.F.) ;
#6202=ORIENTED_EDGE('',*,*,#4604,.F.) ;
#6203=ORIENTED_EDGE('',*,*,#4606,.F.) ;
#6204=ORIENTED_EDGE('',*,*,#4608,.F.) ;
#6205=ORIENTED_EDGE('',*,*,#4610,.F.) ;
#6206=ORIENTED_EDGE('',*,*,#4612,.F.) ;
#6207=ORIENTED_EDGE('',*,*,#4382,.F.) ;
#6208=ORIENTED_EDGE('',*,*,#4614,.T.) ;
#6209=ORIENTED_EDGE('',*,*,#4615,.T.) ;
#6210=ORIENTED_EDGE('',*,*,#4616,.F.) ;
#6211=ORIENTED_EDGE('',*,*,#4383,.F.) ;
#6212=ORIENTED_EDGE('',*,*,#4616,.T.) ;
#6213=ORIENTED_EDGE('',*,*,#4617,.T.) ;
#6214=ORIENTED_EDGE('',*,*,#4618,.F.) ;
#6215=ORIENTED_EDGE('',*,*,#4384,.F.) ;
#6216=ORIENTED_EDGE('',*,*,#4618,.T.) ;
#6217=ORIENTED_EDGE('',*,*,#4619,.T.) ;
#6218=ORIENTED_EDGE('',*,*,#4620,.F.) ;
#6219=ORIENTED_EDGE('',*,*,#4385,.F.) ;
#6220=ORIENTED_EDGE('',*,*,#4620,.T.) ;
#6221=ORIENTED_EDGE('',*,*,#4621,.T.) ;
#6222=ORIENTED_EDGE('',*,*,#4622,.F.) ;
#6223=ORIENTED_EDGE('',*,*,#4386,.F.) ;
#6224=ORIENTED_EDGE('',*,*,#4622,.T.) ;
#6225=ORIENTED_EDGE('',*,*,#4623,.T.) ;
#6226=ORIENTED_EDGE('',*,*,#4624,.F.) ;
#6227=ORIENTED_EDGE('',*,*,#4387,.F.) ;
#6228=ORIENTED_EDGE('',*,*,#4624,.T.) ;
#6229=ORIENTED_EDGE('',*,*,#4625,.T.) ;
#6230=ORIENTED_EDGE('',*,*,#4626,.F.) ;
#6231=ORIENTED_EDGE('',*,*,#4388,.F.) ;
#6232=ORIENTED_EDGE('',*,*,#4626,.T.) ;
#6233=ORIENTED_EDGE('',*,*,#4627,.T.) ;
#6234=ORIENTED_EDGE('',*,*,#4628,.F.) ;
#6235=ORIENTED_EDGE('',*,*,#4374,.F.) ;
#6236=ORIENTED_EDGE('',*,*,#4628,.T.) ;
#6237=ORIENTED_EDGE('',*,*,#4629,.T.) ;
#6238=ORIENTED_EDGE('',*,*,#4630,.F.) ;
#6239=ORIENTED_EDGE('',*,*,#4381,.F.) ;
#6240=ORIENTED_EDGE('',*,*,#4631,.T.) ;
#6241=ORIENTED_EDGE('',*,*,#4632,.T.) ;
#6242=ORIENTED_EDGE('',*,*,#4614,.F.) ;
#6243=ORIENTED_EDGE('',*,*,#4380,.F.) ;
#6244=ORIENTED_EDGE('',*,*,#4633,.T.) ;
#6245=ORIENTED_EDGE('',*,*,#4634,.T.) ;
#6246=ORIENTED_EDGE('',*,*,#4631,.F.) ;
#6247=ORIENTED_EDGE('',*,*,#4379,.F.) ;
#6248=ORIENTED_EDGE('',*,*,#4635,.T.) ;
#6249=ORIENTED_EDGE('',*,*,#4636,.T.) ;
#6250=ORIENTED_EDGE('',*,*,#4633,.F.) ;
#6251=ORIENTED_EDGE('',*,*,#4378,.F.) ;
#6252=ORIENTED_EDGE('',*,*,#4637,.T.) ;
#6253=ORIENTED_EDGE('',*,*,#4638,.T.) ;
#6254=ORIENTED_EDGE('',*,*,#4635,.F.) ;
#6255=ORIENTED_EDGE('',*,*,#4377,.F.) ;
#6256=ORIENTED_EDGE('',*,*,#4639,.T.) ;
#6257=ORIENTED_EDGE('',*,*,#4640,.T.) ;
#6258=ORIENTED_EDGE('',*,*,#4637,.F.) ;
#6259=ORIENTED_EDGE('',*,*,#4376,.F.) ;
#6260=ORIENTED_EDGE('',*,*,#4641,.T.) ;
#6261=ORIENTED_EDGE('',*,*,#4642,.T.) ;
#6262=ORIENTED_EDGE('',*,*,#4639,.F.) ;
#6263=ORIENTED_EDGE('',*,*,#4375,.F.) ;
#6264=ORIENTED_EDGE('',*,*,#4630,.T.) ;
#6265=ORIENTED_EDGE('',*,*,#4643,.T.) ;
#6266=ORIENTED_EDGE('',*,*,#4641,.F.) ;
#6267=ORIENTED_EDGE('',*,*,#4643,.F.) ;
#6268=ORIENTED_EDGE('',*,*,#4629,.F.) ;
#6269=ORIENTED_EDGE('',*,*,#4627,.F.) ;
#6270=ORIENTED_EDGE('',*,*,#4625,.F.) ;
#6271=ORIENTED_EDGE('',*,*,#4623,.F.) ;
#6272=ORIENTED_EDGE('',*,*,#4621,.F.) ;
#6273=ORIENTED_EDGE('',*,*,#4619,.F.) ;
#6274=ORIENTED_EDGE('',*,*,#4617,.F.) ;
#6275=ORIENTED_EDGE('',*,*,#4615,.F.) ;
#6276=ORIENTED_EDGE('',*,*,#4632,.F.) ;
#6277=ORIENTED_EDGE('',*,*,#4634,.F.) ;
#6278=ORIENTED_EDGE('',*,*,#4636,.F.) ;
#6279=ORIENTED_EDGE('',*,*,#4638,.F.) ;
#6280=ORIENTED_EDGE('',*,*,#4640,.F.) ;
#6281=ORIENTED_EDGE('',*,*,#4642,.F.) ;
#6282=ORIENTED_EDGE('',*,*,#4644,.T.) ;
#6283=ORIENTED_EDGE('',*,*,#4645,.T.) ;
#6284=ORIENTED_EDGE('',*,*,#4646,.F.) ;
#6285=ORIENTED_EDGE('',*,*,#4645,.F.) ;
#6286=ORIENTED_EDGE('',*,*,#4647,.F.) ;
#6287=ORIENTED_EDGE('',*,*,#4644,.F.) ;
#6288=ORIENTED_EDGE('',*,*,#4373,.F.) ;
#6289=ORIENTED_EDGE('',*,*,#4646,.T.) ;
#6290=ORIENTED_EDGE('',*,*,#4301,.T.) ;
#6291=ORIENTED_EDGE('',*,*,#4313,.T.) ;
#6292=ORIENTED_EDGE('',*,*,#4310,.T.) ;
#6293=ORIENTED_EDGE('',*,*,#4307,.T.) ;
#6294=ORIENTED_EDGE('',*,*,#4304,.T.) ;
#6295=ORIENTED_EDGE('',*,*,#4260,.T.) ;
#6296=ORIENTED_EDGE('',*,*,#4264,.T.) ;
#6297=ORIENTED_EDGE('',*,*,#4267,.T.) ;
#6298=ORIENTED_EDGE('',*,*,#4270,.T.) ;
#6299=ORIENTED_EDGE('',*,*,#4648,.T.) ;
#6300=ORIENTED_EDGE('',*,*,#4649,.T.) ;
#6301=ORIENTED_EDGE('',*,*,#4650,.T.) ;
#6302=ORIENTED_EDGE('',*,*,#4651,.T.) ;
#6303=ORIENTED_EDGE('',*,*,#4652,.T.) ;
#6304=ORIENTED_EDGE('',*,*,#4648,.F.) ;
#6305=ORIENTED_EDGE('',*,*,#4653,.T.) ;
#6306=ORIENTED_EDGE('',*,*,#4651,.F.) ;
#6307=ORIENTED_EDGE('',*,*,#4654,.T.) ;
#6308=ORIENTED_EDGE('',*,*,#4653,.F.) ;
#6309=ORIENTED_EDGE('',*,*,#4655,.T.) ;
#6310=ORIENTED_EDGE('',*,*,#4656,.F.) ;
#6311=ORIENTED_EDGE('',*,*,#4657,.T.) ;
#6312=ORIENTED_EDGE('',*,*,#4658,.F.) ;
#6313=ORIENTED_EDGE('',*,*,#4659,.T.) ;
#6314=ORIENTED_EDGE('',*,*,#4660,.F.) ;
#6315=ORIENTED_EDGE('',*,*,#4661,.T.) ;
#6316=ORIENTED_EDGE('',*,*,#4662,.T.) ;
#6317=ORIENTED_EDGE('',*,*,#4663,.T.) ;
#6318=ORIENTED_EDGE('',*,*,#4664,.T.) ;
#6319=ORIENTED_EDGE('',*,*,#4662,.F.) ;
#6320=ORIENTED_EDGE('',*,*,#4665,.T.) ;
#6321=ORIENTED_EDGE('',*,*,#4649,.F.) ;
#6322=ORIENTED_EDGE('',*,*,#4654,.F.) ;
#6323=ORIENTED_EDGE('',*,*,#4650,.F.) ;
#6324=ORIENTED_EDGE('',*,*,#4666,.T.) ;
#6325=ORIENTED_EDGE('',*,*,#4667,.T.) ;
#6326=ORIENTED_EDGE('',*,*,#4666,.F.) ;
#6327=ORIENTED_EDGE('',*,*,#4668,.T.) ;
#6328=ORIENTED_EDGE('',*,*,#4669,.T.) ;
#6329=ORIENTED_EDGE('',*,*,#4670,.T.) ;
#6330=ORIENTED_EDGE('',*,*,#4671,.T.) ;
#6331=ORIENTED_EDGE('',*,*,#4672,.T.) ;
#6332=ORIENTED_EDGE('',*,*,#4668,.F.) ;
#6333=ORIENTED_EDGE('',*,*,#4660,.T.) ;
#6334=ORIENTED_EDGE('',*,*,#4671,.F.) ;
#6335=ORIENTED_EDGE('',*,*,#4673,.T.) ;
#6336=ORIENTED_EDGE('',*,*,#4669,.F.) ;
#6337=ORIENTED_EDGE('',*,*,#4673,.F.) ;
#6338=ORIENTED_EDGE('',*,*,#4670,.F.) ;
#6339=ORIENTED_EDGE('',*,*,#4674,.T.) ;
#6340=ORIENTED_EDGE('',*,*,#4675,.T.) ;
#6341=ORIENTED_EDGE('',*,*,#4674,.F.) ;
#6342=ORIENTED_EDGE('',*,*,#4676,.T.) ;
#6343=ORIENTED_EDGE('',*,*,#4677,.T.) ;
#6344=ORIENTED_EDGE('',*,*,#4678,.T.) ;
#6345=ORIENTED_EDGE('',*,*,#4679,.T.) ;
#6346=ORIENTED_EDGE('',*,*,#4680,.T.) ;
#6347=ORIENTED_EDGE('',*,*,#4676,.F.) ;
#6348=ORIENTED_EDGE('',*,*,#4658,.T.) ;
#6349=ORIENTED_EDGE('',*,*,#4679,.F.) ;
#6350=ORIENTED_EDGE('',*,*,#4681,.T.) ;
#6351=ORIENTED_EDGE('',*,*,#4677,.F.) ;
#6352=ORIENTED_EDGE('',*,*,#4681,.F.) ;
#6353=ORIENTED_EDGE('',*,*,#4678,.F.) ;
#6354=ORIENTED_EDGE('',*,*,#4682,.T.) ;
#6355=ORIENTED_EDGE('',*,*,#4683,.T.) ;
#6356=ORIENTED_EDGE('',*,*,#4682,.F.) ;
#6357=ORIENTED_EDGE('',*,*,#4684,.T.) ;
#6358=ORIENTED_EDGE('',*,*,#4685,.T.) ;
#6359=ORIENTED_EDGE('',*,*,#4686,.T.) ;
#6360=ORIENTED_EDGE('',*,*,#4687,.T.) ;
#6361=ORIENTED_EDGE('',*,*,#4688,.T.) ;
#6362=ORIENTED_EDGE('',*,*,#4684,.F.) ;
#6363=ORIENTED_EDGE('',*,*,#4656,.T.) ;
#6364=ORIENTED_EDGE('',*,*,#4687,.F.) ;
#6365=ORIENTED_EDGE('',*,*,#4689,.T.) ;
#6366=ORIENTED_EDGE('',*,*,#4685,.F.) ;
#6367=ORIENTED_EDGE('',*,*,#4689,.F.) ;
#6368=ORIENTED_EDGE('',*,*,#4686,.F.) ;
#6369=ORIENTED_EDGE('',*,*,#4690,.T.) ;
#6370=ORIENTED_EDGE('',*,*,#4691,.T.) ;
#6371=ORIENTED_EDGE('',*,*,#4690,.F.) ;
#6372=ORIENTED_EDGE('',*,*,#4691,.F.) ;
#6373=ORIENTED_EDGE('',*,*,#4692,.F.) ;
#6374=ORIENTED_EDGE('',*,*,#4683,.F.) ;
#6375=ORIENTED_EDGE('',*,*,#4693,.F.) ;
#6376=ORIENTED_EDGE('',*,*,#4675,.F.) ;
#6377=ORIENTED_EDGE('',*,*,#4694,.F.) ;
#6378=ORIENTED_EDGE('',*,*,#4667,.F.) ;
#6379=ORIENTED_EDGE('',*,*,#4695,.F.) ;
#6380=ORIENTED_EDGE('',*,*,#4692,.T.) ;
#6381=ORIENTED_EDGE('',*,*,#4696,.T.) ;
#6382=ORIENTED_EDGE('',*,*,#4697,.F.) ;
#6383=ORIENTED_EDGE('',*,*,#4696,.F.) ;
#6384=ORIENTED_EDGE('',*,*,#4693,.T.) ;
#6385=ORIENTED_EDGE('',*,*,#4698,.T.) ;
#6386=ORIENTED_EDGE('',*,*,#4699,.F.) ;
#6387=ORIENTED_EDGE('',*,*,#4698,.F.) ;
#6388=ORIENTED_EDGE('',*,*,#4694,.T.) ;
#6389=ORIENTED_EDGE('',*,*,#4700,.T.) ;
#6390=ORIENTED_EDGE('',*,*,#4701,.F.) ;
#6391=ORIENTED_EDGE('',*,*,#4700,.F.) ;
#6392=ORIENTED_EDGE('',*,*,#4695,.T.) ;
#6393=ORIENTED_EDGE('',*,*,#4702,.T.) ;
#6394=ORIENTED_EDGE('',*,*,#4703,.F.) ;
#6395=ORIENTED_EDGE('',*,*,#4702,.F.) ;
#6396=ORIENTED_EDGE('',*,*,#4704,.F.) ;
#6397=ORIENTED_EDGE('',*,*,#4705,.F.) ;
#6398=ORIENTED_EDGE('',*,*,#4706,.F.) ;
#6399=ORIENTED_EDGE('',*,*,#4707,.F.) ;
#6400=ORIENTED_EDGE('',*,*,#4708,.F.) ;
#6401=ORIENTED_EDGE('',*,*,#4709,.F.) ;
#6402=ORIENTED_EDGE('',*,*,#4710,.F.) ;
#6403=ORIENTED_EDGE('',*,*,#4711,.F.) ;
#6404=ORIENTED_EDGE('',*,*,#4712,.F.) ;
#6405=ORIENTED_EDGE('',*,*,#4713,.F.) ;
#6406=ORIENTED_EDGE('',*,*,#4714,.F.) ;
#6407=ORIENTED_EDGE('',*,*,#4715,.F.) ;
#6408=ORIENTED_EDGE('',*,*,#4716,.F.) ;
#6409=ORIENTED_EDGE('',*,*,#4717,.F.) ;
#6410=ORIENTED_EDGE('',*,*,#4718,.F.) ;
#6411=ORIENTED_EDGE('',*,*,#4719,.F.) ;
#6412=ORIENTED_EDGE('',*,*,#4720,.T.) ;
#6413=ORIENTED_EDGE('',*,*,#4707,.T.) ;
#6414=ORIENTED_EDGE('',*,*,#4721,.F.) ;
#6415=ORIENTED_EDGE('',*,*,#4717,.T.) ;
#6416=ORIENTED_EDGE('',*,*,#4722,.F.) ;
#6417=ORIENTED_EDGE('',*,*,#4713,.T.) ;
#6418=ORIENTED_EDGE('',*,*,#4723,.F.) ;
#6419=ORIENTED_EDGE('',*,*,#4711,.T.) ;
#6420=ORIENTED_EDGE('',*,*,#4724,.F.) ;
#6421=ORIENTED_EDGE('',*,*,#4714,.T.) ;
#6422=ORIENTED_EDGE('',*,*,#4722,.T.) ;
#6423=ORIENTED_EDGE('',*,*,#4716,.T.) ;
#6424=ORIENTED_EDGE('',*,*,#4725,.F.) ;
#6425=ORIENTED_EDGE('',*,*,#4708,.T.) ;
#6426=ORIENTED_EDGE('',*,*,#4723,.T.) ;
#6427=ORIENTED_EDGE('',*,*,#4712,.T.) ;
#6428=ORIENTED_EDGE('',*,*,#4726,.F.) ;
#6429=ORIENTED_EDGE('',*,*,#4706,.T.) ;
#6430=ORIENTED_EDGE('',*,*,#4727,.F.) ;
#6431=ORIENTED_EDGE('',*,*,#4718,.T.) ;
#6432=ORIENTED_EDGE('',*,*,#4721,.T.) ;
#6433=ORIENTED_EDGE('',*,*,#4704,.T.) ;
#6434=ORIENTED_EDGE('',*,*,#4724,.T.) ;
#6435=ORIENTED_EDGE('',*,*,#4710,.T.) ;
#6436=ORIENTED_EDGE('',*,*,#4728,.F.) ;
#6437=ORIENTED_EDGE('',*,*,#4729,.T.) ;
#6438=ORIENTED_EDGE('',*,*,#4652,.F.) ;
#6439=ORIENTED_EDGE('',*,*,#4665,.F.) ;
#6440=ORIENTED_EDGE('',*,*,#4661,.F.) ;
#6441=ORIENTED_EDGE('',*,*,#4672,.F.) ;
#6442=ORIENTED_EDGE('',*,*,#4659,.F.) ;
#6443=ORIENTED_EDGE('',*,*,#4680,.F.) ;
#6444=ORIENTED_EDGE('',*,*,#4657,.F.) ;
#6445=ORIENTED_EDGE('',*,*,#4688,.F.) ;
#6446=ORIENTED_EDGE('',*,*,#4655,.F.) ;
#6447=ORIENTED_EDGE('',*,*,#4647,.T.) ;
#6448=ORIENTED_EDGE('',*,*,#4730,.T.) ;
#6449=ORIENTED_EDGE('',*,*,#4663,.F.) ;
#6450=ORIENTED_EDGE('',*,*,#4664,.F.) ;
#6451=ORIENTED_EDGE('',*,*,#4730,.F.) ;
#6452=ORIENTED_EDGE('',*,*,#4731,.T.) ;
#6453=ORIENTED_EDGE('',*,*,#4732,.F.) ;
#6454=ORIENTED_EDGE('',*,*,#4731,.F.) ;
#6455=ORIENTED_EDGE('',*,*,#4733,.T.) ;
#6456=ORIENTED_EDGE('',*,*,#4734,.T.) ;
#6457=ORIENTED_EDGE('',*,*,#4733,.F.) ;
#6458=ORIENTED_EDGE('',*,*,#4734,.F.) ;
#6459=ORIENTED_EDGE('',*,*,#4735,.F.) ;
#6460=ORIENTED_EDGE('',*,*,#4736,.T.) ;
#6461=ORIENTED_EDGE('',*,*,#4737,.T.) ;
#6462=ORIENTED_EDGE('',*,*,#4735,.T.) ;
#6463=ORIENTED_EDGE('',*,*,#4737,.F.) ;
#6464=ORIENTED_EDGE('',*,*,#4738,.T.) ;
#6465=ORIENTED_EDGE('',*,*,#4739,.F.) ;
#6466=ORIENTED_EDGE('',*,*,#4738,.F.) ;
#6467=ORIENTED_EDGE('',*,*,#4740,.T.) ;
#6468=ORIENTED_EDGE('',*,*,#4741,.T.) ;
#6469=ORIENTED_EDGE('',*,*,#4740,.F.) ;
#6470=ORIENTED_EDGE('',*,*,#4741,.F.) ;
#6471=ORIENTED_EDGE('',*,*,#4742,.F.) ;
#6472=ORIENTED_EDGE('',*,*,#4743,.T.) ;
#6473=ORIENTED_EDGE('',*,*,#4744,.T.) ;
#6474=ORIENTED_EDGE('',*,*,#4742,.T.) ;
#6475=ORIENTED_EDGE('',*,*,#4744,.F.) ;
#6476=ORIENTED_EDGE('',*,*,#4743,.F.) ;
#6477=ORIENTED_EDGE('',*,*,#4705,.T.) ;
#6478=ORIENTED_EDGE('',*,*,#4728,.T.) ;
#6479=ORIENTED_EDGE('',*,*,#4709,.T.) ;
#6480=ORIENTED_EDGE('',*,*,#4726,.T.) ;
#6481=ORIENTED_EDGE('',*,*,#4715,.T.) ;
#6482=ORIENTED_EDGE('',*,*,#4725,.T.) ;
#6483=ORIENTED_EDGE('',*,*,#4719,.T.) ;
#6484=ORIENTED_EDGE('',*,*,#4727,.T.) ;
#6485=ORIENTED_EDGE('',*,*,#4739,.T.) ;
#6486=ORIENTED_EDGE('',*,*,#4745,.T.) ;
#6487=ORIENTED_EDGE('',*,*,#4746,.F.) ;
#6488=ORIENTED_EDGE('',*,*,#4745,.F.) ;
#6489=ORIENTED_EDGE('',*,*,#4747,.F.) ;
#6490=ORIENTED_EDGE('',*,*,#4746,.T.) ;
#6491=ORIENTED_EDGE('',*,*,#4703,.T.) ;
#6492=ORIENTED_EDGE('',*,*,#4701,.T.) ;
#6493=ORIENTED_EDGE('',*,*,#4699,.T.) ;
#6494=ORIENTED_EDGE('',*,*,#4697,.T.) ;
#6495=ORIENTED_EDGE('',*,*,#4748,.F.) ;
#6496=ORIENTED_EDGE('',*,*,#4749,.T.) ;
#6497=ORIENTED_EDGE('',*,*,#4747,.T.) ;
#6498=ORIENTED_EDGE('',*,*,#4749,.F.) ;
#6499=ORIENTED_EDGE('',*,*,#4750,.F.) ;
#6500=ORIENTED_EDGE('',*,*,#4751,.T.) ;
#6501=ORIENTED_EDGE('',*,*,#4748,.T.) ;
#6502=ORIENTED_EDGE('',*,*,#4751,.F.) ;
#6503=ORIENTED_EDGE('',*,*,#4729,.F.) ;
#6504=ORIENTED_EDGE('',*,*,#4752,.T.) ;
#6505=ORIENTED_EDGE('',*,*,#4750,.T.) ;
#6506=ORIENTED_EDGE('',*,*,#4752,.F.) ;
#6507=ORIENTED_EDGE('',*,*,#4753,.F.) ;
#6508=ORIENTED_EDGE('',*,*,#4754,.T.) ;
#6509=ORIENTED_EDGE('',*,*,#4371,.T.) ;
#6510=ORIENTED_EDGE('',*,*,#4754,.F.) ;
#6511=ORIENTED_EDGE('',*,*,#4753,.T.) ;
#6512=ORIENTED_EDGE('',*,*,#4736,.F.) ;
#6513=ORIENTED_EDGE('',*,*,#4732,.T.) ;
#6514=ORIENTED_EDGE('',*,*,#4755,.T.) ;
#6515=ORIENTED_EDGE('',*,*,#4720,.F.) ;
#6516=ORIENTED_EDGE('',*,*,#4755,.F.) ;
#7721=CONICAL_SURFACE('',#8442,4.15,0.785398163397448) ;
#7722=CONICAL_SURFACE('',#8457,4.15,0.785398163397448) ;
#7723=CONICAL_SURFACE('',#8463,4.15,0.785398163397452) ;
#7724=CONICAL_SURFACE('',#8469,4.15,0.785398163397452) ;
#7725=CONICAL_SURFACE('',#8543,25.25,0.785398163397448) ;
#7726=CONICAL_SURFACE('',#8547,25.25,0.785398163397448) ;
#7727=CONICAL_SURFACE('',#8548,15.25,0.785398163397448) ;
#7772=ADVANCED_FACE('',(#1097),#330,.F.) ;
#7773=ADVANCED_FACE('',(#1098),#331,.F.) ;
#7774=ADVANCED_FACE('',(#1099),#332,.F.) ;
#7775=ADVANCED_FACE('',(#1100),#333,.F.) ;
#7776=ADVANCED_FACE('',(#1101),#334,.F.) ;
#7777=ADVANCED_FACE('',(#1102),#335,.F.) ;
#7778=ADVANCED_FACE('',(#1103),#336,.F.) ;
#7779=ADVANCED_FACE('',(#1104),#337,.F.) ;
#7780=ADVANCED_FACE('',(#1105),#338,.F.) ;
#7781=ADVANCED_FACE('',(#1106),#339,.F.) ;
#7782=ADVANCED_FACE('',(#1107),#340,.F.) ;
#7783=ADVANCED_FACE('',(#1108),#341,.F.) ;
#7784=ADVANCED_FACE('',(#1109),#342,.F.) ;
#7785=ADVANCED_FACE('',(#1110),#343,.F.) ;
#7786=ADVANCED_FACE('',(#1111),#344,.F.) ;
#7787=ADVANCED_FACE('',(#1112),#345,.F.) ;
#7788=ADVANCED_FACE('',(#1113),#346,.F.) ;
#7789=ADVANCED_FACE('',(#1114),#347,.F.) ;
#7790=ADVANCED_FACE('',(#1115),#348,.F.) ;
#7791=ADVANCED_FACE('',(#1116),#349,.F.) ;
#7792=ADVANCED_FACE('',(#1117),#350,.F.) ;
#7793=ADVANCED_FACE('',(#1118),#351,.F.) ;
#7794=ADVANCED_FACE('',(#1119),#352,.F.) ;
#7795=ADVANCED_FACE('',(#1120),#353,.F.) ;
#7796=ADVANCED_FACE('',(#1121),#354,.F.) ;
#7797=ADVANCED_FACE('',(#1122),#355,.F.) ;
#7798=ADVANCED_FACE('',(#1123),#747,.F.) ;
#7799=ADVANCED_FACE('',(#1124),#356,.F.) ;
#7800=ADVANCED_FACE('',(#1125,#691),#748,.T.) ;
#7801=ADVANCED_FACE('',(#1126),#357,.F.) ;
#7802=ADVANCED_FACE('',(#1127),#749,.F.) ;
#7803=ADVANCED_FACE('',(#1128),#358,.F.) ;
#7804=ADVANCED_FACE('',(#1129),#359,.F.) ;
#7805=ADVANCED_FACE('',(#1130),#750,.F.) ;
#7806=ADVANCED_FACE('',(#1131),#360,.F.) ;
#7807=ADVANCED_FACE('',(#1132),#751,.F.) ;
#7808=ADVANCED_FACE('',(#1133),#752,.F.) ;
#7809=ADVANCED_FACE('',(#1134),#753,.F.) ;
#7810=ADVANCED_FACE('',(#1135),#754,.T.) ;
#7811=ADVANCED_FACE('',(#1136,#692,#693,#694,#695,#696,#697,#698,#699),
#989,.T.) ;
#7812=ADVANCED_FACE('',(#1137),#755,.F.) ;
#7813=ADVANCED_FACE('',(#1138),#756,.F.) ;
#7814=ADVANCED_FACE('',(#1139),#757,.F.) ;
#7815=ADVANCED_FACE('',(#1140),#758,.F.) ;
#7816=ADVANCED_FACE('',(#1141),#759,.F.) ;
#7817=ADVANCED_FACE('',(#1142),#760,.F.) ;
#7818=ADVANCED_FACE('',(#1143),#761,.F.) ;
#7819=ADVANCED_FACE('',(#1144),#762,.F.) ;
#7820=ADVANCED_FACE('',(#1145),#763,.F.) ;
#7821=ADVANCED_FACE('',(#1146),#764,.F.) ;
#7822=ADVANCED_FACE('',(#1147),#765,.F.) ;
#7823=ADVANCED_FACE('',(#1148),#766,.F.) ;
#7824=ADVANCED_FACE('',(#1149),#767,.F.) ;
#7825=ADVANCED_FACE('',(#1150),#768,.F.) ;
#7826=ADVANCED_FACE('',(#1151),#769,.F.) ;
#7827=ADVANCED_FACE('',(#1152),#770,.F.) ;
#7828=ADVANCED_FACE('',(#1153),#771,.F.) ;
#7829=ADVANCED_FACE('',(#1154),#772,.F.) ;
#7830=ADVANCED_FACE('',(#1155),#773,.F.) ;
#7831=ADVANCED_FACE('',(#1156),#361,.F.) ;
#7832=ADVANCED_FACE('',(#1157),#362,.F.) ;
#7833=ADVANCED_FACE('',(#1158),#774,.F.) ;
#7834=ADVANCED_FACE('',(#1159),#775,.F.) ;
#7835=ADVANCED_FACE('',(#1160),#776,.F.) ;
#7836=ADVANCED_FACE('',(#1161),#777,.F.) ;
#7837=ADVANCED_FACE('',(#1162),#778,.T.) ;
#7838=ADVANCED_FACE('',(#1163),#363,.F.) ;
#7839=ADVANCED_FACE('',(#1164),#779,.F.) ;
#7840=ADVANCED_FACE('',(#1165),#780,.F.) ;
#7841=ADVANCED_FACE('',(#1166),#781,.F.) ;
#7842=ADVANCED_FACE('',(#1167),#364,.F.) ;
#7843=ADVANCED_FACE('',(#1168),#365,.F.) ;
#7844=ADVANCED_FACE('',(#1169),#366,.F.) ;
#7845=ADVANCED_FACE('',(#1170),#367,.F.) ;
#7846=ADVANCED_FACE('',(#1171),#368,.F.) ;
#7847=ADVANCED_FACE('',(#1172),#369,.F.) ;
#7848=ADVANCED_FACE('',(#1173),#370,.F.) ;
#7849=ADVANCED_FACE('',(#1174),#371,.F.) ;
#7850=ADVANCED_FACE('',(#1175),#372,.F.) ;
#7851=ADVANCED_FACE('',(#1176),#373,.F.) ;
#7852=ADVANCED_FACE('',(#1177),#782,.F.) ;
#7853=ADVANCED_FACE('',(#1178),#783,.F.) ;
#7854=ADVANCED_FACE('',(#1179),#784,.F.) ;
#7855=ADVANCED_FACE('',(#1180),#785,.T.) ;
#7856=ADVANCED_FACE('',(#1181),#374,.F.) ;
#7857=ADVANCED_FACE('',(#1182),#375,.F.) ;
#7858=ADVANCED_FACE('',(#1183),#376,.F.) ;
#7859=ADVANCED_FACE('',(#1184),#786,.F.) ;
#7860=ADVANCED_FACE('',(#1185),#377,.F.) ;
#7861=ADVANCED_FACE('',(#1186),#378,.F.) ;
#7862=ADVANCED_FACE('',(#1187),#379,.F.) ;
#7863=ADVANCED_FACE('',(#1188),#380,.F.) ;
#7864=ADVANCED_FACE('',(#1189),#381,.F.) ;
#7865=ADVANCED_FACE('',(#1190),#382,.F.) ;
#7866=ADVANCED_FACE('',(#1191),#383,.F.) ;
#7867=ADVANCED_FACE('',(#1192),#384,.F.) ;
#7868=ADVANCED_FACE('',(#1193),#385,.F.) ;
#7869=ADVANCED_FACE('',(#1194),#386,.F.) ;
#7870=ADVANCED_FACE('',(#1195),#387,.F.) ;
#7871=ADVANCED_FACE('',(#1196),#388,.F.) ;
#7872=ADVANCED_FACE('',(#1197),#389,.F.) ;
#7873=ADVANCED_FACE('',(#1198),#390,.F.) ;
#7874=ADVANCED_FACE('',(#1199),#391,.F.) ;
#7875=ADVANCED_FACE('',(#1200),#392,.F.) ;
#7876=ADVANCED_FACE('',(#1201),#393,.F.) ;
#7877=ADVANCED_FACE('',(#1202),#394,.F.) ;
#7878=ADVANCED_FACE('',(#1203),#395,.F.) ;
#7879=ADVANCED_FACE('',(#1204),#396,.F.) ;
#7880=ADVANCED_FACE('',(#1205),#397,.F.) ;
#7881=ADVANCED_FACE('',(#1206),#398,.F.) ;
#7882=ADVANCED_FACE('',(#1207),#399,.F.) ;
#7883=ADVANCED_FACE('',(#1208),#400,.F.) ;
#7884=ADVANCED_FACE('',(#1209),#401,.F.) ;
#7885=ADVANCED_FACE('',(#1210),#402,.F.) ;
#7886=ADVANCED_FACE('',(#1211),#403,.F.) ;
#7887=ADVANCED_FACE('',(#1212),#404,.F.) ;
#7888=ADVANCED_FACE('',(#1213),#405,.F.) ;
#7889=ADVANCED_FACE('',(#1214),#787,.F.) ;
#7890=ADVANCED_FACE('',(#1215),#406,.F.) ;
#7891=ADVANCED_FACE('',(#1216),#788,.T.) ;
#7892=ADVANCED_FACE('',(#1217),#789,.F.) ;
#7893=ADVANCED_FACE('',(#1218),#790,.F.) ;
#7894=ADVANCED_FACE('',(#1219),#791,.F.) ;
#7895=ADVANCED_FACE('',(#1220),#792,.F.) ;
#7896=ADVANCED_FACE('',(#1221),#793,.F.) ;
#7897=ADVANCED_FACE('',(#1222),#794,.F.) ;
#7898=ADVANCED_FACE('',(#1223),#795,.F.) ;
#7899=ADVANCED_FACE('',(#1224),#796,.F.) ;
#7900=ADVANCED_FACE('',(#1225),#797,.F.) ;
#7901=ADVANCED_FACE('',(#1226),#407,.F.) ;
#7902=ADVANCED_FACE('',(#1227),#408,.F.) ;
#7903=ADVANCED_FACE('',(#1228),#798,.F.) ;
#7904=ADVANCED_FACE('',(#1229),#799,.F.) ;
#7905=ADVANCED_FACE('',(#1230),#800,.F.) ;
#7906=ADVANCED_FACE('',(#1231),#801,.F.) ;
#7907=ADVANCED_FACE('',(#1232),#802,.T.) ;
#7908=ADVANCED_FACE('',(#1233),#990,.T.) ;
#7909=ADVANCED_FACE('',(#1234,#700),#803,.F.) ;
#7910=ADVANCED_FACE('',(#1235,#701),#804,.F.) ;
#7911=ADVANCED_FACE('',(#1236),#991,.T.) ;
#7912=ADVANCED_FACE('',(#1237),#7721,.F.) ;
#7913=ADVANCED_FACE('',(#1238),#409,.T.) ;
#7914=ADVANCED_FACE('',(#1239),#316,.F.) ;
#7915=ADVANCED_FACE('',(#1240),#992,.F.) ;
#7916=ADVANCED_FACE('',(#1241),#7722,.F.) ;
#7917=ADVANCED_FACE('',(#1242),#410,.T.) ;
#7918=ADVANCED_FACE('',(#1243),#993,.F.) ;
#7919=ADVANCED_FACE('',(#1244),#7723,.F.) ;
#7920=ADVANCED_FACE('',(#1245),#411,.T.) ;
#7921=ADVANCED_FACE('',(#1246),#994,.F.) ;
#7922=ADVANCED_FACE('',(#1247),#7724,.F.) ;
#7923=ADVANCED_FACE('',(#1248),#412,.T.) ;
#7924=ADVANCED_FACE('',(#1249),#995,.F.) ;
#7925=ADVANCED_FACE('',(#1250,#702),#805,.T.) ;
#7926=ADVANCED_FACE('',(#1251,#703),#806,.T.) ;
#7927=ADVANCED_FACE('',(#1252,#704),#807,.T.) ;
#7928=ADVANCED_FACE('',(#1253,#705),#808,.T.) ;
#7929=ADVANCED_FACE('',(#1254),#996,.F.) ;
#7930=ADVANCED_FACE('',(#1255),#997,.F.) ;
#7931=ADVANCED_FACE('',(#1256),#998,.F.) ;
#7932=ADVANCED_FACE('',(#1257),#999,.F.) ;
#7933=ADVANCED_FACE('',(#1258),#1000,.F.) ;
#7934=ADVANCED_FACE('',(#1259),#1001,.F.) ;
#7935=ADVANCED_FACE('',(#1260),#1002,.F.) ;
#7936=ADVANCED_FACE('',(#1261),#1003,.F.) ;
#7937=ADVANCED_FACE('',(#1262,#706),#809,.T.) ;
#7938=ADVANCED_FACE('',(#1263),#1004,.F.) ;
#7939=ADVANCED_FACE('',(#1264),#1005,.F.) ;
#7940=ADVANCED_FACE('',(#1265),#1006,.F.) ;
#7941=ADVANCED_FACE('',(#1266),#1007,.F.) ;
#7942=ADVANCED_FACE('',(#1267,#707),#810,.T.) ;
#7943=ADVANCED_FACE('',(#1268),#1008,.T.) ;
#7944=ADVANCED_FACE('',(#1269,#708),#811,.F.) ;
#7945=ADVANCED_FACE('',(#1270),#1009,.F.) ;
#7946=ADVANCED_FACE('',(#1271,#709),#812,.F.) ;
#7947=ADVANCED_FACE('',(#1272),#1010,.F.) ;
#7948=ADVANCED_FACE('',(#1273,#710),#813,.F.) ;
#7949=ADVANCED_FACE('',(#1274),#1011,.F.) ;
#7950=ADVANCED_FACE('',(#1275,#711),#814,.F.) ;
#7951=ADVANCED_FACE('',(#1276),#1012,.F.) ;
#7952=ADVANCED_FACE('',(#1277,#712),#815,.T.) ;
#7953=ADVANCED_FACE('',(#1278),#1013,.F.) ;
#7954=ADVANCED_FACE('',(#1279,#713,#714,#715,#716,#717),#816,.T.) ;
#7955=ADVANCED_FACE('',(#1280),#7725,.T.) ;
#7956=ADVANCED_FACE('',(#1281),#1014,.T.) ;
#7957=ADVANCED_FACE('',(#1282),#7726,.T.) ;
#7958=ADVANCED_FACE('',(#1283),#7727,.T.) ;
#7959=ADVANCED_FACE('',(#1284,#718),#817,.T.) ;
#7960=ADVANCED_FACE('',(#1285),#1015,.F.) ;
#8179=CLOSED_SHELL('',(#7772,#7773,#7774,#7775,#7776,#7777,#7778,#7779,
#7780,#7781,#7782,#7783,#7784,#7785,#7786,#7787,#7788,#7789,#7790,#7791,
#7792,#7793,#7794,#7795,#7796,#7797,#7798,#7799,#7800,#7801,#7802,#7803,
#7804,#7805,#7806,#7807,#7808,#7809,#7810,#7811,#7812,#7813,#7814,#7815,
#7816,#7817,#7818,#7819,#7820,#7821,#7822,#7823,#7824,#7825,#7826,#7827,
#7828,#7829,#7830,#7831,#7832,#7833,#7834,#7835,#7836,#7837,#7838,#7839,
#7840,#7841,#7842,#7843,#7844,#7845,#7846,#7847,#7848,#7849,#7850,#7851,
#7852,#7853,#7854,#7855,#7856,#7857,#7858,#7859,#7860,#7861,#7862,#7863,
#7864,#7865,#7866,#7867,#7868,#7869,#7870,#7871,#7872,#7873,#7874,#7875,
#7876,#7877,#7878,#7879,#7880,#7881,#7882,#7883,#7884,#7885,#7886,#7887,
#7888,#7889,#7890,#7891,#7892,#7893,#7894,#7895,#7896,#7897,#7898,#7899,
#7900,#7901,#7902,#7903,#7904,#7905,#7906,#7907,#7908,#7909,#7910,#7911,
#7912,#7913,#7914,#7915,#7916,#7917,#7918,#7919,#7920,#7921,#7922,#7923,
#7924,#7925,#7926,#7927,#7928,#7929,#7930,#7931,#7932,#7933,#7934,#7935,
#7936,#7937,#7938,#7939,#7940,#7941,#7942,#7943,#7944,#7945,#7946,#7947,
#7948,#7949,#7950,#7951,#7952,#7953,#7954,#7955,#7956,#7957,#7958,#7959,
#7960)) ;
#8345=AXIS2_PLACEMENT_3D('',#11223,#9163,#9164) ;
#8346=AXIS2_PLACEMENT_3D('',#11757,#9192,#9193) ;
#8347=AXIS2_PLACEMENT_3D('',#11759,#9194,#9195) ;
#8348=AXIS2_PLACEMENT_3D('',#11779,#9198,#9199) ;
#8349=AXIS2_PLACEMENT_3D('',#11802,#9202,#9203) ;
#8350=AXIS2_PLACEMENT_3D('',#11804,#9204,#9205) ;
#8351=AXIS2_PLACEMENT_3D('',#11846,#9210,#9211) ;
#8352=AXIS2_PLACEMENT_3D('',#11871,#9216,#9217) ;
#8353=AXIS2_PLACEMENT_3D('',#11873,#9218,#9219) ;
#8354=AXIS2_PLACEMENT_3D('',#11877,#9222,#9223) ;
#8355=AXIS2_PLACEMENT_3D('',#11883,#9227,#9228) ;
#8356=AXIS2_PLACEMENT_3D('',#11884,#9229,#9230) ;
#8357=AXIS2_PLACEMENT_3D('',#11886,#9232,#9233) ;
#8358=AXIS2_PLACEMENT_3D('',#11887,#9234,#9235) ;
#8359=AXIS2_PLACEMENT_3D('',#11889,#9236,#9237) ;
#8360=AXIS2_PLACEMENT_3D('',#11892,#9239,#9240) ;
#8361=AXIS2_PLACEMENT_3D('',#11895,#9241,#9242) ;
#8362=AXIS2_PLACEMENT_3D('',#11899,#9244,#9245) ;
#8363=AXIS2_PLACEMENT_3D('',#11903,#9247,#9248) ;
#8364=AXIS2_PLACEMENT_3D('',#11957,#9249,#9250) ;
#8365=AXIS2_PLACEMENT_3D('',#11961,#9252,#9253) ;
#8366=AXIS2_PLACEMENT_3D('',#11965,#9255,#9256) ;
#8367=AXIS2_PLACEMENT_3D('',#11967,#9257,#9258) ;
#8368=AXIS2_PLACEMENT_3D('',#11970,#9260,#9261) ;
#8369=AXIS2_PLACEMENT_3D('',#11989,#9262,#9263) ;
#8370=AXIS2_PLACEMENT_3D('',#12156,#9264,#9265) ;
#8371=AXIS2_PLACEMENT_3D('',#12318,#9266,#9267) ;
#8372=AXIS2_PLACEMENT_3D('',#12322,#9269,#9270) ;
#8373=AXIS2_PLACEMENT_3D('',#12387,#9271,#9272) ;
#8374=AXIS2_PLACEMENT_3D('',#12391,#9274,#9275) ;
#8375=AXIS2_PLACEMENT_3D('',#12440,#9276,#9277) ;
#8376=AXIS2_PLACEMENT_3D('',#12444,#9279,#9280) ;
#8377=AXIS2_PLACEMENT_3D('',#12448,#9282,#9283) ;
#8378=AXIS2_PLACEMENT_3D('',#12502,#9284,#9285) ;
#8379=AXIS2_PLACEMENT_3D('',#12506,#9287,#9288) ;
#8380=AXIS2_PLACEMENT_3D('',#12510,#9290,#9291) ;
#8381=AXIS2_PLACEMENT_3D('',#12512,#9292,#9293) ;
#8382=AXIS2_PLACEMENT_3D('',#12515,#9295,#9296) ;
#8383=AXIS2_PLACEMENT_3D('',#12518,#9297,#9298) ;
#8384=AXIS2_PLACEMENT_3D('',#12522,#9300,#9301) ;
#8385=AXIS2_PLACEMENT_3D('',#12526,#9303,#9304) ;
#8386=AXIS2_PLACEMENT_3D('',#12530,#9306,#9307) ;
#8387=AXIS2_PLACEMENT_3D('',#12532,#9309,#9310) ;
#8388=AXIS2_PLACEMENT_3D('',#12538,#9314,#9315) ;
#8389=AXIS2_PLACEMENT_3D('',#12542,#9318,#9319) ;
#8390=AXIS2_PLACEMENT_3D('',#12546,#9322,#9323) ;
#8391=AXIS2_PLACEMENT_3D('',#12548,#9325,#9326) ;
#8392=AXIS2_PLACEMENT_3D('',#12549,#9327,#9328) ;
#8393=AXIS2_PLACEMENT_3D('',#12555,#9332,#9333) ;
#8394=AXIS2_PLACEMENT_3D('',#12559,#9336,#9337) ;
#8395=AXIS2_PLACEMENT_3D('',#12563,#9340,#9341) ;
#8396=AXIS2_PLACEMENT_3D('',#12565,#9343,#9344) ;
#8397=AXIS2_PLACEMENT_3D('',#12566,#9345,#9346) ;
#8398=AXIS2_PLACEMENT_3D('',#12572,#9350,#9351) ;
#8399=AXIS2_PLACEMENT_3D('',#12576,#9354,#9355) ;
#8400=AXIS2_PLACEMENT_3D('',#12580,#9358,#9359) ;
#8401=AXIS2_PLACEMENT_3D('',#12584,#9362,#9363) ;
#8402=AXIS2_PLACEMENT_3D('',#12588,#9366,#9367) ;
#8403=AXIS2_PLACEMENT_3D('',#12592,#9370,#9371) ;
#8404=AXIS2_PLACEMENT_3D('',#12596,#9374,#9375) ;
#8405=AXIS2_PLACEMENT_3D('',#12600,#9378,#9379) ;
#8406=AXIS2_PLACEMENT_3D('',#12626,#9384,#9385) ;
#8407=AXIS2_PLACEMENT_3D('',#12630,#9388,#9389) ;
#8408=AXIS2_PLACEMENT_3D('',#12634,#9392,#9393) ;
#8409=AXIS2_PLACEMENT_3D('',#12638,#9396,#9397) ;
#8410=AXIS2_PLACEMENT_3D('',#12640,#9399,#9400) ;
#8411=AXIS2_PLACEMENT_3D('',#12654,#9403,#9404) ;
#8412=AXIS2_PLACEMENT_3D('',#12658,#9407,#9408) ;
#8413=AXIS2_PLACEMENT_3D('',#12662,#9411,#9412) ;
#8414=AXIS2_PLACEMENT_3D('',#12776,#9425,#9426) ;
#8415=AXIS2_PLACEMENT_3D('',#12780,#9429,#9430) ;
#8416=AXIS2_PLACEMENT_3D('',#12784,#9433,#9434) ;
#8417=AXIS2_PLACEMENT_3D('',#12786,#9436,#9437) ;
#8418=AXIS2_PLACEMENT_3D('',#12822,#9442,#9443) ;
#8419=AXIS2_PLACEMENT_3D('',#13145,#9475,#9476) ;
#8420=AXIS2_PLACEMENT_3D('',#13158,#9479,#9480) ;
#8421=AXIS2_PLACEMENT_3D('',#13159,#9481,#9482) ;
#8422=AXIS2_PLACEMENT_3D('',#13165,#9486,#9487) ;
#8423=AXIS2_PLACEMENT_3D('',#13169,#9490,#9491) ;
#8424=AXIS2_PLACEMENT_3D('',#13173,#9494,#9495) ;
#8425=AXIS2_PLACEMENT_3D('',#13177,#9498,#9499) ;
#8426=AXIS2_PLACEMENT_3D('',#13181,#9502,#9503) ;
#8427=AXIS2_PLACEMENT_3D('',#13185,#9506,#9507) ;
#8428=AXIS2_PLACEMENT_3D('',#13189,#9510,#9511) ;
#8429=AXIS2_PLACEMENT_3D('',#13193,#9514,#9515) ;
#8430=AXIS2_PLACEMENT_3D('',#13219,#9520,#9521) ;
#8431=AXIS2_PLACEMENT_3D('',#13223,#9524,#9525) ;
#8432=AXIS2_PLACEMENT_3D('',#13227,#9528,#9529) ;
#8433=AXIS2_PLACEMENT_3D('',#13231,#9532,#9533) ;
#8434=AXIS2_PLACEMENT_3D('',#13233,#9535,#9536) ;
#8435=AXIS2_PLACEMENT_3D('',#13234,#9537,#9538) ;
#8436=AXIS2_PLACEMENT_3D('',#13236,#9539,#9540) ;
#8437=AXIS2_PLACEMENT_3D('',#13239,#9542,#9543) ;
#8438=AXIS2_PLACEMENT_3D('',#13240,#9544,#9545) ;
#8439=AXIS2_PLACEMENT_3D('',#13242,#9546,#9547) ;
#8440=AXIS2_PLACEMENT_3D('',#13243,#9548,#9549) ;
#8441=AXIS2_PLACEMENT_3D('',#13244,#9550,#9551) ;
#8442=AXIS2_PLACEMENT_3D('',#13245,#9552,#9553) ;
#8443=AXIS2_PLACEMENT_3D('',#13250,#9555,#9556) ;
#8444=AXIS2_PLACEMENT_3D('',#13252,#9557,#9558) ;
#8445=AXIS2_PLACEMENT_3D('',#13255,#9560,#9561) ;
#8446=AXIS2_PLACEMENT_3D('',#13292,#9562,#9563) ;
#8447=AXIS2_PLACEMENT_3D('',#13294,#9564,#9565) ;
#8448=AXIS2_PLACEMENT_3D('',#13303,#9566,#9567) ;
#8449=AXIS2_PLACEMENT_3D('',#13312,#9568,#9569) ;
#8450=AXIS2_PLACEMENT_3D('',#13321,#9570,#9571) ;
#8451=AXIS2_PLACEMENT_3D('',#13323,#9572,#9573) ;
#8452=AXIS2_PLACEMENT_3D('',#13325,#9574,#9575) ;
#8453=AXIS2_PLACEMENT_3D('',#13326,#9576,#9577) ;
#8454=AXIS2_PLACEMENT_3D('',#13327,#9578,#9579) ;
#8455=AXIS2_PLACEMENT_3D('',#13328,#9580,#9581) ;
#8456=AXIS2_PLACEMENT_3D('',#13331,#9583,#9584) ;
#8457=AXIS2_PLACEMENT_3D('',#13332,#9585,#9586) ;
#8458=AXIS2_PLACEMENT_3D('',#13336,#9588,#9589) ;
#8459=AXIS2_PLACEMENT_3D('',#13338,#9590,#9591) ;
#8460=AXIS2_PLACEMENT_3D('',#13340,#9593,#9594) ;
#8461=AXIS2_PLACEMENT_3D('',#13371,#9595,#9596) ;
#8462=AXIS2_PLACEMENT_3D('',#13374,#9598,#9599) ;
#8463=AXIS2_PLACEMENT_3D('',#13375,#9600,#9601) ;
#8464=AXIS2_PLACEMENT_3D('',#13379,#9603,#9604) ;
#8465=AXIS2_PLACEMENT_3D('',#13381,#9605,#9606) ;
#8466=AXIS2_PLACEMENT_3D('',#13383,#9608,#9609) ;
#8467=AXIS2_PLACEMENT_3D('',#13414,#9610,#9611) ;
#8468=AXIS2_PLACEMENT_3D('',#13417,#9613,#9614) ;
#8469=AXIS2_PLACEMENT_3D('',#13418,#9615,#9616) ;
#8470=AXIS2_PLACEMENT_3D('',#13422,#9618,#9619) ;
#8471=AXIS2_PLACEMENT_3D('',#13424,#9620,#9621) ;
#8472=AXIS2_PLACEMENT_3D('',#13426,#9623,#9624) ;
#8473=AXIS2_PLACEMENT_3D('',#13457,#9625,#9626) ;
#8474=AXIS2_PLACEMENT_3D('',#13460,#9628,#9629) ;
#8475=AXIS2_PLACEMENT_3D('',#13461,#9630,#9631) ;
#8476=AXIS2_PLACEMENT_3D('',#13463,#9632,#9633) ;
#8477=AXIS2_PLACEMENT_3D('',#13464,#9634,#9635) ;
#8478=AXIS2_PLACEMENT_3D('',#13466,#9636,#9637) ;
#8479=AXIS2_PLACEMENT_3D('',#13467,#9638,#9639) ;
#8480=AXIS2_PLACEMENT_3D('',#13469,#9640,#9641) ;
#8481=AXIS2_PLACEMENT_3D('',#13470,#9642,#9643) ;
#8482=AXIS2_PLACEMENT_3D('',#13472,#9644,#9645) ;
#8483=AXIS2_PLACEMENT_3D('',#13473,#9646,#9647) ;
#8484=AXIS2_PLACEMENT_3D('',#13476,#9649,#9650) ;
#8485=AXIS2_PLACEMENT_3D('',#13477,#9651,#9652) ;
#8486=AXIS2_PLACEMENT_3D('',#13480,#9654,#9655) ;
#8487=AXIS2_PLACEMENT_3D('',#13481,#9656,#9657) ;
#8488=AXIS2_PLACEMENT_3D('',#13484,#9659,#9660) ;
#8489=AXIS2_PLACEMENT_3D('',#13485,#9661,#9662) ;
#8490=AXIS2_PLACEMENT_3D('',#13488,#9664,#9665) ;
#8491=AXIS2_PLACEMENT_3D('',#13489,#9666,#9667) ;
#8492=AXIS2_PLACEMENT_3D('',#13494,#9669,#9670) ;
#8493=AXIS2_PLACEMENT_3D('',#13497,#9672,#9673) ;
#8494=AXIS2_PLACEMENT_3D('',#13498,#9674,#9675) ;
#8495=AXIS2_PLACEMENT_3D('',#13503,#9677,#9678) ;
#8496=AXIS2_PLACEMENT_3D('',#13506,#9680,#9681) ;
#8497=AXIS2_PLACEMENT_3D('',#13507,#9682,#9683) ;
#8498=AXIS2_PLACEMENT_3D('',#13512,#9685,#9686) ;
#8499=AXIS2_PLACEMENT_3D('',#13515,#9688,#9689) ;
#8500=AXIS2_PLACEMENT_3D('',#13516,#9690,#9691) ;
#8501=AXIS2_PLACEMENT_3D('',#13521,#9693,#9694) ;
#8502=AXIS2_PLACEMENT_3D('',#13524,#9696,#9697) ;
#8503=AXIS2_PLACEMENT_3D('',#13525,#9698,#9699) ;
#8504=AXIS2_PLACEMENT_3D('',#13527,#9700,#9701) ;
#8505=AXIS2_PLACEMENT_3D('',#13528,#9702,#9703) ;
#8506=AXIS2_PLACEMENT_3D('',#13529,#9704,#9705) ;
#8507=AXIS2_PLACEMENT_3D('',#13530,#9706,#9707) ;
#8508=AXIS2_PLACEMENT_3D('',#13531,#9708,#9709) ;
#8509=AXIS2_PLACEMENT_3D('',#13532,#9710,#9711) ;
#8510=AXIS2_PLACEMENT_3D('',#13533,#9712,#9713) ;
#8511=AXIS2_PLACEMENT_3D('',#13534,#9714,#9715) ;
#8512=AXIS2_PLACEMENT_3D('',#13535,#9716,#9717) ;
#8513=AXIS2_PLACEMENT_3D('',#13536,#9718,#9719) ;
#8514=AXIS2_PLACEMENT_3D('',#13537,#9720,#9721) ;
#8515=AXIS2_PLACEMENT_3D('',#13538,#9722,#9723) ;
#8516=AXIS2_PLACEMENT_3D('',#13539,#9724,#9725) ;
#8517=AXIS2_PLACEMENT_3D('',#13540,#9726,#9727) ;
#8518=AXIS2_PLACEMENT_3D('',#13542,#9728,#9729) ;
#8519=AXIS2_PLACEMENT_3D('',#13543,#9730,#9731) ;
#8520=AXIS2_PLACEMENT_3D('',#13545,#9733,#9734) ;
#8521=AXIS2_PLACEMENT_3D('',#13547,#9735,#9736) ;
#8522=AXIS2_PLACEMENT_3D('',#13549,#9737,#9738) ;
#8523=AXIS2_PLACEMENT_3D('',#13550,#9739,#9740) ;
#8524=AXIS2_PLACEMENT_3D('',#13553,#9742,#9743) ;
#8525=AXIS2_PLACEMENT_3D('',#13554,#9744,#9745) ;
#8526=AXIS2_PLACEMENT_3D('',#13556,#9746,#9747) ;
#8527=AXIS2_PLACEMENT_3D('',#13557,#9748,#9749) ;
#8528=AXIS2_PLACEMENT_3D('',#13559,#9750,#9751) ;
#8529=AXIS2_PLACEMENT_3D('',#13561,#9753,#9754) ;
#8530=AXIS2_PLACEMENT_3D('',#13563,#9755,#9756) ;
#8531=AXIS2_PLACEMENT_3D('',#13565,#9757,#9758) ;
#8532=AXIS2_PLACEMENT_3D('',#13566,#9759,#9760) ;
#8533=AXIS2_PLACEMENT_3D('',#13569,#9762,#9763) ;
#8534=AXIS2_PLACEMENT_3D('',#13570,#9764,#9765) ;
#8535=AXIS2_PLACEMENT_3D('',#13572,#9766,#9767) ;
#8536=AXIS2_PLACEMENT_3D('',#13573,#9768,#9769) ;
#8537=AXIS2_PLACEMENT_3D('',#13575,#9770,#9771) ;
#8538=AXIS2_PLACEMENT_3D('',#13577,#9773,#9774) ;
#8539=AXIS2_PLACEMENT_3D('',#13578,#9775,#9776) ;
#8540=AXIS2_PLACEMENT_3D('',#13581,#9778,#9779) ;
#8541=AXIS2_PLACEMENT_3D('',#13582,#9780,#9781) ;
#8542=AXIS2_PLACEMENT_3D('',#13584,#9782,#9783) ;
#8543=AXIS2_PLACEMENT_3D('',#13585,#9784,#9785) ;
#8544=AXIS2_PLACEMENT_3D('',#13587,#9786,#9787) ;
#8545=AXIS2_PLACEMENT_3D('',#13589,#9789,#9790) ;
#8546=AXIS2_PLACEMENT_3D('',#13591,#9791,#9792) ;
#8547=AXIS2_PLACEMENT_3D('',#13593,#9794,#9795) ;
#8548=AXIS2_PLACEMENT_3D('',#13595,#9797,#9798) ;
#8549=AXIS2_PLACEMENT_3D('',#13597,#9799,#9800) ;
#8550=AXIS2_PLACEMENT_3D('',#13599,#9802,#9803) ;
#8551=AXIS2_PLACEMENT_3D('',#13600,#9804,#9805) ;
#9163=DIRECTION('axis',(0.,0.,1.)) ;
#9164=DIRECTION('refdir',(1.,0.,0.)) ;
#9165=DIRECTION('',(0.,-1.,0.)) ;
#9166=DIRECTION('',(0.,-1.,0.)) ;
#9167=DIRECTION('',(0.,-1.,0.)) ;
#9168=DIRECTION('',(0.,-1.,0.)) ;
#9169=DIRECTION('',(0.,-1.,0.)) ;
#9170=DIRECTION('',(0.,-1.,0.)) ;
#9171=DIRECTION('',(0.,-1.,0.)) ;
#9172=DIRECTION('',(0.,-1.,0.)) ;
#9173=DIRECTION('',(0.,-1.,0.)) ;
#9174=DIRECTION('',(0.,-1.,0.)) ;
#9175=DIRECTION('',(0.,-1.,0.)) ;
#9176=DIRECTION('',(0.,-1.,0.)) ;
#9177=DIRECTION('',(0.,-1.,0.)) ;
#9178=DIRECTION('',(0.,-1.,0.)) ;
#9179=DIRECTION('',(0.,-1.,0.)) ;
#9180=DIRECTION('',(0.,-1.,0.)) ;
#9181=DIRECTION('',(0.,-1.,0.)) ;
#9182=DIRECTION('',(0.,-1.,0.)) ;
#9183=DIRECTION('',(0.,-1.,0.)) ;
#9184=DIRECTION('',(0.,-1.,0.)) ;
#9185=DIRECTION('',(0.,-1.,0.)) ;
#9186=DIRECTION('',(0.,-1.,0.)) ;
#9187=DIRECTION('',(0.,-1.,0.)) ;
#9188=DIRECTION('',(0.,-1.,0.)) ;
#9189=DIRECTION('',(0.,-1.,0.)) ;
#9190=DIRECTION('',(0.,-1.,0.)) ;
#9191=DIRECTION('',(0.,-1.,0.)) ;
#9192=DIRECTION('center_axis',(0.0779742589964975,0.,0.996955372588938)) ;
#9193=DIRECTION('ref_axis',(-0.996955372588938,0.,0.0779742589964975)) ;
#9194=DIRECTION('center_axis',(0.0779742589964975,0.,0.996955372588938)) ;
#9195=DIRECTION('ref_axis',(-0.996955372588938,0.,0.0779742589964975)) ;
#9196=DIRECTION('',(0.,-1.,0.)) ;
#9197=DIRECTION('',(-0.996955372588938,0.,0.0779742589964975)) ;
#9198=DIRECTION('center_axis',(0.,1.,0.)) ;
#9199=DIRECTION('ref_axis',(1.,0.,0.)) ;
#9200=DIRECTION('',(0.,-1.,0.)) ;
#9201=DIRECTION('',(0.,-1.,0.)) ;
#9202=DIRECTION('center_axis',(-1.,0.,0.)) ;
#9203=DIRECTION('ref_axis',(0.,0.,-1.)) ;
#9204=DIRECTION('center_axis',(-1.,0.,0.)) ;
#9205=DIRECTION('ref_axis',(0.,1.,0.)) ;
#9206=DIRECTION('',(0.,0.,-1.)) ;
#9207=DIRECTION('',(0.,-1.,0.)) ;
#9208=DIRECTION('',(0.,-1.,0.)) ;
#9209=DIRECTION('',(0.,-1.,0.)) ;
#9210=DIRECTION('center_axis',(0.,0.,-1.)) ;
#9211=DIRECTION('ref_axis',(1.,0.,0.)) ;
#9212=DIRECTION('',(1.,0.,0.)) ;
#9213=DIRECTION('',(1.,0.,0.)) ;
#9214=DIRECTION('',(0.,-1.,0.)) ;
#9215=DIRECTION('',(0.,-1.,0.)) ;
#9216=DIRECTION('center_axis',(-1.,0.,0.)) ;
#9217=DIRECTION('ref_axis',(0.,0.,-1.)) ;
#9218=DIRECTION('center_axis',(-1.,0.,0.)) ;
#9219=DIRECTION('ref_axis',(0.,1.,0.)) ;
#9220=DIRECTION('',(0.,-1.,0.)) ;
#9221=DIRECTION('',(0.,0.,-1.)) ;
#9222=DIRECTION('center_axis',(0.,0.,1.)) ;
#9223=DIRECTION('ref_axis',(-1.,0.,0.)) ;
#9224=DIRECTION('',(-1.,0.,0.)) ;
#9225=DIRECTION('',(0.,-1.,0.)) ;
#9226=DIRECTION('',(-1.,0.,0.)) ;
#9227=DIRECTION('center_axis',(1.,0.,0.)) ;
#9228=DIRECTION('ref_axis',(0.,0.,1.)) ;
#9229=DIRECTION('center_axis',(1.,0.,0.)) ;
#9230=DIRECTION('ref_axis',(0.,1.,0.)) ;
#9231=DIRECTION('',(0.,0.,1.)) ;
#9232=DIRECTION('center_axis',(0.,1.,0.)) ;
#9233=DIRECTION('ref_axis',(1.,0.,0.)) ;
#9234=DIRECTION('center_axis',(1.,0.,0.)) ;
#9235=DIRECTION('ref_axis',(0.,1.,0.)) ;
#9236=DIRECTION('center_axis',(1.,0.,0.)) ;
#9237=DIRECTION('ref_axis',(0.,0.,-1.)) ;
#9238=DIRECTION('',(-1.,0.,0.)) ;
#9239=DIRECTION('center_axis',(1.,0.,0.)) ;
#9240=DIRECTION('ref_axis',(0.,1.,0.)) ;
#9241=DIRECTION('center_axis',(1.,0.,0.)) ;
#9242=DIRECTION('ref_axis',(0.,1.,0.)) ;
#9243=DIRECTION('',(-1.,0.,0.)) ;
#9244=DIRECTION('center_axis',(-1.,0.,0.)) ;
#9245=DIRECTION('ref_axis',(0.,1.,0.)) ;
#9246=DIRECTION('',(1.,0.,0.)) ;
#9247=DIRECTION('center_axis',(0.948408846174048,0.,-0.317049933762509)) ;
#9248=DIRECTION('ref_axis',(0.317049933762509,0.,0.948408846174048)) ;
#9249=DIRECTION('center_axis',(-0.945579694085495,0.,-0.325390599331299)) ;
#9250=DIRECTION('ref_axis',(-0.325390599331299,0.,0.945579694085495)) ;
#9251=DIRECTION('',(1.,0.,0.)) ;
#9252=DIRECTION('center_axis',(1.,0.,0.)) ;
#9253=DIRECTION('ref_axis',(0.,1.,0.)) ;
#9254=DIRECTION('',(-1.,0.,0.)) ;
#9255=DIRECTION('center_axis',(-1.,0.,0.)) ;
#9256=DIRECTION('ref_axis',(0.,1.,0.)) ;
#9257=DIRECTION('center_axis',(0.944683590425841,0.,0.327983100144111)) ;
#9258=DIRECTION('ref_axis',(-0.327983100144111,0.,0.944683590425841)) ;
#9259=DIRECTION('',(-1.,0.,0.)) ;
#9260=DIRECTION('center_axis',(-0.946846702516136,0.,0.321685128556358)) ;
#9261=DIRECTION('ref_axis',(0.321685128556358,0.,0.946846702516135)) ;
#9262=DIRECTION('center_axis',(-0.0870991451328652,0.,-0.996199648121361)) ;
#9263=DIRECTION('ref_axis',(-0.996199648121361,0.,0.0870991451328652)) ;
#9264=DIRECTION('center_axis',(0.0750566132645402,0.,0.997179274155484)) ;
#9265=DIRECTION('ref_axis',(-0.997179274155484,0.,0.0750566132645402)) ;
#9266=DIRECTION('center_axis',(-1.,0.,0.)) ;
#9267=DIRECTION('ref_axis',(0.,1.,0.)) ;
#9268=DIRECTION('',(1.,0.,0.)) ;
#9269=DIRECTION('center_axis',(1.,0.,0.)) ;
#9270=DIRECTION('ref_axis',(0.,1.,0.)) ;
#9271=DIRECTION('center_axis',(-1.,0.,0.)) ;
#9272=DIRECTION('ref_axis',(0.,1.,0.)) ;
#9273=DIRECTION('',(1.,0.,0.)) ;
#9274=DIRECTION('center_axis',(1.,0.,0.)) ;
#9275=DIRECTION('ref_axis',(0.,1.,0.)) ;
#9276=DIRECTION('center_axis',(1.,0.,0.)) ;
#9277=DIRECTION('ref_axis',(0.,1.,0.)) ;
#9278=DIRECTION('',(-1.,0.,0.)) ;
#9279=DIRECTION('center_axis',(-1.,0.,0.)) ;
#9280=DIRECTION('ref_axis',(0.,1.,0.)) ;
#9281=DIRECTION('',(1.,0.,0.)) ;
#9282=DIRECTION('center_axis',(0.948408859814315,0.,-0.317049892959627)) ;
#9283=DIRECTION('ref_axis',(0.317049892959627,0.,0.948408859814315)) ;
#9284=DIRECTION('center_axis',(-0.945579694085495,0.,-0.325390599331299)) ;
#9285=DIRECTION('ref_axis',(-0.325390599331299,0.,0.945579694085495)) ;
#9286=DIRECTION('',(1.,0.,0.)) ;
#9287=DIRECTION('center_axis',(1.,0.,0.)) ;
#9288=DIRECTION('ref_axis',(0.,1.,0.)) ;
#9289=DIRECTION('',(-1.,0.,0.)) ;
#9290=DIRECTION('center_axis',(-1.,0.,0.)) ;
#9291=DIRECTION('ref_axis',(0.,1.,0.)) ;
#9292=DIRECTION('center_axis',(0.944683566738785,0.,0.327983168369488)) ;
#9293=DIRECTION('ref_axis',(-0.327983168369488,0.,0.944683566738785)) ;
#9294=DIRECTION('',(-1.,0.,0.)) ;
#9295=DIRECTION('center_axis',(-0.946846725462142,0.,0.321685061017167)) ;
#9296=DIRECTION('ref_axis',(0.321685061017167,0.,0.946846725462142)) ;
#9297=DIRECTION('center_axis',(1.,0.,0.)) ;
#9298=DIRECTION('ref_axis',(0.,1.,0.)) ;
#9299=DIRECTION('',(-1.,0.,0.)) ;
#9300=DIRECTION('center_axis',(-1.,0.,0.)) ;
#9301=DIRECTION('ref_axis',(0.,1.,0.)) ;
#9302=DIRECTION('',(1.,0.,0.)) ;
#9303=DIRECTION('center_axis',(1.,0.,0.)) ;
#9304=DIRECTION('ref_axis',(0.,1.,0.)) ;
#9305=DIRECTION('',(-1.,0.,0.)) ;
#9306=DIRECTION('center_axis',(-1.,0.,0.)) ;
#9307=DIRECTION('ref_axis',(0.,1.,0.)) ;
#9308=DIRECTION('',(1.,0.,0.)) ;
#9309=DIRECTION('center_axis',(-1.,0.,0.)) ;
#9310=DIRECTION('ref_axis',(0.,0.,-1.)) ;
#9311=DIRECTION('',(0.,-1.,0.)) ;
#9312=DIRECTION('',(0.,0.,-1.)) ;
#9313=DIRECTION('',(0.,-1.,0.)) ;
#9314=DIRECTION('center_axis',(0.,0.,-1.)) ;
#9315=DIRECTION('ref_axis',(1.,0.,0.)) ;
#9316=DIRECTION('',(1.,0.,0.)) ;
#9317=DIRECTION('',(0.,-1.,0.)) ;
#9318=DIRECTION('center_axis',(1.,0.,0.)) ;
#9319=DIRECTION('ref_axis',(0.,0.,1.)) ;
#9320=DIRECTION('',(0.,0.,1.)) ;
#9321=DIRECTION('',(0.,-1.,0.)) ;
#9322=DIRECTION('center_axis',(0.,0.,1.)) ;
#9323=DIRECTION('ref_axis',(-1.,0.,0.)) ;
#9324=DIRECTION('',(-1.,0.,0.)) ;
#9325=DIRECTION('center_axis',(0.,-1.,0.)) ;
#9326=DIRECTION('ref_axis',(0.,0.,-1.)) ;
#9327=DIRECTION('center_axis',(-1.,0.,0.)) ;
#9328=DIRECTION('ref_axis',(0.,0.,-1.)) ;
#9329=DIRECTION('',(0.,-1.,0.)) ;
#9330=DIRECTION('',(0.,0.,-1.)) ;
#9331=DIRECTION('',(0.,-1.,0.)) ;
#9332=DIRECTION('center_axis',(0.,0.,-1.)) ;
#9333=DIRECTION('ref_axis',(1.,0.,0.)) ;
#9334=DIRECTION('',(1.,0.,0.)) ;
#9335=DIRECTION('',(0.,-1.,0.)) ;
#9336=DIRECTION('center_axis',(1.,0.,0.)) ;
#9337=DIRECTION('ref_axis',(0.,0.,1.)) ;
#9338=DIRECTION('',(0.,0.,1.)) ;
#9339=DIRECTION('',(0.,-1.,0.)) ;
#9340=DIRECTION('center_axis',(0.,0.,1.)) ;
#9341=DIRECTION('ref_axis',(-1.,0.,0.)) ;
#9342=DIRECTION('',(-1.,0.,0.)) ;
#9343=DIRECTION('center_axis',(0.,-1.,0.)) ;
#9344=DIRECTION('ref_axis',(0.,0.,-1.)) ;
#9345=DIRECTION('center_axis',(0.,0.,-1.)) ;
#9346=DIRECTION('ref_axis',(1.,0.,0.)) ;
#9347=DIRECTION('',(0.,-1.,0.)) ;
#9348=DIRECTION('',(1.,0.,0.)) ;
#9349=DIRECTION('',(0.,-1.,0.)) ;
#9350=DIRECTION('center_axis',(1.,0.,0.)) ;
#9351=DIRECTION('ref_axis',(0.,0.,1.)) ;
#9352=DIRECTION('',(0.,0.,1.)) ;
#9353=DIRECTION('',(0.,-1.,0.)) ;
#9354=DIRECTION('center_axis',(0.,0.,1.)) ;
#9355=DIRECTION('ref_axis',(-1.,0.,0.)) ;
#9356=DIRECTION('',(-1.,0.,0.)) ;
#9357=DIRECTION('',(0.,-1.,0.)) ;
#9358=DIRECTION('center_axis',(-1.,0.,0.)) ;
#9359=DIRECTION('ref_axis',(0.,0.,-1.)) ;
#9360=DIRECTION('',(0.,0.,-1.)) ;
#9361=DIRECTION('',(0.,-1.,0.)) ;
#9362=DIRECTION('center_axis',(0.944683566738785,0.,0.327983168369488)) ;
#9363=DIRECTION('ref_axis',(-0.327983168369488,0.,0.944683566738785)) ;
#9364=DIRECTION('',(-0.327983168369488,0.,0.944683566738785)) ;
#9365=DIRECTION('',(0.,-1.,0.)) ;
#9366=DIRECTION('center_axis',(0.,0.,1.)) ;
#9367=DIRECTION('ref_axis',(-1.,0.,0.)) ;
#9368=DIRECTION('',(-1.,0.,0.)) ;
#9369=DIRECTION('',(0.,-1.,0.)) ;
#9370=DIRECTION('center_axis',(-0.946846725462142,0.,0.321685061017167)) ;
#9371=DIRECTION('ref_axis',(-0.321685061017167,0.,-0.946846725462142)) ;
#9372=DIRECTION('',(-0.321685061017167,0.,-0.946846725462142)) ;
#9373=DIRECTION('',(0.,-1.,0.)) ;
#9374=DIRECTION('center_axis',(1.,0.,0.)) ;
#9375=DIRECTION('ref_axis',(0.,0.,1.)) ;
#9376=DIRECTION('',(0.,0.,1.)) ;
#9377=DIRECTION('',(0.,-1.,0.)) ;
#9378=DIRECTION('center_axis',(-0.945579694085495,0.,-0.325390599331299)) ;
#9379=DIRECTION('ref_axis',(0.325390599331299,0.,-0.945579694085495)) ;
#9380=DIRECTION('',(0.,-1.,0.)) ;
#9381=DIRECTION('',(0.325390599331299,0.,-0.945579694085495)) ;
#9382=DIRECTION('',(0.,-1.,0.)) ;
#9383=DIRECTION('',(0.,-1.,0.)) ;
#9384=DIRECTION('center_axis',(0.948408859814315,0.,-0.317049892959627)) ;
#9385=DIRECTION('ref_axis',(0.317049892959627,0.,0.948408859814315)) ;
#9386=DIRECTION('',(0.,-1.,0.)) ;
#9387=DIRECTION('',(0.317049892959627,0.,0.948408859814315)) ;
#9388=DIRECTION('center_axis',(0.,0.,-1.)) ;
#9389=DIRECTION('ref_axis',(1.,0.,0.)) ;
#9390=DIRECTION('',(0.,-1.,0.)) ;
#9391=DIRECTION('',(1.,0.,0.)) ;
#9392=DIRECTION('center_axis',(-1.,0.,0.)) ;
#9393=DIRECTION('ref_axis',(0.,0.,-1.)) ;
#9394=DIRECTION('',(0.,-1.,0.)) ;
#9395=DIRECTION('',(0.,0.,-1.)) ;
#9396=DIRECTION('center_axis',(0.,0.,1.)) ;
#9397=DIRECTION('ref_axis',(-1.,0.,0.)) ;
#9398=DIRECTION('',(-1.,0.,0.)) ;
#9399=DIRECTION('center_axis',(0.,1.,0.)) ;
#9400=DIRECTION('ref_axis',(1.,0.,0.)) ;
#9401=DIRECTION('',(0.,-1.,0.)) ;
#9402=DIRECTION('',(0.,-1.,0.)) ;
#9403=DIRECTION('center_axis',(-1.,0.,0.)) ;
#9404=DIRECTION('ref_axis',(0.,0.,-1.)) ;
#9405=DIRECTION('',(0.,0.,-1.)) ;
#9406=DIRECTION('',(0.,-1.,0.)) ;
#9407=DIRECTION('center_axis',(0.,0.,-1.)) ;
#9408=DIRECTION('ref_axis',(1.,0.,0.)) ;
#9409=DIRECTION('',(1.,0.,0.)) ;
#9410=DIRECTION('',(0.,-1.,0.)) ;
#9411=DIRECTION('center_axis',(1.,0.,0.)) ;
#9412=DIRECTION('ref_axis',(0.,0.,1.)) ;
#9413=DIRECTION('',(0.,0.,1.)) ;
#9414=DIRECTION('',(0.,-1.,0.)) ;
#9415=DIRECTION('',(0.,-1.,0.)) ;
#9416=DIRECTION('',(0.,-1.,0.)) ;
#9417=DIRECTION('',(0.,-1.,0.)) ;
#9418=DIRECTION('',(0.,-1.,0.)) ;
#9419=DIRECTION('',(0.,-1.,0.)) ;
#9420=DIRECTION('',(0.,-1.,0.)) ;
#9421=DIRECTION('',(0.,-1.,0.)) ;
#9422=DIRECTION('',(0.,-1.,0.)) ;
#9423=DIRECTION('',(0.,-1.,0.)) ;
#9424=DIRECTION('',(0.,-1.,0.)) ;
#9425=DIRECTION('center_axis',(1.,0.,0.)) ;
#9426=DIRECTION('ref_axis',(0.,0.,1.)) ;
#9427=DIRECTION('',(0.,-1.,0.)) ;
#9428=DIRECTION('',(0.,0.,1.)) ;
#9429=DIRECTION('center_axis',(0.,0.,-1.)) ;
#9430=DIRECTION('ref_axis',(1.,0.,0.)) ;
#9431=DIRECTION('',(0.,-1.,0.)) ;
#9432=DIRECTION('',(1.,0.,0.)) ;
#9433=DIRECTION('center_axis',(-1.,0.,0.)) ;
#9434=DIRECTION('ref_axis',(0.,0.,-1.)) ;
#9435=DIRECTION('',(0.,0.,-1.)) ;
#9436=DIRECTION('center_axis',(0.,1.,0.)) ;
#9437=DIRECTION('ref_axis',(1.,0.,0.)) ;
#9438=DIRECTION('',(0.,-1.,0.)) ;
#9439=DIRECTION('',(0.,-1.,0.)) ;
#9440=DIRECTION('',(0.,-1.,0.)) ;
#9441=DIRECTION('',(0.,-1.,0.)) ;
#9442=DIRECTION('center_axis',(0.0750566132645402,0.,0.997179274155484)) ;
#9443=DIRECTION('ref_axis',(-0.997179274155484,0.,0.0750566132645402)) ;
#9444=DIRECTION('',(-0.997179274155484,0.,0.0750566132645402)) ;
#9445=DIRECTION('',(0.,-1.,0.)) ;
#9446=DIRECTION('',(0.,-1.,0.)) ;
#9447=DIRECTION('',(0.,-1.,0.)) ;
#9448=DIRECTION('',(0.,-1.,0.)) ;
#9449=DIRECTION('',(0.,-1.,0.)) ;
#9450=DIRECTION('',(0.,-1.,0.)) ;
#9451=DIRECTION('',(0.,-1.,0.)) ;
#9452=DIRECTION('',(0.,-1.,0.)) ;
#9453=DIRECTION('',(0.,-1.,0.)) ;
#9454=DIRECTION('',(0.,-1.,0.)) ;
#9455=DIRECTION('',(0.,-1.,0.)) ;
#9456=DIRECTION('',(0.,-1.,0.)) ;
#9457=DIRECTION('',(0.,-1.,0.)) ;
#9458=DIRECTION('',(0.,-1.,0.)) ;
#9459=DIRECTION('',(0.,-1.,0.)) ;
#9460=DIRECTION('',(0.,-1.,0.)) ;
#9461=DIRECTION('',(0.,-1.,0.)) ;
#9462=DIRECTION('',(0.,-1.,0.)) ;
#9463=DIRECTION('',(0.,-1.,0.)) ;
#9464=DIRECTION('',(0.,-1.,0.)) ;
#9465=DIRECTION('',(0.,-1.,0.)) ;
#9466=DIRECTION('',(0.,-1.,0.)) ;
#9467=DIRECTION('',(0.,-1.,0.)) ;
#9468=DIRECTION('',(0.,-1.,0.)) ;
#9469=DIRECTION('',(0.,-1.,0.)) ;
#9470=DIRECTION('',(0.,-1.,0.)) ;
#9471=DIRECTION('',(0.,-1.,0.)) ;
#9472=DIRECTION('',(0.,-1.,0.)) ;
#9473=DIRECTION('',(0.,-1.,0.)) ;
#9474=DIRECTION('',(0.,-1.,0.)) ;
#9475=DIRECTION('center_axis',(-0.0870991451328652,0.,-0.996199648121361)) ;
#9476=DIRECTION('ref_axis',(0.996199648121361,0.,-0.0870991451328652)) ;
#9477=DIRECTION('',(0.,-1.,0.)) ;
#9478=DIRECTION('',(0.996199648121361,0.,-0.0870991451328652)) ;
#9479=DIRECTION('center_axis',(0.,1.,0.)) ;
#9480=DIRECTION('ref_axis',(1.,0.,0.)) ;
#9481=DIRECTION('center_axis',(0.,0.,-1.)) ;
#9482=DIRECTION('ref_axis',(1.,0.,0.)) ;
#9483=DIRECTION('',(0.,-1.,0.)) ;
#9484=DIRECTION('',(1.,0.,0.)) ;
#9485=DIRECTION('',(0.,-1.,0.)) ;
#9486=DIRECTION('center_axis',(1.,0.,0.)) ;
#9487=DIRECTION('ref_axis',(0.,0.,1.)) ;
#9488=DIRECTION('',(0.,0.,1.)) ;
#9489=DIRECTION('',(0.,-1.,0.)) ;
#9490=DIRECTION('center_axis',(0.,0.,1.)) ;
#9491=DIRECTION('ref_axis',(-1.,0.,0.)) ;
#9492=DIRECTION('',(-1.,0.,0.)) ;
#9493=DIRECTION('',(0.,-1.,0.)) ;
#9494=DIRECTION('center_axis',(-1.,0.,0.)) ;
#9495=DIRECTION('ref_axis',(0.,0.,-1.)) ;
#9496=DIRECTION('',(0.,0.,-1.)) ;
#9497=DIRECTION('',(0.,-1.,0.)) ;
#9498=DIRECTION('center_axis',(0.944683590425841,0.,0.327983100144111)) ;
#9499=DIRECTION('ref_axis',(-0.327983100144111,0.,0.944683590425841)) ;
#9500=DIRECTION('',(-0.327983100144111,0.,0.944683590425841)) ;
#9501=DIRECTION('',(0.,-1.,0.)) ;
#9502=DIRECTION('center_axis',(0.,0.,1.)) ;
#9503=DIRECTION('ref_axis',(-1.,0.,0.)) ;
#9504=DIRECTION('',(-1.,0.,0.)) ;
#9505=DIRECTION('',(0.,-1.,0.)) ;
#9506=DIRECTION('center_axis',(-0.946846702516136,0.,0.321685128556358)) ;
#9507=DIRECTION('ref_axis',(-0.321685128556358,0.,-0.946846702516135)) ;
#9508=DIRECTION('',(-0.321685128556358,0.,-0.946846702516135)) ;
#9509=DIRECTION('',(0.,-1.,0.)) ;
#9510=DIRECTION('center_axis',(1.,0.,0.)) ;
#9511=DIRECTION('ref_axis',(0.,0.,1.)) ;
#9512=DIRECTION('',(0.,0.,1.)) ;
#9513=DIRECTION('',(0.,-1.,0.)) ;
#9514=DIRECTION('center_axis',(-0.945579694085495,0.,-0.325390599331299)) ;
#9515=DIRECTION('ref_axis',(0.325390599331299,0.,-0.945579694085495)) ;
#9516=DIRECTION('',(0.,-1.,0.)) ;
#9517=DIRECTION('',(0.325390599331299,0.,-0.945579694085495)) ;
#9518=DIRECTION('',(0.,-1.,0.)) ;
#9519=DIRECTION('',(0.,-1.,0.)) ;
#9520=DIRECTION('center_axis',(0.948408846174048,0.,-0.317049933762509)) ;
#9521=DIRECTION('ref_axis',(0.317049933762509,0.,0.948408846174048)) ;
#9522=DIRECTION('',(0.,-1.,0.)) ;
#9523=DIRECTION('',(0.317049933762509,0.,0.948408846174048)) ;
#9524=DIRECTION('center_axis',(0.,0.,-1.)) ;
#9525=DIRECTION('ref_axis',(1.,0.,0.)) ;
#9526=DIRECTION('',(0.,-1.,0.)) ;
#9527=DIRECTION('',(1.,0.,0.)) ;
#9528=DIRECTION('center_axis',(-1.,0.,0.)) ;
#9529=DIRECTION('ref_axis',(0.,0.,-1.)) ;
#9530=DIRECTION('',(0.,-1.,0.)) ;
#9531=DIRECTION('',(0.,0.,-1.)) ;
#9532=DIRECTION('center_axis',(0.,0.,1.)) ;
#9533=DIRECTION('ref_axis',(-1.,0.,0.)) ;
#9534=DIRECTION('',(-1.,0.,0.)) ;
#9535=DIRECTION('center_axis',(0.,1.,0.)) ;
#9536=DIRECTION('ref_axis',(1.,0.,0.)) ;
#9537=DIRECTION('center_axis',(1.,0.,0.)) ;
#9538=DIRECTION('ref_axis',(0.,1.,0.)) ;
#9539=DIRECTION('center_axis',(1.,0.,0.)) ;
#9540=DIRECTION('ref_axis',(0.,0.,-1.)) ;
#9541=DIRECTION('',(1.,0.,0.)) ;
#9542=DIRECTION('center_axis',(1.,0.,0.)) ;
#9543=DIRECTION('ref_axis',(0.,0.,-1.)) ;
#9544=DIRECTION('center_axis',(-1.,0.,0.)) ;
#9545=DIRECTION('ref_axis',(0.,0.,1.)) ;
#9546=DIRECTION('center_axis',(-1.,0.,0.)) ;
#9547=DIRECTION('ref_axis',(0.,1.,0.)) ;
#9548=DIRECTION('center_axis',(1.,0.,0.)) ;
#9549=DIRECTION('ref_axis',(0.,0.,-1.)) ;
#9550=DIRECTION('center_axis',(1.,0.,0.)) ;
#9551=DIRECTION('ref_axis',(0.,1.,0.)) ;
#9552=DIRECTION('center_axis',(1.,0.,0.)) ;
#9553=DIRECTION('ref_axis',(0.,-0.707106781186547,0.707106781186548)) ;
#9554=DIRECTION('',(-0.707106781186548,-0.347335095474414,0.615920718479075)) ;
#9555=DIRECTION('center_axis',(-1.,0.,0.)) ;
#9556=DIRECTION('ref_axis',(0.,0.,-1.)) ;
#9557=DIRECTION('center_axis',(-1.,0.,0.)) ;
#9558=DIRECTION('ref_axis',(0.,0.,-1.)) ;
#9559=DIRECTION('',(0.707106781186545,0.615920718479078,-0.347335095474413)) ;
#9560=DIRECTION('center_axis',(1.,0.,0.)) ;
#9561=DIRECTION('ref_axis',(0.,0.,-1.)) ;
#9562=DIRECTION('center_axis',(1.,0.,0.)) ;
#9563=DIRECTION('ref_axis',(0.,0.,-1.)) ;
#9564=DIRECTION('center_axis',(1.,0.,0.)) ;
#9565=DIRECTION('ref_axis',(0.,-1.,2.86509167645202E-16)) ;
#9566=DIRECTION('center_axis',(1.,0.,0.)) ;
#9567=DIRECTION('ref_axis',(0.,-1.,2.86509167645202E-16)) ;
#9568=DIRECTION('center_axis',(1.,0.,0.)) ;
#9569=DIRECTION('ref_axis',(0.,-1.,2.86509167645202E-16)) ;
#9570=DIRECTION('center_axis',(1.,0.,0.)) ;
#9571=DIRECTION('ref_axis',(0.,-1.,2.86509167645202E-16)) ;
#9572=DIRECTION('center_axis',(0.,-1.,0.)) ;
#9573=DIRECTION('ref_axis',(0.,0.,1.)) ;
#9574=DIRECTION('center_axis',(-1.,0.,0.)) ;
#9575=DIRECTION('ref_axis',(0.,-1.,2.86509167645202E-16)) ;
#9576=DIRECTION('center_axis',(-1.,0.,0.)) ;
#9577=DIRECTION('ref_axis',(0.,-1.,2.86509167645202E-16)) ;
#9578=DIRECTION('center_axis',(1.,0.,0.)) ;
#9579=DIRECTION('ref_axis',(0.,-1.,2.86509167645202E-16)) ;
#9580=DIRECTION('center_axis',(-1.,0.,0.)) ;
#9581=DIRECTION('ref_axis',(0.,0.,-1.)) ;
#9582=DIRECTION('',(-1.,0.,0.)) ;
#9583=DIRECTION('center_axis',(-1.,0.,0.)) ;
#9584=DIRECTION('ref_axis',(0.,0.,-1.)) ;
#9585=DIRECTION('center_axis',(1.,0.,0.)) ;
#9586=DIRECTION('ref_axis',(0.,0.707106781186547,0.707106781186548)) ;
#9587=DIRECTION('',(-0.707106781186548,0.615920718479075,0.347335095474414)) ;
#9588=DIRECTION('center_axis',(-1.,0.,0.)) ;
#9589=DIRECTION('ref_axis',(0.,0.,-1.)) ;
#9590=DIRECTION('center_axis',(-1.,0.,0.)) ;
#9591=DIRECTION('ref_axis',(0.,0.,-1.)) ;
#9592=DIRECTION('',(0.707106781186548,-0.347335095474414,-0.615920718479075)) ;
#9593=DIRECTION('center_axis',(1.,0.,0.)) ;
#9594=DIRECTION('ref_axis',(0.,0.,-1.)) ;
#9595=DIRECTION('center_axis',(-1.,0.,0.)) ;
#9596=DIRECTION('ref_axis',(0.,0.,-1.)) ;
#9597=DIRECTION('',(-1.,0.,0.)) ;
#9598=DIRECTION('center_axis',(-1.,0.,0.)) ;
#9599=DIRECTION('ref_axis',(0.,0.,-1.)) ;
#9600=DIRECTION('center_axis',(1.,0.,0.)) ;
#9601=DIRECTION('ref_axis',(0.,0.707106781186548,-0.707106781186547)) ;
#9602=DIRECTION('',(-0.70710678118654,0.347335095474421,-0.615920718479079)) ;
#9603=DIRECTION('center_axis',(-1.,0.,0.)) ;
#9604=DIRECTION('ref_axis',(0.,0.,-1.)) ;
#9605=DIRECTION('center_axis',(-1.,0.,0.)) ;
#9606=DIRECTION('ref_axis',(0.,0.,-1.)) ;
#9607=DIRECTION('',(0.707106781186546,-0.615920718479074,0.347335095474418)) ;
#9608=DIRECTION('center_axis',(1.,0.,0.)) ;
#9609=DIRECTION('ref_axis',(0.,0.,-1.)) ;
#9610=DIRECTION('center_axis',(-1.,0.,0.)) ;
#9611=DIRECTION('ref_axis',(0.,0.,-1.)) ;
#9612=DIRECTION('',(-1.,0.,0.)) ;
#9613=DIRECTION('center_axis',(-1.,0.,0.)) ;
#9614=DIRECTION('ref_axis',(0.,0.,-1.)) ;
#9615=DIRECTION('center_axis',(1.,0.,0.)) ;
#9616=DIRECTION('ref_axis',(0.,-0.707106781186547,-0.707106781186548)) ;
#9617=DIRECTION('',(-0.707106781186544,-0.615920718479077,-0.347335095474417)) ;
#9618=DIRECTION('center_axis',(-1.,0.,0.)) ;
#9619=DIRECTION('ref_axis',(0.,0.,-1.)) ;
#9620=DIRECTION('center_axis',(-1.,0.,0.)) ;
#9621=DIRECTION('ref_axis',(0.,0.,-1.)) ;
#9622=DIRECTION('',(0.707106781186544,0.347335095474417,0.615920718479077)) ;
#9623=DIRECTION('center_axis',(1.,0.,0.)) ;
#9624=DIRECTION('ref_axis',(0.,0.,-1.)) ;
#9625=DIRECTION('center_axis',(-1.,0.,0.)) ;
#9626=DIRECTION('ref_axis',(0.,0.,-1.)) ;
#9627=DIRECTION('',(-1.,0.,0.)) ;
#9628=DIRECTION('center_axis',(-1.,0.,0.)) ;
#9629=DIRECTION('ref_axis',(0.,0.,-1.)) ;
#9630=DIRECTION('center_axis',(1.,0.,0.)) ;
#9631=DIRECTION('ref_axis',(0.,0.,-1.)) ;
#9632=DIRECTION('center_axis',(1.,0.,0.)) ;
#9633=DIRECTION('ref_axis',(0.,0.,-1.)) ;
#9634=DIRECTION('center_axis',(1.,0.,0.)) ;
#9635=DIRECTION('ref_axis',(0.,0.,-1.)) ;
#9636=DIRECTION('center_axis',(1.,0.,0.)) ;
#9637=DIRECTION('ref_axis',(0.,0.,-1.)) ;
#9638=DIRECTION('center_axis',(1.,0.,0.)) ;
#9639=DIRECTION('ref_axis',(0.,0.,-1.)) ;
#9640=DIRECTION('center_axis',(1.,0.,0.)) ;
#9641=DIRECTION('ref_axis',(0.,0.,-1.)) ;
#9642=DIRECTION('center_axis',(1.,0.,0.)) ;
#9643=DIRECTION('ref_axis',(0.,0.,-1.)) ;
#9644=DIRECTION('center_axis',(1.,0.,0.)) ;
#9645=DIRECTION('ref_axis',(0.,0.,-1.)) ;
#9646=DIRECTION('center_axis',(-1.,0.,0.)) ;
#9647=DIRECTION('ref_axis',(0.,0.,-1.)) ;
#9648=DIRECTION('',(-1.,0.,0.)) ;
#9649=DIRECTION('center_axis',(1.,0.,0.)) ;
#9650=DIRECTION('ref_axis',(0.,0.,-1.)) ;
#9651=DIRECTION('center_axis',(-1.,0.,0.)) ;
#9652=DIRECTION('ref_axis',(0.,0.,-1.)) ;
#9653=DIRECTION('',(-1.,0.,0.)) ;
#9654=DIRECTION('center_axis',(1.,0.,0.)) ;
#9655=DIRECTION('ref_axis',(0.,0.,-1.)) ;
#9656=DIRECTION('center_axis',(-1.,0.,0.)) ;
#9657=DIRECTION('ref_axis',(0.,0.,-1.)) ;
#9658=DIRECTION('',(-1.,0.,0.)) ;
#9659=DIRECTION('center_axis',(1.,0.,0.)) ;
#9660=DIRECTION('ref_axis',(0.,0.,-1.)) ;
#9661=DIRECTION('center_axis',(-1.,0.,0.)) ;
#9662=DIRECTION('ref_axis',(0.,0.,-1.)) ;
#9663=DIRECTION('',(-1.,0.,0.)) ;
#9664=DIRECTION('center_axis',(1.,0.,0.)) ;
#9665=DIRECTION('ref_axis',(0.,0.,-1.)) ;
#9666=DIRECTION('center_axis',(1.,0.,0.)) ;
#9667=DIRECTION('ref_axis',(0.,0.,-1.)) ;
#9668=DIRECTION('',(1.,0.,0.)) ;
#9669=DIRECTION('center_axis',(1.,0.,0.)) ;
#9670=DIRECTION('ref_axis',(0.,0.,-1.)) ;
#9671=DIRECTION('',(-1.,0.,0.)) ;
#9672=DIRECTION('center_axis',(-1.,0.,0.)) ;
#9673=DIRECTION('ref_axis',(0.,0.,-1.)) ;
#9674=DIRECTION('center_axis',(1.,0.,0.)) ;
#9675=DIRECTION('ref_axis',(0.,0.,-1.)) ;
#9676=DIRECTION('',(1.,0.,0.)) ;
#9677=DIRECTION('center_axis',(1.,0.,0.)) ;
#9678=DIRECTION('ref_axis',(0.,0.,-1.)) ;
#9679=DIRECTION('',(-1.,0.,0.)) ;
#9680=DIRECTION('center_axis',(-1.,0.,0.)) ;
#9681=DIRECTION('ref_axis',(0.,0.,-1.)) ;
#9682=DIRECTION('center_axis',(1.,0.,0.)) ;
#9683=DIRECTION('ref_axis',(0.,0.707106781186548,0.707106781186547)) ;
#9684=DIRECTION('',(-1.,0.,0.)) ;
#9685=DIRECTION('center_axis',(-1.,0.,0.)) ;
#9686=DIRECTION('ref_axis',(0.,0.,-1.)) ;
#9687=DIRECTION('',(1.,0.,0.)) ;
#9688=DIRECTION('center_axis',(1.,0.,0.)) ;
#9689=DIRECTION('ref_axis',(0.,0.,-1.)) ;
#9690=DIRECTION('center_axis',(1.,0.,0.)) ;
#9691=DIRECTION('ref_axis',(0.,-0.707106781186547,0.707106781186548)) ;
#9692=DIRECTION('',(-1.,0.,0.)) ;
#9693=DIRECTION('center_axis',(-1.,0.,0.)) ;
#9694=DIRECTION('ref_axis',(0.,0.,-1.)) ;
#9695=DIRECTION('',(1.,0.,0.)) ;
#9696=DIRECTION('center_axis',(1.,0.,0.)) ;
#9697=DIRECTION('ref_axis',(0.,0.,-1.)) ;
#9698=DIRECTION('center_axis',(1.,0.,0.)) ;
#9699=DIRECTION('ref_axis',(0.,0.,-1.)) ;
#9700=DIRECTION('center_axis',(1.,0.,0.)) ;
#9701=DIRECTION('ref_axis',(0.,0.,-1.)) ;
#9702=DIRECTION('center_axis',(1.,0.,0.)) ;
#9703=DIRECTION('ref_axis',(0.,0.,-1.)) ;
#9704=DIRECTION('center_axis',(1.,0.,0.)) ;
#9705=DIRECTION('ref_axis',(0.,0.,-1.)) ;
#9706=DIRECTION('center_axis',(1.,0.,0.)) ;
#9707=DIRECTION('ref_axis',(0.,0.,-1.)) ;
#9708=DIRECTION('center_axis',(1.,0.,0.)) ;
#9709=DIRECTION('ref_axis',(0.,0.,-1.)) ;
#9710=DIRECTION('center_axis',(1.,0.,0.)) ;
#9711=DIRECTION('ref_axis',(0.,1.,0.)) ;
#9712=DIRECTION('center_axis',(1.,0.,0.)) ;
#9713=DIRECTION('ref_axis',(0.,0.,-1.)) ;
#9714=DIRECTION('center_axis',(1.,0.,0.)) ;
#9715=DIRECTION('ref_axis',(0.,1.,0.)) ;
#9716=DIRECTION('center_axis',(1.,0.,0.)) ;
#9717=DIRECTION('ref_axis',(0.,0.,-1.)) ;
#9718=DIRECTION('center_axis',(1.,0.,0.)) ;
#9719=DIRECTION('ref_axis',(0.,-1.,-1.22464679914735E-16)) ;
#9720=DIRECTION('center_axis',(1.,0.,0.)) ;
#9721=DIRECTION('ref_axis',(0.,0.,-1.)) ;
#9722=DIRECTION('center_axis',(1.,0.,0.)) ;
#9723=DIRECTION('ref_axis',(0.,1.,0.)) ;
#9724=DIRECTION('center_axis',(1.,0.,0.)) ;
#9725=DIRECTION('ref_axis',(0.,0.,-1.)) ;
#9726=DIRECTION('center_axis',(1.,0.,0.)) ;
#9727=DIRECTION('ref_axis',(0.,0.,-1.)) ;
#9728=DIRECTION('center_axis',(1.,0.,0.)) ;
#9729=DIRECTION('ref_axis',(0.,0.,-1.)) ;
#9730=DIRECTION('center_axis',(1.,0.,0.)) ;
#9731=DIRECTION('ref_axis',(0.,1.,0.)) ;
#9732=DIRECTION('',(-1.,0.,0.)) ;
#9733=DIRECTION('center_axis',(-1.,0.,0.)) ;
#9734=DIRECTION('ref_axis',(0.,0.,1.)) ;
#9735=DIRECTION('center_axis',(1.,0.,0.)) ;
#9736=DIRECTION('ref_axis',(0.,0.,-1.)) ;
#9737=DIRECTION('center_axis',(1.,0.,0.)) ;
#9738=DIRECTION('ref_axis',(0.,1.,0.)) ;
#9739=DIRECTION('center_axis',(1.,0.,0.)) ;
#9740=DIRECTION('ref_axis',(0.,1.,0.)) ;
#9741=DIRECTION('',(1.,0.,0.)) ;
#9742=DIRECTION('center_axis',(1.,0.,0.)) ;
#9743=DIRECTION('ref_axis',(0.,0.,-1.)) ;
#9744=DIRECTION('center_axis',(1.,0.,0.)) ;
#9745=DIRECTION('ref_axis',(0.,0.,-1.)) ;
#9746=DIRECTION('center_axis',(-1.,0.,0.)) ;
#9747=DIRECTION('ref_axis',(0.,1.,0.)) ;
#9748=DIRECTION('center_axis',(1.,0.,0.)) ;
#9749=DIRECTION('ref_axis',(0.,1.,0.)) ;
#9750=DIRECTION('center_axis',(1.,0.,0.)) ;
#9751=DIRECTION('ref_axis',(0.,0.,-1.)) ;
#9752=DIRECTION('',(-1.,0.,0.)) ;
#9753=DIRECTION('center_axis',(-1.,0.,0.)) ;
#9754=DIRECTION('ref_axis',(0.,0.,1.)) ;
#9755=DIRECTION('center_axis',(1.,0.,0.)) ;
#9756=DIRECTION('ref_axis',(0.,0.,-1.)) ;
#9757=DIRECTION('center_axis',(1.,0.,0.)) ;
#9758=DIRECTION('ref_axis',(0.,1.,0.)) ;
#9759=DIRECTION('center_axis',(1.,0.,0.)) ;
#9760=DIRECTION('ref_axis',(0.,1.,0.)) ;
#9761=DIRECTION('',(1.,0.,0.)) ;
#9762=DIRECTION('center_axis',(1.,0.,0.)) ;
#9763=DIRECTION('ref_axis',(0.,0.,-1.)) ;
#9764=DIRECTION('center_axis',(1.,0.,0.)) ;
#9765=DIRECTION('ref_axis',(0.,0.,-1.)) ;
#9766=DIRECTION('center_axis',(-1.,0.,0.)) ;
#9767=DIRECTION('ref_axis',(0.,1.,0.)) ;
#9768=DIRECTION('center_axis',(1.,0.,0.)) ;
#9769=DIRECTION('ref_axis',(0.,1.,0.)) ;
#9770=DIRECTION('center_axis',(1.,0.,0.)) ;
#9771=DIRECTION('ref_axis',(0.,0.,-1.)) ;
#9772=DIRECTION('',(-1.,0.,0.)) ;
#9773=DIRECTION('center_axis',(-1.,0.,0.)) ;
#9774=DIRECTION('ref_axis',(0.,0.,1.)) ;
#9775=DIRECTION('center_axis',(1.,0.,0.)) ;
#9776=DIRECTION('ref_axis',(0.,1.,0.)) ;
#9777=DIRECTION('',(-1.,0.,0.)) ;
#9778=DIRECTION('center_axis',(1.,0.,0.)) ;
#9779=DIRECTION('ref_axis',(0.,0.,-1.)) ;
#9780=DIRECTION('center_axis',(-1.,0.,0.)) ;
#9781=DIRECTION('ref_axis',(0.,0.,1.)) ;
#9782=DIRECTION('center_axis',(1.,0.,0.)) ;
#9783=DIRECTION('ref_axis',(0.,0.,-1.)) ;
#9784=DIRECTION('center_axis',(1.,0.,0.)) ;
#9785=DIRECTION('ref_axis',(0.,1.,0.)) ;
#9786=DIRECTION('center_axis',(1.,0.,0.)) ;
#9787=DIRECTION('ref_axis',(0.,0.,-1.)) ;
#9788=DIRECTION('',(-0.707106781186548,0.707106781186548,8.65956056235493E-17)) ;
#9789=DIRECTION('center_axis',(1.,0.,0.)) ;
#9790=DIRECTION('ref_axis',(0.,1.,0.)) ;
#9791=DIRECTION('center_axis',(1.,0.,0.)) ;
#9792=DIRECTION('ref_axis',(0.,0.,-1.)) ;
#9793=DIRECTION('',(-1.,0.,0.)) ;
#9794=DIRECTION('center_axis',(-1.,0.,0.)) ;
#9795=DIRECTION('ref_axis',(0.,1.,0.)) ;
#9796=DIRECTION('',(-0.707106781186548,-0.707106781186548,-8.65956056235493E-17)) ;
#9797=DIRECTION('center_axis',(-1.,0.,0.)) ;
#9798=DIRECTION('ref_axis',(0.,1.,0.)) ;
#9799=DIRECTION('center_axis',(1.,0.,0.)) ;
#9800=DIRECTION('ref_axis',(0.,0.,-1.)) ;
#9801=DIRECTION('',(-0.707106781186548,-0.707106781186548,-8.65956056235493E-17)) ;
#9802=DIRECTION('center_axis',(1.,0.,0.)) ;
#9803=DIRECTION('ref_axis',(0.,0.,-1.)) ;
#9804=DIRECTION('center_axis',(1.,0.,0.)) ;
#9805=DIRECTION('ref_axis',(0.,1.,0.)) ;
#9806=DIRECTION('',(-1.,0.,0.)) ;
#11223=CARTESIAN_POINT('',(0.,0.,0.)) ;
#11224=CARTESIAN_POINT('Ctrl Pts',(66.2495224699378,41.5,26.4154158473015)) ;
#11225=CARTESIAN_POINT('Ctrl Pts',(66.2495224699378,40.85,26.4154158473015)) ;
#11226=CARTESIAN_POINT('Ctrl Pts',(66.4206003174186,41.5,26.4154158473015)) ;
#11227=CARTESIAN_POINT('Ctrl Pts',(66.4206003174186,40.85,26.4154158473015)) ;
#11228=CARTESIAN_POINT('Ctrl Pts',(66.5436561927199,41.5,26.277353310585)) ;
#11229=CARTESIAN_POINT('Ctrl Pts',(66.5436561927199,40.85,26.277353310585)) ;
#11230=CARTESIAN_POINT('',(66.2495224699378,40.9729445751773,26.4154158473015)) ;
#11231=CARTESIAN_POINT('',(66.5436561927199,40.9804948832562,26.277353310585)) ;
#11232=CARTESIAN_POINT('Ctrl Pts',(66.2495224699378,40.9729445751773,26.4154158473015)) ;
#11233=CARTESIAN_POINT('Ctrl Pts',(66.2995225246323,40.9729445751773,26.4154158473015)) ;
#11234=CARTESIAN_POINT('Ctrl Pts',(66.3478889016248,40.9734772686179,26.4065715531905)) ;
#11235=CARTESIAN_POINT('Ctrl Pts',(66.3940330750068,40.9745795963019,26.3873479124433)) ;
#11236=CARTESIAN_POINT('Ctrl Pts',(66.4219819653177,40.9752472609986,26.3757044179944)) ;
#11237=CARTESIAN_POINT('Ctrl Pts',(66.4480801252716,40.9760959140079,26.3606844081376)) ;
#11238=CARTESIAN_POINT('Ctrl Pts',(66.4724676043192,40.9770721634385,26.3427557461786)) ;
#11239=CARTESIAN_POINT('Ctrl Pts',(66.4985095759234,40.978114643471,26.3236107699913)) ;
#11240=CARTESIAN_POINT('Ctrl Pts',(66.5221553224869,40.979283551382,26.3014762114925)) ;
#11241=CARTESIAN_POINT('Ctrl Pts',(66.5436561927199,40.9804948832562,26.277353310585)) ;
#11242=CARTESIAN_POINT('',(66.2495224699378,40.85,26.4154158473015)) ;
#11243=CARTESIAN_POINT('',(66.2495224699378,41.5,26.4154158473015)) ;
#11244=CARTESIAN_POINT('',(66.5436561927199,40.85,26.277353310585)) ;
#11245=CARTESIAN_POINT('Ctrl Pts',(66.2495224699378,40.85,26.4154158473015)) ;
#11246=CARTESIAN_POINT('Ctrl Pts',(66.4206003174186,40.85,26.4154158473015)) ;
#11247=CARTESIAN_POINT('Ctrl Pts',(66.5436561927199,40.85,26.277353310585)) ;
#11248=CARTESIAN_POINT('',(66.5436561927199,41.5,26.277353310585)) ;
#11249=CARTESIAN_POINT('Ctrl Pts',(66.5436561927199,41.5,26.277353310585)) ;
#11250=CARTESIAN_POINT('Ctrl Pts',(66.5436561927199,40.85,26.277353310585)) ;
#11251=CARTESIAN_POINT('Ctrl Pts',(66.6667120680213,41.5,26.1392904758453)) ;
#11252=CARTESIAN_POINT('Ctrl Pts',(66.6667120680213,40.85,26.1392904758453)) ;
#11253=CARTESIAN_POINT('Ctrl Pts',(66.6667120680213,41.5,25.9021826028824)) ;
#11254=CARTESIAN_POINT('Ctrl Pts',(66.6667120680213,40.85,25.9021826028824)) ;
#11255=CARTESIAN_POINT('',(66.6667120680213,40.9947813522469,25.9021826028824)) ;
#11256=CARTESIAN_POINT('Ctrl Pts',(66.5436561927199,40.9804948832562,26.277353310585)) ;
#11257=CARTESIAN_POINT('Ctrl Pts',(66.5821223532304,40.9826620228363,26.2341961094468)) ;
#11258=CARTESIAN_POINT('Ctrl Pts',(66.6105875841343,40.9849568963094,26.1848827603603)) ;
#11259=CARTESIAN_POINT('Ctrl Pts',(66.6303948051965,40.9871681759971,26.1305726670125)) ;
#11260=CARTESIAN_POINT('Ctrl Pts',(66.6499886361015,40.9893556327912,26.076847675397)) ;
#11261=CARTESIAN_POINT('Ctrl Pts',(66.6604621061239,40.9913728985934,26.0199931986045)) ;
#11262=CARTESIAN_POINT('Ctrl Pts',(66.6645899528845,40.9930871506489,25.9627489167057)) ;
#11263=CARTESIAN_POINT('Ctrl Pts',(66.6660451595907,40.9936914829393,25.9425683558126)) ;
#11264=CARTESIAN_POINT('Ctrl Pts',(66.6667120680213,40.9942581565947,25.9223396215523)) ;
#11265=CARTESIAN_POINT('Ctrl Pts',(66.6667120680213,40.9947813522469,25.9021826028824)) ;
#11266=CARTESIAN_POINT('',(66.6667120680213,40.85,25.9021826028824)) ;
#11267=CARTESIAN_POINT('Ctrl Pts',(66.5436561927199,40.85,26.277353310585)) ;
#11268=CARTESIAN_POINT('Ctrl Pts',(66.6667120680213,40.85,26.1392904758453)) ;
#11269=CARTESIAN_POINT('Ctrl Pts',(66.6667120680213,40.85,25.9021826028824)) ;
#11270=CARTESIAN_POINT('',(66.6667120680213,41.5,25.9021826028824)) ;
#11271=CARTESIAN_POINT('Ctrl Pts',(66.6667120680213,41.5,25.9021826028824)) ;
#11272=CARTESIAN_POINT('Ctrl Pts',(66.6667120680213,40.85,25.9021826028824)) ;
#11273=CARTESIAN_POINT('Ctrl Pts',(66.6667120680213,41.5,25.6740789055824)) ;
#11274=CARTESIAN_POINT('Ctrl Pts',(66.6667120680213,40.85,25.6740789055824)) ;
#11275=CARTESIAN_POINT('Ctrl Pts',(66.5451570376754,41.5,25.5427692770958)) ;
#11276=CARTESIAN_POINT('Ctrl Pts',(66.5451570376754,40.85,25.5427692770958)) ;
#11277=CARTESIAN_POINT('',(66.5451570376754,40.9999409930792,25.5427692770958)) ;
#11278=CARTESIAN_POINT('Ctrl Pts',(66.6667120680213,40.9947813522469,25.9021826028824)) ;
#11279=CARTESIAN_POINT('Ctrl Pts',(66.6667120680213,40.9965684739587,25.8333306436577)) ;
#11280=CARTESIAN_POINT('Ctrl Pts',(66.6584071624267,40.997895970425,25.7635943278561)) ;
#11281=CARTESIAN_POINT('Ctrl Pts',(66.6363375933712,40.9987312162041,25.6983196608033)) ;
#11282=CARTESIAN_POINT('Ctrl Pts',(66.6264687443208,40.9991047130536,25.6691307883633)) ;
#11283=CARTESIAN_POINT('Ctrl Pts',(66.613931069591,40.999380770686,25.6410760408134)) ;
#11284=CARTESIAN_POINT('Ctrl Pts',(66.5983483633277,40.9995771384542,25.6144924849394)) ;
#11285=CARTESIAN_POINT('Ctrl Pts',(66.5832078919034,40.9997679333349,25.5886633663468)) ;
#11286=CARTESIAN_POINT('Ctrl Pts',(66.5654960787534,40.9998803674897,25.5647404939194)) ;
#11287=CARTESIAN_POINT('Ctrl Pts',(66.5451570376754,40.9999409930792,25.5427692770958)) ;
#11288=CARTESIAN_POINT('',(66.5451570376754,40.85,25.5427692770958)) ;
#11289=CARTESIAN_POINT('Ctrl Pts',(66.6667120680213,40.85,25.9021826028824)) ;
#11290=CARTESIAN_POINT('Ctrl Pts',(66.6667120680213,40.85,25.6740789055824)) ;
#11291=CARTESIAN_POINT('Ctrl Pts',(66.5451570376754,40.85,25.5427692770958)) ;
#11292=CARTESIAN_POINT('',(66.5451570376754,41.5,25.5427692770958)) ;
#11293=CARTESIAN_POINT('Ctrl Pts',(66.5451570376754,41.5,25.5427692770958)) ;
#11294=CARTESIAN_POINT('Ctrl Pts',(66.5451570376754,40.85,25.5427692770958)) ;
#11295=CARTESIAN_POINT('Ctrl Pts',(66.4236017093062,41.5,25.4114596486092)) ;
#11296=CARTESIAN_POINT('Ctrl Pts',(66.4236017093062,40.85,25.4114596486092)) ;
#11297=CARTESIAN_POINT('Ctrl Pts',(66.2390177473426,41.5,25.4114596486092)) ;
#11298=CARTESIAN_POINT('Ctrl Pts',(66.2390177473426,40.85,25.4114596486092)) ;
#11299=CARTESIAN_POINT('',(66.2390177473426,40.9997471142653,25.4114596486092)) ;
#11300=CARTESIAN_POINT('Ctrl Pts',(66.5451570376754,40.9999409930792,25.5427692770958)) ;
#11301=CARTESIAN_POINT('Ctrl Pts',(66.5082425374556,41.000051025693,25.5028925446262)) ;
#11302=CARTESIAN_POINT('Ctrl Pts',(66.4655429676267,40.9999885189357,25.4705584633671)) ;
#11303=CARTESIAN_POINT('Ctrl Pts',(66.4161246072134,40.9999126252241,25.4479556879396)) ;
#11304=CARTESIAN_POINT('Ctrl Pts',(66.389129448404,40.9998711677015,25.4356087483184)) ;
#11305=CARTESIAN_POINT('Ctrl Pts',(66.3610245827433,40.9998272455883,25.4265748528042)) ;
#11306=CARTESIAN_POINT('Ctrl Pts',(66.3319507146315,40.999796548506,25.4205836608745)) ;
#11307=CARTESIAN_POINT('Ctrl Pts',(66.301358198468,40.9997642479885,25.4142795242786)) ;
#11308=CARTESIAN_POINT('Ctrl Pts',(66.2702519538158,40.9997471142653,25.4114596486092)) ;
#11309=CARTESIAN_POINT('Ctrl Pts',(66.2390177473426,40.9997471142653,25.4114596486092)) ;
#11310=CARTESIAN_POINT('',(66.2390177473426,40.85,25.4114596486092)) ;
#11311=CARTESIAN_POINT('Ctrl Pts',(66.5451570376754,40.85,25.5427692770958)) ;
#11312=CARTESIAN_POINT('Ctrl Pts',(66.4236017093062,40.85,25.4114596486092)) ;
#11313=CARTESIAN_POINT('Ctrl Pts',(66.2390177473426,40.85,25.4114596486092)) ;
#11314=CARTESIAN_POINT('',(66.2390177473426,41.5,25.4114596486092)) ;
#11315=CARTESIAN_POINT('Ctrl Pts',(66.2930422052741,41.5,25.172851228714)) ;
#11316=CARTESIAN_POINT('Ctrl Pts',(66.2930422052741,40.85,25.172851228714)) ;
#11317=CARTESIAN_POINT('Ctrl Pts',(66.5631650909781,41.5,25.172851228714)) ;
#11318=CARTESIAN_POINT('Ctrl Pts',(66.5631650909781,40.85,25.172851228714)) ;
#11319=CARTESIAN_POINT('Ctrl Pts',(66.7530014142394,41.5,25.371691429615)) ;
#11320=CARTESIAN_POINT('Ctrl Pts',(66.7530014142394,40.85,25.371691429615)) ;
#11321=CARTESIAN_POINT('',(66.2930422052741,40.9965471535257,25.172851228714)) ;
#11322=CARTESIAN_POINT('',(66.7530014142394,40.9994689235072,25.371691429615)) ;
#11323=CARTESIAN_POINT('Ctrl Pts',(66.2930422052741,40.9965471535257,25.172851228714)) ;
#11324=CARTESIAN_POINT('Ctrl Pts',(66.3770902451354,40.9965471535257,25.172851228714)) ;
#11325=CARTESIAN_POINT('Ctrl Pts',(66.4586948235472,40.9968790271012,25.1872883524376)) ;
#11326=CARTESIAN_POINT('Ctrl Pts',(66.5362595609816,40.9974645836146,25.2196582806458)) ;
#11327=CARTESIAN_POINT('Ctrl Pts',(66.5764466645678,40.9977679665827,25.2364294797887)) ;
#11328=CARTESIAN_POINT('Ctrl Pts',(66.6143004551277,40.998122981106,25.2574932807612)) ;
#11329=CARTESIAN_POINT('Ctrl Pts',(66.6499502310137,40.9984739132174,25.2824997440933)) ;
#11330=CARTESIAN_POINT('Ctrl Pts',(66.6872709183778,40.9988412935807,25.3086782649088)) ;
#11331=CARTESIAN_POINT('Ctrl Pts',(66.7215222344078,40.9991959709695,25.3387192020962)) ;
#11332=CARTESIAN_POINT('Ctrl Pts',(66.7530014142394,40.9994689235072,25.371691429615)) ;
#11333=CARTESIAN_POINT('',(66.2930422052741,40.85,25.172851228714)) ;
#11334=CARTESIAN_POINT('',(66.2930422052741,41.5,25.172851228714)) ;
#11335=CARTESIAN_POINT('',(66.7530014142394,40.85,25.371691429615)) ;
#11336=CARTESIAN_POINT('Ctrl Pts',(66.2930422052741,40.85,25.172851228714)) ;
#11337=CARTESIAN_POINT('Ctrl Pts',(66.5631650909781,40.85,25.172851228714)) ;
#11338=CARTESIAN_POINT('Ctrl Pts',(66.7530014142394,40.85,25.371691429615)) ;
#11339=CARTESIAN_POINT('',(66.7530014142394,41.5,25.371691429615)) ;
#11340=CARTESIAN_POINT('Ctrl Pts',(66.7530014142394,41.5,25.371691429615)) ;
#11341=CARTESIAN_POINT('Ctrl Pts',(66.7530014142394,40.85,25.371691429615)) ;
#11342=CARTESIAN_POINT('Ctrl Pts',(66.9428374394774,41.5,25.5705319285393)) ;
#11343=CARTESIAN_POINT('Ctrl Pts',(66.9428374394774,40.85,25.5705319285393)) ;
#11344=CARTESIAN_POINT('Ctrl Pts',(66.9428374394774,41.5,25.8856750965118)) ;
#11345=CARTESIAN_POINT('Ctrl Pts',(66.9428374394774,40.85,25.8856750965118)) ;
#11346=CARTESIAN_POINT('',(66.9428374394774,40.9952010222498,25.8856750965118)) ;
#11347=CARTESIAN_POINT('Ctrl Pts',(66.7530014142394,40.9994689235072,25.371691429615)) ;
#11348=CARTESIAN_POINT('Ctrl Pts',(66.8141251609826,40.9999989224803,25.4357144530812)) ;
#11349=CARTESIAN_POINT('Ctrl Pts',(66.8606682486204,41.0002177343997,25.5089691574663)) ;
#11350=CARTESIAN_POINT('Ctrl Pts',(66.8923690068865,40.9997292569968,25.5916130983996)) ;
#11351=CARTESIAN_POINT('Ctrl Pts',(66.9283689303448,40.9991745337007,25.6854649716862)) ;
#11352=CARTESIAN_POINT('Ctrl Pts',(66.9428374394774,40.997701693568,25.7852060615196)) ;
#11353=CARTESIAN_POINT('Ctrl Pts',(66.9428374394774,40.9952010222498,25.8856750965118)) ;
#11354=CARTESIAN_POINT('',(66.9428374394774,40.85,25.8856750965118)) ;
#11355=CARTESIAN_POINT('Ctrl Pts',(66.7530014142394,40.85,25.371691429615)) ;
#11356=CARTESIAN_POINT('Ctrl Pts',(66.9428374394774,40.85,25.5705319285393)) ;
#11357=CARTESIAN_POINT('Ctrl Pts',(66.9428374394774,40.85,25.8856750965118)) ;
#11358=CARTESIAN_POINT('',(66.9428374394774,41.5,25.8856750965118)) ;
#11359=CARTESIAN_POINT('Ctrl Pts',(66.9428374394774,41.5,25.8856750965118)) ;
#11360=CARTESIAN_POINT('Ctrl Pts',(66.9428374394774,40.85,25.8856750965118)) ;
#11361=CARTESIAN_POINT('Ctrl Pts',(66.9428374394774,41.5,26.0927693486214)) ;
#11362=CARTESIAN_POINT('Ctrl Pts',(66.9428374394774,40.85,26.0927693486214)) ;
#11363=CARTESIAN_POINT('Ctrl Pts',(66.8535469993949,41.5,26.270600104332)) ;
#11364=CARTESIAN_POINT('Ctrl Pts',(66.8535469993949,40.85,26.270600104332)) ;
#11365=CARTESIAN_POINT('',(66.8535469993949,40.9808325189314,26.270600104332)) ;
#11366=CARTESIAN_POINT('Ctrl Pts',(66.9428374394774,40.9952010222498,25.8856750965118)) ;
#11367=CARTESIAN_POINT('Ctrl Pts',(66.9428374394774,40.9935236896344,25.9530649961756)) ;
#11368=CARTESIAN_POINT('Ctrl Pts',(66.9357463397121,40.9914218942895,26.0197695444074)) ;
#11369=CARTESIAN_POINT('Ctrl Pts',(66.9205286843305,40.9889416737403,26.0853937371291)) ;
#11370=CARTESIAN_POINT('Ctrl Pts',(66.9055916133819,40.9865071837101,26.1498079453662)) ;
#11371=CARTESIAN_POINT('Ctrl Pts',(66.8832087746672,40.9837731043684,26.2115257408558)) ;
#11372=CARTESIAN_POINT('Ctrl Pts',(66.8535469993949,40.9808325189314,26.270600104332)) ;
#11373=CARTESIAN_POINT('',(66.8535469993949,40.85,26.270600104332)) ;
#11374=CARTESIAN_POINT('Ctrl Pts',(66.9428374394774,40.85,25.8856750965118)) ;
#11375=CARTESIAN_POINT('Ctrl Pts',(66.9428374394774,40.85,26.0927693486214)) ;
#11376=CARTESIAN_POINT('Ctrl Pts',(66.8535469993949,40.85,26.270600104332)) ;
#11377=CARTESIAN_POINT('',(66.8535469993949,41.5,26.270600104332)) ;
#11378=CARTESIAN_POINT('Ctrl Pts',(66.8535469993949,41.5,26.270600104332)) ;
#11379=CARTESIAN_POINT('Ctrl Pts',(66.8535469993949,40.85,26.270600104332)) ;
#11380=CARTESIAN_POINT('Ctrl Pts',(66.7642565593123,41.5,26.4484308600426)) ;
#11381=CARTESIAN_POINT('Ctrl Pts',(66.7642565593123,40.85,26.4484308600426)) ;
#11382=CARTESIAN_POINT('Ctrl Pts',(66.6081853732467,41.5,26.542973959446)) ;
#11383=CARTESIAN_POINT('Ctrl Pts',(66.6081853732467,40.85,26.542973959446)) ;
#11384=CARTESIAN_POINT('',(66.6081853732467,40.9648700388952,26.542973959446)) ;
#11385=CARTESIAN_POINT('Ctrl Pts',(66.8535469993949,40.9808325189314,26.270600104332)) ;
#11386=CARTESIAN_POINT('Ctrl Pts',(66.8250381231084,40.9780062286752,26.3273783552825)) ;
#11387=CARTESIAN_POINT('Ctrl Pts',(66.7901650255163,40.9750546868546,26.3802952508486)) ;
#11388=CARTESIAN_POINT('Ctrl Pts',(66.747650047791,40.9722242840042,26.4275104880653)) ;
#11389=CARTESIAN_POINT('Ctrl Pts',(66.7068356273123,40.9695070944809,26.4728371622837)) ;
#11390=CARTESIAN_POINT('Ctrl Pts',(66.66037489326,40.9670021881262,26.5113591617192)) ;
#11391=CARTESIAN_POINT('Ctrl Pts',(66.6081853732467,40.9648700388952,26.542973959446)) ;
#11392=CARTESIAN_POINT('',(66.6081853732467,40.85,26.542973959446)) ;
#11393=CARTESIAN_POINT('Ctrl Pts',(66.8535469993949,40.85,26.270600104332)) ;
#11394=CARTESIAN_POINT('Ctrl Pts',(66.7642565593123,40.85,26.4484308600426)) ;
#11395=CARTESIAN_POINT('Ctrl Pts',(66.6081853732467,40.85,26.542973959446)) ;
#11396=CARTESIAN_POINT('',(66.6081853732467,41.5,26.542973959446)) ;
#11397=CARTESIAN_POINT('Ctrl Pts',(66.6081853732467,41.5,26.542973959446)) ;
#11398=CARTESIAN_POINT('Ctrl Pts',(66.6081853732467,40.85,26.542973959446)) ;
#11399=CARTESIAN_POINT('Ctrl Pts',(66.4521144852042,41.5,26.6375167608261)) ;
#11400=CARTESIAN_POINT('Ctrl Pts',(66.4521144852042,40.85,26.6375167608261)) ;
#11401=CARTESIAN_POINT('Ctrl Pts',(66.2540247067809,41.5,26.6375167608261)) ;
#11402=CARTESIAN_POINT('Ctrl Pts',(66.2540247067809,40.85,26.6375167608261)) ;
#11403=CARTESIAN_POINT('',(66.2540247067809,40.9582035055449,26.6375167608261)) ;
#11404=CARTESIAN_POINT('Ctrl Pts',(66.6081853732467,40.9648700388952,26.542973959446)) ;
#11405=CARTESIAN_POINT('Ctrl Pts',(66.5560744050866,40.962741101465,26.5745411336594)) ;
#11406=CARTESIAN_POINT('Ctrl Pts',(66.500554898558,40.9610587138301,26.5981402654571)) ;
#11407=CARTESIAN_POINT('Ctrl Pts',(66.4416646695438,40.9599256674031,26.613866400593)) ;
#11408=CARTESIAN_POINT('Ctrl Pts',(66.3803551756684,40.9587460743851,26.6302385798481)) ;
#11409=CARTESIAN_POINT('Ctrl Pts',(66.3174911111484,40.9582035055449,26.6375167608261)) ;
#11410=CARTESIAN_POINT('Ctrl Pts',(66.2540247067809,40.9582035055449,26.6375167608261)) ;
#11411=CARTESIAN_POINT('',(66.2540247067809,40.85,26.6375167608261)) ;
#11412=CARTESIAN_POINT('Ctrl Pts',(66.6081853732467,40.85,26.542973959446)) ;
#11413=CARTESIAN_POINT('Ctrl Pts',(66.4521144852042,40.85,26.6375167608261)) ;
#11414=CARTESIAN_POINT('Ctrl Pts',(66.2540247067809,40.85,26.6375167608261)) ;
#11415=CARTESIAN_POINT('',(66.2540247067809,41.5,26.6375167608261)) ;
#11416=CARTESIAN_POINT('Ctrl Pts',(66.2540247067809,41.5,26.6375167608261)) ;
#11417=CARTESIAN_POINT('Ctrl Pts',(66.2540247067809,40.85,26.6375167608261)) ;
#11418=CARTESIAN_POINT('Ctrl Pts',(65.9163710996509,41.5,26.6375167608261)) ;
#11419=CARTESIAN_POINT('Ctrl Pts',(65.9163710996509,40.85,26.6375167608261)) ;
#11420=CARTESIAN_POINT('Ctrl Pts',(65.7032742127776,41.5,26.3891540408134)) ;
#11421=CARTESIAN_POINT('Ctrl Pts',(65.7032742127776,40.85,26.3891540408134)) ;
#11422=CARTESIAN_POINT('',(65.7032742127776,40.9744759230064,26.3891540408134)) ;
#11423=CARTESIAN_POINT('Ctrl Pts',(66.2540247067809,40.9582035055449,26.6375167608261)) ;
#11424=CARTESIAN_POINT('Ctrl Pts',(66.1548439595539,40.9582035055449,26.6375167608261)) ;
#11425=CARTESIAN_POINT('Ctrl Pts',(66.0577652439653,40.9594243783883,26.6214479538109)) ;
#11426=CARTESIAN_POINT('Ctrl Pts',(65.9661626126997,40.9620840160781,26.5834933685731)) ;
#11427=CARTESIAN_POINT('Ctrl Pts',(65.9161152714711,40.9635371162038,26.5627567799801)) ;
#11428=CARTESIAN_POINT('Ctrl Pts',(65.8693746381324,40.9653603683843,26.5361801946976)) ;
#11429=CARTESIAN_POINT('Ctrl Pts',(65.8258305111509,40.9674499706989,26.503987750885)) ;
#11430=CARTESIAN_POINT('Ctrl Pts',(65.7805849393146,40.9696212222128,26.4705374183124)) ;
#11431=CARTESIAN_POINT('Ctrl Pts',(65.7399057668323,40.9720227639775,26.4318478245509)) ;
#11432=CARTESIAN_POINT('Ctrl Pts',(65.7032742127776,40.9744759230064,26.3891540408134)) ;
#11433=CARTESIAN_POINT('',(65.7032742127776,40.85,26.3891540408134)) ;
#11434=CARTESIAN_POINT('Ctrl Pts',(66.2540247067809,40.85,26.6375167608261)) ;
#11435=CARTESIAN_POINT('Ctrl Pts',(65.9163710996509,40.85,26.6375167608261)) ;
#11436=CARTESIAN_POINT('Ctrl Pts',(65.7032742127776,40.85,26.3891540408134)) ;
#11437=CARTESIAN_POINT('',(65.7032742127776,41.5,26.3891540408134)) ;
#11438=CARTESIAN_POINT('Ctrl Pts',(65.7032742127776,41.5,26.3891540408134)) ;
#11439=CARTESIAN_POINT('Ctrl Pts',(65.7032742127776,40.85,26.3891540408134)) ;
#11440=CARTESIAN_POINT('Ctrl Pts',(65.4901773259044,41.5,26.1407910227776)) ;
#11441=CARTESIAN_POINT('Ctrl Pts',(65.4901773259044,40.85,26.1407910227776)) ;
#11442=CARTESIAN_POINT('Ctrl Pts',(65.4901773259044,41.5,25.5705319285393)) ;
#11443=CARTESIAN_POINT('Ctrl Pts',(65.4901773259044,40.85,25.5705319285393)) ;
#11444=CARTESIAN_POINT('',(65.4901773259044,40.9998395232679,25.5705319285393)) ;
#11445=CARTESIAN_POINT('Ctrl Pts',(65.7032742127776,40.9744759230064,26.3891540408134)) ;
#11446=CARTESIAN_POINT('Ctrl Pts',(65.6506026346571,40.9780032620947,26.3277656634483)) ;
#11447=CARTESIAN_POINT('Ctrl Pts',(65.6114170771088,40.9817382887103,26.2559550399376)) ;
#11448=CARTESIAN_POINT('Ctrl Pts',(65.5095628589581,40.9932219304136,25.9946808285601)) ;
#11449=CARTESIAN_POINT('Ctrl Pts',(65.4901773259044,40.9989319317972,25.7699809219056)) ;
#11450=CARTESIAN_POINT('Ctrl Pts',(65.4901773259044,40.9998395232679,25.5705319285393)) ;
#11451=CARTESIAN_POINT('',(65.4901773259044,40.85,25.5705319285393)) ;
#11452=CARTESIAN_POINT('Ctrl Pts',(65.7032742127776,40.85,26.3891540408134)) ;
#11453=CARTESIAN_POINT('Ctrl Pts',(65.4901773259044,40.85,26.1407910227776)) ;
#11454=CARTESIAN_POINT('Ctrl Pts',(65.4901773259044,40.85,25.5705319285393)) ;
#11455=CARTESIAN_POINT('',(65.4901773259044,41.5,25.5705319285393)) ;
#11456=CARTESIAN_POINT('Ctrl Pts',(65.4901773259044,41.5,25.5705319285393)) ;
#11457=CARTESIAN_POINT('Ctrl Pts',(65.4901773259044,40.85,25.5705319285393)) ;
#11458=CARTESIAN_POINT('Ctrl Pts',(65.4901773259044,41.5,24.9327419638634)) ;
#11459=CARTESIAN_POINT('Ctrl Pts',(65.4901773259044,40.85,24.9327419638634)) ;
#11460=CARTESIAN_POINT('Ctrl Pts',(65.7257843539119,41.5,24.6431103289127)) ;
#11461=CARTESIAN_POINT('Ctrl Pts',(65.7257843539119,40.85,24.6431103289127)) ;
#11462=CARTESIAN_POINT('',(65.7257843539119,40.9762960714631,24.6431103289127)) ;
#11463=CARTESIAN_POINT('Ctrl Pts',(65.4901773259044,40.9998395232679,25.5705319285393)) ;
#11464=CARTESIAN_POINT('Ctrl Pts',(65.4901773259044,41.0006654854803,25.3890214834158)) ;
#11465=CARTESIAN_POINT('Ctrl Pts',(65.5044117837423,40.9980094292655,25.1956347335121)) ;
#11466=CARTESIAN_POINT('Ctrl Pts',(65.5673107019122,40.9903345932874,24.9480044597343)) ;
#11467=CARTESIAN_POINT('Ctrl Pts',(65.5912320855921,40.9876113571461,24.8767797364898)) ;
#11468=CARTESIAN_POINT('Ctrl Pts',(65.6505396584418,40.9819752858246,24.7503534890286)) ;
#11469=CARTESIAN_POINT('Ctrl Pts',(65.6844211051244,40.9791114077331,24.6939581557985)) ;
#11470=CARTESIAN_POINT('Ctrl Pts',(65.7257843539119,40.9762960714631,24.6431103289127)) ;
#11471=CARTESIAN_POINT('',(65.7257843539119,40.85,24.6431103289127)) ;
#11472=CARTESIAN_POINT('Ctrl Pts',(65.4901773259044,40.85,25.5705319285393)) ;
#11473=CARTESIAN_POINT('Ctrl Pts',(65.4901773259044,40.85,24.9327419638634)) ;
#11474=CARTESIAN_POINT('Ctrl Pts',(65.7257843539119,40.85,24.6431103289127)) ;
#11475=CARTESIAN_POINT('',(65.7257843539119,41.5,24.6431103289127)) ;
#11476=CARTESIAN_POINT('Ctrl Pts',(65.7257843539119,41.5,24.6431103289127)) ;
#11477=CARTESIAN_POINT('Ctrl Pts',(65.7257843539119,40.85,24.6431103289127)) ;
#11478=CARTESIAN_POINT('Ctrl Pts',(65.9313779100776,41.5,24.3909957945347)) ;
#11479=CARTESIAN_POINT('Ctrl Pts',(65.9313779100776,40.85,24.3909957945347)) ;
#11480=CARTESIAN_POINT('Ctrl Pts',(66.2795360907912,41.5,24.3909957945347)) ;
#11481=CARTESIAN_POINT('Ctrl Pts',(66.2795360907912,40.85,24.3909957945347)) ;
#11482=CARTESIAN_POINT('',(66.2795360907912,40.9602752133414,24.3909957945347)) ;
#11483=CARTESIAN_POINT('Ctrl Pts',(65.7257843539119,40.9762960714631,24.6431103289127)) ;
#11484=CARTESIAN_POINT('Ctrl Pts',(65.7828697153532,40.9724201852525,24.5731078950428)) ;
#11485=CARTESIAN_POINT('Ctrl Pts',(65.8503581339868,40.9687321451926,24.5150347541818)) ;
#11486=CARTESIAN_POINT('Ctrl Pts',(65.9300081545895,40.9658953545615,24.4723420404865)) ;
#11487=CARTESIAN_POINT('Ctrl Pts',(65.9816166823416,40.9640572811135,24.4446796735105)) ;
#11488=CARTESIAN_POINT('Ctrl Pts',(66.0361961405409,40.9626560029032,24.4246179460631)) ;
#11489=CARTESIAN_POINT('Ctrl Pts',(66.0932472026151,40.9617209739421,24.4113381957841)) ;
#11490=CARTESIAN_POINT('Ctrl Pts',(66.1543031375699,40.9607203077783,24.3971262330306)) ;
#11491=CARTESIAN_POINT('Ctrl Pts',(66.216844930776,40.9602752133414,24.3909957945347)) ;
#11492=CARTESIAN_POINT('Ctrl Pts',(66.2795360907912,40.9602752133414,24.3909957945347)) ;
#11493=CARTESIAN_POINT('',(66.2795360907912,40.85,24.3909957945347)) ;
#11494=CARTESIAN_POINT('Ctrl Pts',(65.7257843539119,40.85,24.6431103289127)) ;
#11495=CARTESIAN_POINT('Ctrl Pts',(65.9313779100776,40.85,24.3909957945347)) ;
#11496=CARTESIAN_POINT('Ctrl Pts',(66.2795360907912,40.85,24.3909957945347)) ;
#11497=CARTESIAN_POINT('',(66.2795360907912,41.5,24.3909957945347)) ;
#11498=CARTESIAN_POINT('Ctrl Pts',(66.2390177473426,41.5,25.4114596486092)) ;
#11499=CARTESIAN_POINT('Ctrl Pts',(66.2390177473426,40.85,25.4114596486092)) ;
#11500=CARTESIAN_POINT('Ctrl Pts',(66.0559344813228,41.5,25.4114596486092)) ;
#11501=CARTESIAN_POINT('Ctrl Pts',(66.0559344813228,40.85,25.4114596486092)) ;
#11502=CARTESIAN_POINT('Ctrl Pts',(65.9283765181899,41.5,25.5427692770958)) ;
#11503=CARTESIAN_POINT('Ctrl Pts',(65.9283765181899,40.85,25.5427692770958)) ;
#11504=CARTESIAN_POINT('',(65.9283765181899,40.9999409930792,25.5427692770958)) ;
#11505=CARTESIAN_POINT('Ctrl Pts',(66.2390177473426,40.9997471142653,25.4114596486092)) ;
#11506=CARTESIAN_POINT('Ctrl Pts',(66.1805248823561,40.9997471142653,25.4114596486092)) ;
#11507=CARTESIAN_POINT('Ctrl Pts',(66.1236953715062,40.9998180096227,25.4215118920112)) ;
#11508=CARTESIAN_POINT('Ctrl Pts',(66.0698158208354,40.9998998728118,25.4442870499013)) ;
#11509=CARTESIAN_POINT('Ctrl Pts',(66.0159384991141,40.9999817326143,25.4670612656033)) ;
#11510=CARTESIAN_POINT('Ctrl Pts',(65.9691314140412,41.0000567563128,25.5008157204395)) ;
#11511=CARTESIAN_POINT('Ctrl Pts',(65.9283765181899,40.9999409930792,25.5427692770958)) ;
#11512=CARTESIAN_POINT('',(65.9283765181899,40.85,25.5427692770958)) ;
#11513=CARTESIAN_POINT('Ctrl Pts',(66.2390177473426,40.85,25.4114596486092)) ;
#11514=CARTESIAN_POINT('Ctrl Pts',(66.0559344813228,40.85,25.4114596486092)) ;
#11515=CARTESIAN_POINT('Ctrl Pts',(65.9283765181899,40.85,25.5427692770958)) ;
#11516=CARTESIAN_POINT('',(65.9283765181899,41.5,25.5427692770958)) ;
#11517=CARTESIAN_POINT('Ctrl Pts',(66.0259208604693,41.5,26.3486356973648)) ;
#11518=CARTESIAN_POINT('Ctrl Pts',(66.0259208604693,40.85,26.3486356973648)) ;
#11519=CARTESIAN_POINT('Ctrl Pts',(66.1324693784118,41.5,26.4154158473015)) ;
#11520=CARTESIAN_POINT('Ctrl Pts',(66.1324693784118,40.85,26.4154158473015)) ;
#11521=CARTESIAN_POINT('Ctrl Pts',(66.2495224699378,41.5,26.4154158473015)) ;
#11522=CARTESIAN_POINT('Ctrl Pts',(66.2495224699378,40.85,26.4154158473015)) ;
#11523=CARTESIAN_POINT('',(66.0259208604693,40.9767508687437,26.3486356973648)) ;
#11524=CARTESIAN_POINT('Ctrl Pts',(66.0259208604693,40.9767508687437,26.3486356973648)) ;
#11525=CARTESIAN_POINT('Ctrl Pts',(66.0600873712772,40.9755766686503,26.370049835812)) ;
#11526=CARTESIAN_POINT('Ctrl Pts',(66.0964354476884,40.9745939178592,26.3871734830869)) ;
#11527=CARTESIAN_POINT('Ctrl Pts',(66.1350841335519,40.973923452691,26.3987174084555)) ;
#11528=CARTESIAN_POINT('Ctrl Pts',(66.1724117020424,40.9732759058487,26.4098667310059)) ;
#11529=CARTESIAN_POINT('Ctrl Pts',(66.2105599112183,40.9729445751773,26.4154158473015)) ;
#11530=CARTESIAN_POINT('Ctrl Pts',(66.2495224699378,40.9729445751773,26.4154158473015)) ;
#11531=CARTESIAN_POINT('',(66.0259208604693,40.85,26.3486356973648)) ;
#11532=CARTESIAN_POINT('',(66.0259208604693,41.5,26.3486356973648)) ;
#11533=CARTESIAN_POINT('Ctrl Pts',(66.0259208604693,40.85,26.3486356973648)) ;
#11534=CARTESIAN_POINT('Ctrl Pts',(66.1324693784118,40.85,26.4154158473015)) ;
#11535=CARTESIAN_POINT('Ctrl Pts',(66.2495224699378,40.85,26.4154158473015)) ;
#11536=CARTESIAN_POINT('Ctrl Pts',(65.8600955232978,41.5,26.1542971372604)) ;
#11537=CARTESIAN_POINT('Ctrl Pts',(65.8600955232978,40.85,26.1542971372604)) ;
#11538=CARTESIAN_POINT('Ctrl Pts',(65.9193723425269,41.5,26.2818552494049)) ;
#11539=CARTESIAN_POINT('Ctrl Pts',(65.9193723425269,40.85,26.2818552494049)) ;
#11540=CARTESIAN_POINT('Ctrl Pts',(66.0259208604693,41.5,26.3486356973648)) ;
#11541=CARTESIAN_POINT('Ctrl Pts',(66.0259208604693,40.85,26.3486356973648)) ;
#11542=CARTESIAN_POINT('',(65.8600955232978,40.9861840120855,26.1542971372604)) ;
#11543=CARTESIAN_POINT('Ctrl Pts',(65.8600955232978,40.9861840120855,26.1542971372604)) ;
#11544=CARTESIAN_POINT('Ctrl Pts',(65.8788862094647,40.9844755850496,26.1947329177985)) ;
#11545=CARTESIAN_POINT('Ctrl Pts',(65.9022260091426,40.9827093371832,26.232710898843)) ;
#11546=CARTESIAN_POINT('Ctrl Pts',(65.9311684027272,40.9810293733619,26.2666352073223)) ;
#11547=CARTESIAN_POINT('Ctrl Pts',(65.9585896197335,40.9794377063709,26.2987764959093)) ;
#11548=CARTESIAN_POINT('Ctrl Pts',(65.9901116541869,40.977981528826,26.3261918860119)) ;
#11549=CARTESIAN_POINT('Ctrl Pts',(66.0259208604693,40.9767508687437,26.3486356973648)) ;
#11550=CARTESIAN_POINT('',(65.8600955232978,40.85,26.1542971372604)) ;
#11551=CARTESIAN_POINT('',(65.8600955232978,41.5,26.1542971372604)) ;
#11552=CARTESIAN_POINT('Ctrl Pts',(65.8600955232978,40.85,26.1542971372604)) ;
#11553=CARTESIAN_POINT('Ctrl Pts',(65.9193723425269,40.85,26.2818552494049)) ;
#11554=CARTESIAN_POINT('Ctrl Pts',(66.0259208604693,40.85,26.3486356973648)) ;
#11555=CARTESIAN_POINT('Ctrl Pts',(65.800818555057,41.5,25.8871759414673)) ;
#11556=CARTESIAN_POINT('Ctrl Pts',(65.800818555057,40.85,25.8871759414673)) ;
#11557=CARTESIAN_POINT('Ctrl Pts',(65.800818555057,41.5,26.0267393231392)) ;
#11558=CARTESIAN_POINT('Ctrl Pts',(65.800818555057,40.85,26.0267393231392)) ;
#11559=CARTESIAN_POINT('Ctrl Pts',(65.8600955232978,41.5,26.1542971372604)) ;
#11560=CARTESIAN_POINT('Ctrl Pts',(65.8600955232978,40.85,26.1542971372604)) ;
#11561=CARTESIAN_POINT('',(65.800818555057,40.995163593533,25.8871759414673)) ;
#11562=CARTESIAN_POINT('Ctrl Pts',(65.800818555057,40.995163593533,25.8871759414673)) ;
#11563=CARTESIAN_POINT('Ctrl Pts',(65.800818555057,40.9940128045926,25.9332316514998)) ;
#11564=CARTESIAN_POINT('Ctrl Pts',(65.8056599512512,40.9926693613796,25.9787682477252)) ;
#11565=CARTESIAN_POINT('Ctrl Pts',(65.8156338342756,40.9911496437811,26.0237200721573)) ;
#11566=CARTESIAN_POINT('Ctrl Pts',(65.8256508107933,40.9896233600398,26.068866116949)) ;
#11567=CARTESIAN_POINT('Ctrl Pts',(65.8406108493885,40.9879555270766,26.1123681640607)) ;
#11568=CARTESIAN_POINT('Ctrl Pts',(65.8600955232978,40.9861840120855,26.1542971372604)) ;
#11569=CARTESIAN_POINT('',(65.800818555057,40.85,25.8871759414673)) ;
#11570=CARTESIAN_POINT('',(65.800818555057,41.5,25.8871759414673)) ;
#11571=CARTESIAN_POINT('Ctrl Pts',(65.800818555057,40.85,25.8871759414673)) ;
#11572=CARTESIAN_POINT('Ctrl Pts',(65.800818555057,40.85,26.0267393231392)) ;
#11573=CARTESIAN_POINT('Ctrl Pts',(65.8600955232978,40.85,26.1542971372604)) ;
#11574=CARTESIAN_POINT('Ctrl Pts',(65.9283765181899,41.5,25.5427692770958)) ;
#11575=CARTESIAN_POINT('Ctrl Pts',(65.9283765181899,40.85,25.5427692770958)) ;
#11576=CARTESIAN_POINT('Ctrl Pts',(65.800818555057,41.5,25.6740789055824)) ;
#11577=CARTESIAN_POINT('Ctrl Pts',(65.800818555057,40.85,25.6740789055824)) ;
#11578=CARTESIAN_POINT('Ctrl Pts',(65.800818555057,41.5,25.8871759414673)) ;
#11579=CARTESIAN_POINT('Ctrl Pts',(65.800818555057,40.85,25.8871759414673)) ;
#11580=CARTESIAN_POINT('Ctrl Pts',(65.9283765181899,40.9999409930792,25.5427692770958)) ;
#11581=CARTESIAN_POINT('Ctrl Pts',(65.8879994387808,40.9998263030235,25.5843339051784)) ;
#11582=CARTESIAN_POINT('Ctrl Pts',(65.8571868924283,40.9995311591319,25.63206654485)) ;
#11583=CARTESIAN_POINT('Ctrl Pts',(65.8359691306507,40.998884127952,25.6859859895723)) ;
#11584=CARTESIAN_POINT('Ctrl Pts',(65.8107777994687,40.9981159236094,25.7500032315125)) ;
#11585=CARTESIAN_POINT('Ctrl Pts',(65.800818555057,40.9968816429754,25.8184179058545)) ;
#11586=CARTESIAN_POINT('Ctrl Pts',(65.800818555057,40.995163593533,25.8871759414673)) ;
#11587=CARTESIAN_POINT('Ctrl Pts',(65.9283765181899,40.85,25.5427692770958)) ;
#11588=CARTESIAN_POINT('Ctrl Pts',(65.800818555057,40.85,25.6740789055824)) ;
#11589=CARTESIAN_POINT('Ctrl Pts',(65.800818555057,40.85,25.8871759414673)) ;
#11590=CARTESIAN_POINT('Ctrl Pts',(66.2795360907912,41.5,24.3909957945347)) ;
#11591=CARTESIAN_POINT('Ctrl Pts',(66.2795360907912,40.85,24.3909957945347)) ;
#11592=CARTESIAN_POINT('Ctrl Pts',(66.5391542539001,41.5,24.3909957945347)) ;
#11593=CARTESIAN_POINT('Ctrl Pts',(66.5391542539001,40.85,24.3909957945347)) ;
#11594=CARTESIAN_POINT('Ctrl Pts',(66.70497944206,41.5,24.5365619599819)) ;
#11595=CARTESIAN_POINT('Ctrl Pts',(66.70497944206,40.85,24.5365619599819)) ;
#11596=CARTESIAN_POINT('',(66.70497944206,40.9700286729872,24.5365619599819)) ;
#11597=CARTESIAN_POINT('Ctrl Pts',(66.2795360907912,40.9602752133414,24.3909957945347)) ;
#11598=CARTESIAN_POINT('Ctrl Pts',(66.3597536157927,40.9602752133414,24.3909957945347)) ;
#11599=CARTESIAN_POINT('Ctrl Pts',(66.4398014503548,40.9610411641504,24.4014174188477)) ;
#11600=CARTESIAN_POINT('Ctrl Pts',(66.51569958686,40.9628424734339,24.427385138193)) ;
#11601=CARTESIAN_POINT('Ctrl Pts',(66.5859662839039,40.964510130369,24.4514261219665)) ;
#11602=CARTESIAN_POINT('Ctrl Pts',(66.6492016541882,40.9669793466799,24.4875985980963)) ;
#11603=CARTESIAN_POINT('Ctrl Pts',(66.70497944206,40.9700286729872,24.5365619599819)) ;
#11604=CARTESIAN_POINT('',(66.70497944206,40.85,24.5365619599819)) ;
#11605=CARTESIAN_POINT('Ctrl Pts',(66.2795360907912,40.85,24.3909957945347)) ;
#11606=CARTESIAN_POINT('Ctrl Pts',(66.5391542539001,40.85,24.3909957945347)) ;
#11607=CARTESIAN_POINT('Ctrl Pts',(66.70497944206,40.85,24.5365619599819)) ;
#11608=CARTESIAN_POINT('',(66.70497944206,41.5,24.5365619599819)) ;
#11609=CARTESIAN_POINT('Ctrl Pts',(65.9974079355597,41.5,25.2448838889599)) ;
#11610=CARTESIAN_POINT('Ctrl Pts',(65.9974079355597,40.85,25.2448838889599)) ;
#11611=CARTESIAN_POINT('Ctrl Pts',(66.1384720131755,41.5,25.172851228714)) ;
#11612=CARTESIAN_POINT('Ctrl Pts',(66.1384720131755,40.85,25.172851228714)) ;
#11613=CARTESIAN_POINT('Ctrl Pts',(66.2930422052741,41.5,25.172851228714)) ;
#11614=CARTESIAN_POINT('Ctrl Pts',(66.2930422052741,40.85,25.172851228714)) ;
#11615=CARTESIAN_POINT('',(65.9974079355597,40.9979003664976,25.2448838889599)) ;
#11616=CARTESIAN_POINT('Ctrl Pts',(65.9974079355597,40.9979003664976,25.2448838889599)) ;
#11617=CARTESIAN_POINT('Ctrl Pts',(66.0434771360032,40.9975131189137,25.2213592105341)) ;
#11618=CARTESIAN_POINT('Ctrl Pts',(66.0915879306606,40.9971611542325,25.2031057712063)) ;
#11619=CARTESIAN_POINT('Ctrl Pts',(66.1418468502283,40.9969168656354,25.1908598059363)) ;
#11620=CARTESIAN_POINT('Ctrl Pts',(66.1915089745217,40.9966754778225,25.1787592543414)) ;
#11621=CARTESIAN_POINT('Ctrl Pts',(66.2419264991158,40.9965471535257,25.172851228714)) ;
#11622=CARTESIAN_POINT('Ctrl Pts',(66.2930422052741,40.9965471535257,25.172851228714)) ;
#11623=CARTESIAN_POINT('',(65.9974079355597,40.85,25.2448838889599)) ;
#11624=CARTESIAN_POINT('',(65.9974079355597,41.5,25.2448838889599)) ;
#11625=CARTESIAN_POINT('Ctrl Pts',(65.9974079355597,40.85,25.2448838889599)) ;
#11626=CARTESIAN_POINT('Ctrl Pts',(66.1384720131755,40.85,25.172851228714)) ;
#11627=CARTESIAN_POINT('Ctrl Pts',(66.2930422052741,40.85,25.172851228714)) ;
#11628=CARTESIAN_POINT('Ctrl Pts',(65.758799366653,41.5,25.4654841065407)) ;
#11629=CARTESIAN_POINT('Ctrl Pts',(65.758799366653,40.85,25.4654841065407)) ;
#11630=CARTESIAN_POINT('Ctrl Pts',(65.8563437089324,41.5,25.3169166982174)) ;
#11631=CARTESIAN_POINT('Ctrl Pts',(65.8563437089324,40.85,25.3169166982174)) ;
#11632=CARTESIAN_POINT('Ctrl Pts',(65.9974079355597,41.5,25.2448838889599)) ;
#11633=CARTESIAN_POINT('Ctrl Pts',(65.9974079355597,40.85,25.2448838889599)) ;
#11634=CARTESIAN_POINT('',(65.758799366653,40.9999615694072,25.4654841065407)) ;
#11635=CARTESIAN_POINT('Ctrl Pts',(65.758799366653,40.9999615694072,25.4654841065407)) ;
#11636=CARTESIAN_POINT('Ctrl Pts',(65.7898404317904,40.9998562892375,25.4182062174156)) ;
#11637=CARTESIAN_POINT('Ctrl Pts',(65.8256934781911,40.9995390458235,25.3744462358198)) ;
#11638=CARTESIAN_POINT('Ctrl Pts',(65.8672232792857,40.9991328993943,25.3360507184735)) ;
#11639=CARTESIAN_POINT('Ctrl Pts',(65.9064830807812,40.9987489527399,25.2997538822354)) ;
#11640=CARTESIAN_POINT('Ctrl Pts',(65.949789164042,40.998300639841,25.2691998616755)) ;
#11641=CARTESIAN_POINT('Ctrl Pts',(65.9974079355597,40.9979003664976,25.2448838889599)) ;
#11642=CARTESIAN_POINT('',(65.758799366653,40.85,25.4654841065407)) ;
#11643=CARTESIAN_POINT('',(65.758799366653,41.5,25.4654841065407)) ;
#11644=CARTESIAN_POINT('Ctrl Pts',(65.758799366653,40.85,25.4654841065407)) ;
#11645=CARTESIAN_POINT('Ctrl Pts',(65.8563437089324,40.85,25.3169166982174)) ;
#11646=CARTESIAN_POINT('Ctrl Pts',(65.9974079355597,40.85,25.2448838889599)) ;
#11647=CARTESIAN_POINT('Ctrl Pts',(65.835334263742,41.5,24.9567529499531)) ;
#11648=CARTESIAN_POINT('Ctrl Pts',(65.835334263742,40.85,24.9567529499531)) ;
#11649=CARTESIAN_POINT('Ctrl Pts',(65.7618007585406,41.5,25.1353341281414)) ;
#11650=CARTESIAN_POINT('Ctrl Pts',(65.7618007585406,40.85,25.1353341281414)) ;
#11651=CARTESIAN_POINT('Ctrl Pts',(65.758799366653,41.5,25.4654841065407)) ;
#11652=CARTESIAN_POINT('Ctrl Pts',(65.758799366653,40.85,25.4654841065407)) ;
#11653=CARTESIAN_POINT('',(65.835334263742,40.9904771599398,24.9567529499531)) ;
#11654=CARTESIAN_POINT('Ctrl Pts',(65.835334263742,40.9904771599398,24.9567529499531)) ;
#11655=CARTESIAN_POINT('Ctrl Pts',(65.8204030637459,40.9917488395531,24.9930143967556)) ;
#11656=CARTESIAN_POINT('Ctrl Pts',(65.8085450275128,40.9929650207556,25.0318073588892)) ;
#11657=CARTESIAN_POINT('Ctrl Pts',(65.7990827857526,40.9940545364855,25.0711309699265)) ;
#11658=CARTESIAN_POINT('Ctrl Pts',(65.7908915214191,40.9949977074132,25.1051725956554)) ;
#11659=CARTESIAN_POINT('Ctrl Pts',(65.7844937127903,40.9958459552111,25.1396076926084)) ;
#11660=CARTESIAN_POINT('Ctrl Pts',(65.7794477485054,40.9965531109567,25.1731335451618)) ;
#11661=CARTESIAN_POINT('Ctrl Pts',(65.7697518635822,40.9979119197681,25.2375538997173)) ;
#11662=CARTESIAN_POINT('Ctrl Pts',(65.7641154541389,40.9988966859177,25.3048486747571)) ;
#11663=CARTESIAN_POINT('Ctrl Pts',(65.7612165577635,40.9994566523273,25.3714502213717)) ;
#11664=CARTESIAN_POINT('Ctrl Pts',(65.7598399751179,40.9997225604323,25.4030769238695)) ;
#11665=CARTESIAN_POINT('Ctrl Pts',(65.7590806144596,40.9998926778167,25.4345471410405)) ;
#11666=CARTESIAN_POINT('Ctrl Pts',(65.758799366653,40.9999615694072,25.4654841065407)) ;
#11667=CARTESIAN_POINT('',(65.835334263742,40.85,24.9567529499531)) ;
#11668=CARTESIAN_POINT('',(65.835334263742,41.5,24.9567529499531)) ;
#11669=CARTESIAN_POINT('Ctrl Pts',(65.835334263742,40.85,24.9567529499531)) ;
#11670=CARTESIAN_POINT('Ctrl Pts',(65.7618007585406,40.85,25.1353341281414)) ;
#11671=CARTESIAN_POINT('Ctrl Pts',(65.758799366653,40.85,25.4654841065407)) ;
#11672=CARTESIAN_POINT('Ctrl Pts',(66.0364255830646,41.5,24.6851295173168)) ;
#11673=CARTESIAN_POINT('Ctrl Pts',(66.0364255830646,40.85,24.6851295173168)) ;
#11674=CARTESIAN_POINT('Ctrl Pts',(65.9088676199317,41.5,24.7781717717648)) ;
#11675=CARTESIAN_POINT('Ctrl Pts',(65.9088676199317,40.85,24.7781717717648)) ;
#11676=CARTESIAN_POINT('Ctrl Pts',(65.835334263742,41.5,24.9567529499531)) ;
#11677=CARTESIAN_POINT('Ctrl Pts',(65.835334263742,40.85,24.9567529499531)) ;
#11678=CARTESIAN_POINT('',(66.0364255830646,40.9785653759143,24.6851295173168)) ;
#11679=CARTESIAN_POINT('Ctrl Pts',(66.0364255830646,40.9785653759143,24.6851295173168)) ;
#11680=CARTESIAN_POINT('Ctrl Pts',(65.9924837093702,40.9802527411659,24.717181228498)) ;
#11681=CARTESIAN_POINT('Ctrl Pts',(65.9547589853903,40.9821868075603,24.7558189502039)) ;
#11682=CARTESIAN_POINT('Ctrl Pts',(65.922400046105,40.9841638195929,24.7995210152964)) ;
#11683=CARTESIAN_POINT('Ctrl Pts',(65.8866774648815,40.9863463377616,24.8477658157868)) ;
#11684=CARTESIAN_POINT('Ctrl Pts',(65.8581900211715,40.9885305474988,24.9012460575488)) ;
#11685=CARTESIAN_POINT('Ctrl Pts',(65.835334263742,40.9904771599398,24.9567529499531)) ;
#11686=CARTESIAN_POINT('',(66.0364255830646,40.85,24.6851295173168)) ;
#11687=CARTESIAN_POINT('',(66.0364255830646,41.5,24.6851295173168)) ;
#11688=CARTESIAN_POINT('Ctrl Pts',(66.0364255830646,40.85,24.6851295173168)) ;
#11689=CARTESIAN_POINT('Ctrl Pts',(65.9088676199317,40.85,24.7781717717648)) ;
#11690=CARTESIAN_POINT('Ctrl Pts',(65.835334263742,40.85,24.9567529499531)) ;
#11691=CARTESIAN_POINT('Ctrl Pts',(66.2630285844207,41.5,24.6130967080593)) ;
#11692=CARTESIAN_POINT('Ctrl Pts',(66.2630285844207,40.85,24.6130967080593)) ;
#11693=CARTESIAN_POINT('Ctrl Pts',(66.133969925344,41.5,24.6130967080593)) ;
#11694=CARTESIAN_POINT('Ctrl Pts',(66.133969925344,40.85,24.6130967080593)) ;
#11695=CARTESIAN_POINT('Ctrl Pts',(66.0364255830646,41.5,24.6851295173168)) ;
#11696=CARTESIAN_POINT('Ctrl Pts',(66.0364255830646,40.85,24.6851295173168)) ;
#11697=CARTESIAN_POINT('',(66.2630285844207,40.9746050854535,24.6130967080593)) ;
#11698=CARTESIAN_POINT('Ctrl Pts',(66.2630285844207,40.9746050854535,24.6130967080593)) ;
#11699=CARTESIAN_POINT('Ctrl Pts',(66.2217889884937,40.9746050854535,24.6130967080593)) ;
#11700=CARTESIAN_POINT('Ctrl Pts',(66.1811469291785,40.9749253007144,24.618612753171)) ;
#11701=CARTESIAN_POINT('Ctrl Pts',(66.1418490530652,40.975626676171,24.6311047360094)) ;
#11702=CARTESIAN_POINT('Ctrl Pts',(66.1037031127777,40.9763074922591,24.6432305422503)) ;
#11703=CARTESIAN_POINT('Ctrl Pts',(66.0686131950993,40.9773140371269,24.661360182633)) ;
#11704=CARTESIAN_POINT('Ctrl Pts',(66.0364255830646,40.9785653759143,24.6851295173168)) ;
#11705=CARTESIAN_POINT('',(66.2630285844207,40.85,24.6130967080593)) ;
#11706=CARTESIAN_POINT('',(66.2630285844207,41.5,24.6130967080593)) ;
#11707=CARTESIAN_POINT('Ctrl Pts',(66.2630285844207,40.85,24.6130967080593)) ;
#11708=CARTESIAN_POINT('Ctrl Pts',(66.133969925344,40.85,24.6130967080593)) ;
#11709=CARTESIAN_POINT('Ctrl Pts',(66.0364255830646,40.85,24.6851295173168)) ;
#11710=CARTESIAN_POINT('Ctrl Pts',(66.5331514701247,41.5,24.7286492526531)) ;
#11711=CARTESIAN_POINT('Ctrl Pts',(66.5331514701247,40.85,24.7286492526531)) ;
#11712=CARTESIAN_POINT('Ctrl Pts',(66.4236017093062,41.5,24.6130967080593)) ;
#11713=CARTESIAN_POINT('Ctrl Pts',(66.4236017093062,40.85,24.6130967080593)) ;
#11714=CARTESIAN_POINT('Ctrl Pts',(66.2630285844207,41.5,24.6130967080593)) ;
#11715=CARTESIAN_POINT('Ctrl Pts',(66.2630285844207,40.85,24.6130967080593)) ;
#11716=CARTESIAN_POINT('',(66.5331514701247,40.9807951354111,24.7286492526531)) ;
#11717=CARTESIAN_POINT('Ctrl Pts',(66.5331514701247,40.9807951354111,24.7286492526531)) ;
#11718=CARTESIAN_POINT('Ctrl Pts',(66.4991519463673,40.9790082382666,24.6927867235541)) ;
#11719=CARTESIAN_POINT('Ctrl Pts',(66.4599857285765,40.9774358576459,24.6637099460066)) ;
#11720=CARTESIAN_POINT('Ctrl Pts',(66.4147776930977,40.9763284909537,24.6436960585779)) ;
#11721=CARTESIAN_POINT('Ctrl Pts',(66.3914684127497,40.9757575322645,24.6333768905808)) ;
#11722=CARTESIAN_POINT('Ctrl Pts',(66.3672753064892,40.9753279903153,24.6257865971459)) ;
#11723=CARTESIAN_POINT('Ctrl Pts',(66.3422822541488,40.9750416415541,24.6207467986028)) ;
#11724=CARTESIAN_POINT('Ctrl Pts',(66.3161714606551,40.9747424866822,24.615481609813)) ;
#11725=CARTESIAN_POINT('Ctrl Pts',(66.2896659598749,40.9746050854535,24.6130967080593)) ;
#11726=CARTESIAN_POINT('Ctrl Pts',(66.2630285844207,40.9746050854535,24.6130967080593)) ;
#11727=CARTESIAN_POINT('',(66.5331514701247,40.85,24.7286492526531)) ;
#11728=CARTESIAN_POINT('',(66.5331514701247,41.5,24.7286492526531)) ;
#11729=CARTESIAN_POINT('Ctrl Pts',(66.5331514701247,40.85,24.7286492526531)) ;
#11730=CARTESIAN_POINT('Ctrl Pts',(66.4236017093062,40.85,24.6130967080593)) ;
#11731=CARTESIAN_POINT('Ctrl Pts',(66.2630285844207,40.85,24.6130967080593)) ;
#11732=CARTESIAN_POINT('Ctrl Pts',(66.6351976022124,41.5,24.9597543418407)) ;
#11733=CARTESIAN_POINT('Ctrl Pts',(66.6351976022124,40.85,24.9597543418407)) ;
#11734=CARTESIAN_POINT('Ctrl Pts',(66.5991814956069,41.5,24.8006820619106)) ;
#11735=CARTESIAN_POINT('Ctrl Pts',(66.5991814956069,40.85,24.8006820619106)) ;
#11736=CARTESIAN_POINT('Ctrl Pts',(66.5331514701247,41.5,24.7286492526531)) ;
#11737=CARTESIAN_POINT('Ctrl Pts',(66.5331514701247,40.85,24.7286492526531)) ;
#11738=CARTESIAN_POINT('',(66.6351976022124,40.990582126855,24.9597543418407)) ;
#11739=CARTESIAN_POINT('Ctrl Pts',(66.6351976022124,40.990582126855,24.9597543418407)) ;
#11740=CARTESIAN_POINT('Ctrl Pts',(66.6255826971324,40.9891010885524,24.9172882060882)) ;
#11741=CARTESIAN_POINT('Ctrl Pts',(66.6129385031804,40.987370907003,24.8731722925374)) ;
#11742=CARTESIAN_POINT('Ctrl Pts',(66.5960584064866,40.9856269527389,24.8326553272909)) ;
#11743=CARTESIAN_POINT('Ctrl Pts',(66.5946335153935,40.9854797412068,24.8292351891278)) ;
#11744=CARTESIAN_POINT('Ctrl Pts',(66.5931784586585,40.9853324315375,24.8258406454158)) ;
#11745=CARTESIAN_POINT('Ctrl Pts',(66.5916925287781,40.9851851653016,24.8224748002298)) ;
#11746=CARTESIAN_POINT('Ctrl Pts',(66.579173590795,40.9839444493707,24.7941176026917)) ;
#11747=CARTESIAN_POINT('Ctrl Pts',(66.5635747988376,40.9826176783275,24.7657800092439)) ;
#11748=CARTESIAN_POINT('Ctrl Pts',(66.5440341374292,40.9814230256515,24.7413666657469)) ;
#11749=CARTESIAN_POINT('Ctrl Pts',(66.5405345731193,40.9812090736373,24.7369944460047)) ;
#11750=CARTESIAN_POINT('Ctrl Pts',(66.5369086215402,40.9809993591517,24.7327479663714)) ;
#11751=CARTESIAN_POINT('Ctrl Pts',(66.5331514701247,40.9807951354111,24.7286492526531)) ;
#11752=CARTESIAN_POINT('',(66.6351976022124,40.85,24.9597543418407)) ;
#11753=CARTESIAN_POINT('',(66.6351976022124,41.5,24.9597543418407)) ;
#11754=CARTESIAN_POINT('Ctrl Pts',(66.6351976022124,40.85,24.9597543418407)) ;
#11755=CARTESIAN_POINT('Ctrl Pts',(66.5991814956069,40.85,24.8006820619106)) ;
#11756=CARTESIAN_POINT('Ctrl Pts',(66.5331514701247,40.85,24.7286492526531)) ;
#11757=CARTESIAN_POINT('Origin',(66.9038199409842,41.5,24.9387447476387)) ;
#11758=CARTESIAN_POINT('',(66.9038199409842,40.9898351360399,24.9387447476387)) ;
#11759=CARTESIAN_POINT('Origin',(59.7277794574127,25.5,25.5)) ;
#11760=CARTESIAN_POINT('',(66.9038199409842,40.85,24.9387447476387)) ;
#11761=CARTESIAN_POINT('',(66.9038199409842,41.5,24.9387447476387)) ;
#11762=CARTESIAN_POINT('',(66.9038199409842,40.85,24.9387447476387)) ;
#11763=CARTESIAN_POINT('Ctrl Pts',(66.70497944206,41.5,24.5365619599819)) ;
#11764=CARTESIAN_POINT('Ctrl Pts',(66.70497944206,40.85,24.5365619599819)) ;
#11765=CARTESIAN_POINT('Ctrl Pts',(66.8708049282432,41.5,24.6821281254292)) ;
#11766=CARTESIAN_POINT('Ctrl Pts',(66.8708049282432,40.85,24.6821281254292)) ;
#11767=CARTESIAN_POINT('Ctrl Pts',(66.9038199409842,41.5,24.9387447476387)) ;
#11768=CARTESIAN_POINT('Ctrl Pts',(66.9038199409842,40.85,24.9387447476387)) ;
#11769=CARTESIAN_POINT('Ctrl Pts',(66.70497944206,40.9700286729872,24.5365619599819)) ;
#11770=CARTESIAN_POINT('Ctrl Pts',(66.7606666603835,40.9730730424596,24.5854457294335)) ;
#11771=CARTESIAN_POINT('Ctrl Pts',(66.8046639769613,40.9764505641981,24.6433213282491)) ;
#11772=CARTESIAN_POINT('Ctrl Pts',(66.8375183760913,40.9798404114639,24.7097210393724)) ;
#11773=CARTESIAN_POINT('Ctrl Pts',(66.8730210352428,40.9835035005855,24.781472962226)) ;
#11774=CARTESIAN_POINT('Ctrl Pts',(66.8936025795082,40.9869575673714,24.8593280044003)) ;
#11775=CARTESIAN_POINT('Ctrl Pts',(66.9038199409842,40.9898351360399,24.9387447476387)) ;
#11776=CARTESIAN_POINT('Ctrl Pts',(66.70497944206,40.85,24.5365619599819)) ;
#11777=CARTESIAN_POINT('Ctrl Pts',(66.8708049282432,40.85,24.6821281254292)) ;
#11778=CARTESIAN_POINT('Ctrl Pts',(66.9038199409842,40.85,24.9387447476387)) ;
#11779=CARTESIAN_POINT('Origin',(65.4714187197387,40.85,25.5142562776804)) ;
#11780=CARTESIAN_POINT('Ctrl Pts',(64.2843792364001,41.5,25.0648020148277)) ;
#11781=CARTESIAN_POINT('Ctrl Pts',(64.2843792364001,40.85,25.0648020148277)) ;
#11782=CARTESIAN_POINT('Ctrl Pts',(64.1260573044419,41.5,25.1578442692757)) ;
#11783=CARTESIAN_POINT('Ctrl Pts',(64.1260573044419,40.85,25.1578442692757)) ;
#11784=CARTESIAN_POINT('Ctrl Pts',(64.,41.5,25.2043653964996)) ;
#11785=CARTESIAN_POINT('Ctrl Pts',(64.,40.85,25.2043653964996)) ;
#11786=CARTESIAN_POINT('',(64.2843792364001,40.9938892055449,25.0648020148277)) ;
#11787=CARTESIAN_POINT('',(64.,40.9971803945496,25.2043653964996)) ;
#11788=CARTESIAN_POINT('Ctrl Pts',(64.2843792364001,40.9938892055449,25.0648020148277)) ;
#11789=CARTESIAN_POINT('Ctrl Pts',(64.2355786561281,40.9946947519433,25.0934810231668)) ;
#11790=CARTESIAN_POINT('Ctrl Pts',(64.1849598543689,40.9953922950403,25.1212649766542)) ;
#11791=CARTESIAN_POINT('Ctrl Pts',(64.1341309103538,40.9959618246374,25.1462103317239)) ;
#11792=CARTESIAN_POINT('Ctrl Pts',(64.0907067039323,40.9964483854203,25.1675216587403)) ;
#11793=CARTESIAN_POINT('Ctrl Pts',(64.0453985127022,40.9968607800921,25.1876111909853)) ;
#11794=CARTESIAN_POINT('Ctrl Pts',(64.,40.9971803945496,25.2043653964996)) ;
#11795=CARTESIAN_POINT('',(64.2843792364001,40.85,25.0648020148277)) ;
#11796=CARTESIAN_POINT('',(64.2843792364001,41.5,25.0648020148277)) ;
#11797=CARTESIAN_POINT('',(64.,40.85,25.2043653964996)) ;
#11798=CARTESIAN_POINT('Ctrl Pts',(64.2843792364001,40.85,25.0648020148277)) ;
#11799=CARTESIAN_POINT('Ctrl Pts',(64.1260573044419,40.85,25.1578442692757)) ;
#11800=CARTESIAN_POINT('Ctrl Pts',(64.,40.85,25.2043653964996)) ;
#11801=CARTESIAN_POINT('',(64.,41.5,25.2043653964996)) ;
#11802=CARTESIAN_POINT('Origin',(64.,41.5,25.2043653964996)) ;
#11803=CARTESIAN_POINT('',(64.,40.9899976032232,24.9432466864586)) ;
#11804=CARTESIAN_POINT('Origin',(64.,25.5,25.5)) ;
#11805=CARTESIAN_POINT('',(64.,40.85,24.9432466864586)) ;
#11806=CARTESIAN_POINT('',(64.,40.85,25.2043653964996)) ;
#11807=CARTESIAN_POINT('',(64.,41.5,24.9432466864586)) ;
#11808=CARTESIAN_POINT('Ctrl Pts',(64.,41.5,24.9432466864586)) ;
#11809=CARTESIAN_POINT('Ctrl Pts',(64.,40.85,24.9432466864586)) ;
#11810=CARTESIAN_POINT('Ctrl Pts',(64.2266030013561,41.5,24.8366983175278)) ;
#11811=CARTESIAN_POINT('Ctrl Pts',(64.2266030013561,40.85,24.8366983175278)) ;
#11812=CARTESIAN_POINT('Ctrl Pts',(64.3961801156402,41.5,24.6851293683052)) ;
#11813=CARTESIAN_POINT('Ctrl Pts',(64.3961801156402,40.85,24.6851293683052)) ;
#11814=CARTESIAN_POINT('',(64.3961801156402,40.9785653680695,24.6851293683052)) ;
#11815=CARTESIAN_POINT('Ctrl Pts',(64.,40.9899976032232,24.9432466864586)) ;
#11816=CARTESIAN_POINT('Ctrl Pts',(64.0733426948616,40.9887580948318,24.9087610685995)) ;
#11817=CARTESIAN_POINT('Ctrl Pts',(64.1444161728547,40.9872424953141,24.8696983737347)) ;
#11818=CARTESIAN_POINT('Ctrl Pts',(64.2123120711965,40.9853157337165,24.8254656219949)) ;
#11819=CARTESIAN_POINT('Ctrl Pts',(64.2770804763103,40.9834777246651,24.7832703664057)) ;
#11820=CARTESIAN_POINT('Ctrl Pts',(64.3385649661852,40.9812764188499,24.7366261029859)) ;
#11821=CARTESIAN_POINT('Ctrl Pts',(64.3961801156402,40.9785653680695,24.6851293683052)) ;
#11822=CARTESIAN_POINT('',(64.3961801156402,40.85,24.6851293683052)) ;
#11823=CARTESIAN_POINT('Ctrl Pts',(64.,40.85,24.9432466864586)) ;
#11824=CARTESIAN_POINT('Ctrl Pts',(64.2266030013561,40.85,24.8366983175278)) ;
#11825=CARTESIAN_POINT('Ctrl Pts',(64.3961801156402,40.85,24.6851293683052)) ;
#11826=CARTESIAN_POINT('',(64.3961801156402,41.5,24.6851293683052)) ;
#11827=CARTESIAN_POINT('Ctrl Pts',(64.3961801156402,41.5,24.6851293683052)) ;
#11828=CARTESIAN_POINT('Ctrl Pts',(64.3961801156402,40.85,24.6851293683052)) ;
#11829=CARTESIAN_POINT('Ctrl Pts',(64.5657571181655,41.5,24.5335605680943)) ;
#11830=CARTESIAN_POINT('Ctrl Pts',(64.5657571181655,40.85,24.5335605680943)) ;
#11831=CARTESIAN_POINT('Ctrl Pts',(64.6362892314792,41.5,24.3909957945347)) ;
#11832=CARTESIAN_POINT('Ctrl Pts',(64.6362892314792,40.85,24.3909957945347)) ;
#11833=CARTESIAN_POINT('',(64.6362892314792,40.9602752133414,24.3909957945347)) ;
#11834=CARTESIAN_POINT('Ctrl Pts',(64.3961801156402,40.9785653680695,24.6851293683052)) ;
#11835=CARTESIAN_POINT('Ctrl Pts',(64.4474761123885,40.9761516625032,24.6392807416224)) ;
#11836=CARTESIAN_POINT('Ctrl Pts',(64.4974059529476,40.9733088517611,24.5891960070225)) ;
#11837=CARTESIAN_POINT('Ctrl Pts',(64.5409178996485,40.969987876403,24.5359071082398)) ;
#11838=CARTESIAN_POINT('Ctrl Pts',(64.5773705983453,40.9672056861476,24.491263640905)) ;
#11839=CARTESIAN_POINT('Ctrl Pts',(64.6107423855321,40.9639792782932,24.4426329869638)) ;
#11840=CARTESIAN_POINT('Ctrl Pts',(64.6362892314792,40.9602752133414,24.3909957945347)) ;
#11841=CARTESIAN_POINT('',(64.6362892314792,40.85,24.3909957945347)) ;
#11842=CARTESIAN_POINT('Ctrl Pts',(64.3961801156402,40.85,24.6851293683052)) ;
#11843=CARTESIAN_POINT('Ctrl Pts',(64.5657571181655,40.85,24.5335605680943)) ;
#11844=CARTESIAN_POINT('Ctrl Pts',(64.6362892314792,40.85,24.3909957945347)) ;
#11845=CARTESIAN_POINT('',(64.6362892314792,41.5,24.3909957945347)) ;
#11846=CARTESIAN_POINT('Origin',(64.6362892314792,41.5,24.3909957945347)) ;
#11847=CARTESIAN_POINT('',(64.810368321836,40.9602752133414,24.3909957945347)) ;
#11848=CARTESIAN_POINT('',(55.25,40.9602752133414,24.3909957945347)) ;
#11849=CARTESIAN_POINT('',(64.810368321836,40.85,24.3909957945347)) ;
#11850=CARTESIAN_POINT('',(64.6362892314792,40.85,24.3909957945347)) ;
#11851=CARTESIAN_POINT('',(64.810368321836,41.5,24.3909957945347)) ;
#11852=CARTESIAN_POINT('Ctrl Pts',(64.5402455851436,41.5,24.8787173569202)) ;
#11853=CARTESIAN_POINT('Ctrl Pts',(64.5402455851436,40.85,24.8787173569202)) ;
#11854=CARTESIAN_POINT('Ctrl Pts',(64.4427012428641,41.5,24.9717597603798)) ;
#11855=CARTESIAN_POINT('Ctrl Pts',(64.4427012428641,40.85,24.9717597603798)) ;
#11856=CARTESIAN_POINT('Ctrl Pts',(64.2843792364001,41.5,25.0648020148277)) ;
#11857=CARTESIAN_POINT('Ctrl Pts',(64.2843792364001,40.85,25.0648020148277)) ;
#11858=CARTESIAN_POINT('',(64.5402455851436,40.987543636013,24.8787173569202)) ;
#11859=CARTESIAN_POINT('Ctrl Pts',(64.5402455851436,40.987543636013,24.8787173569202)) ;
#11860=CARTESIAN_POINT('Ctrl Pts',(64.5051954022992,40.9888847812188,24.9121498777342)) ;
#11861=CARTESIAN_POINT('Ctrl Pts',(64.4666886720027,40.9900244116147,24.9432630014271)) ;
#11862=CARTESIAN_POINT('Ctrl Pts',(64.4275224800183,40.9909957776269,24.9717483388133)) ;
#11863=CARTESIAN_POINT('Ctrl Pts',(64.381760456328,40.9921307277512,25.0050307851846)) ;
#11864=CARTESIAN_POINT('Ctrl Pts',(64.3331543424579,40.9930840800258,25.0361379906033)) ;
#11865=CARTESIAN_POINT('Ctrl Pts',(64.2843792364001,40.9938892055449,25.0648020148277)) ;
#11866=CARTESIAN_POINT('',(64.5402455851436,40.85,24.8787173569202)) ;
#11867=CARTESIAN_POINT('',(64.5402455851436,41.5,24.8787173569202)) ;
#11868=CARTESIAN_POINT('Ctrl Pts',(64.5402455851436,40.85,24.8787173569202)) ;
#11869=CARTESIAN_POINT('Ctrl Pts',(64.4427012428641,40.85,24.9717597603798)) ;
#11870=CARTESIAN_POINT('Ctrl Pts',(64.2843792364001,40.85,25.0648020148277)) ;
#11871=CARTESIAN_POINT('Origin',(64.5402455851436,41.5,26.5999998092651)) ;
#11872=CARTESIAN_POINT('',(64.5402455851436,40.9609184856404,26.5999998092651)) ;
#11873=CARTESIAN_POINT('Origin',(64.5402455851436,25.5,25.5)) ;
#11874=CARTESIAN_POINT('',(64.5402455851436,40.85,26.5999998092651)) ;
#11875=CARTESIAN_POINT('',(64.5402455851436,41.5,26.5999998092651)) ;
#11876=CARTESIAN_POINT('',(64.5402455851436,40.85,26.5999998092651)) ;
#11877=CARTESIAN_POINT('Origin',(64.810368321836,41.5,26.5999998092651)) ;
#11878=CARTESIAN_POINT('',(64.810368321836,40.9609184856404,26.5999998092651)) ;
#11879=CARTESIAN_POINT('',(55.25,40.9609184856404,26.5999998092651)) ;
#11880=CARTESIAN_POINT('',(64.810368321836,40.85,26.5999998092651)) ;
#11881=CARTESIAN_POINT('',(64.810368321836,41.5,26.5999998092651)) ;
#11882=CARTESIAN_POINT('',(64.810368321836,40.85,26.5999998092651)) ;
#11883=CARTESIAN_POINT('Origin',(64.810368321836,41.5,24.3909957945347)) ;
#11884=CARTESIAN_POINT('Origin',(64.810368321836,25.5,25.5)) ;
#11885=CARTESIAN_POINT('',(64.810368321836,40.85,24.3909957945347)) ;
#11886=CARTESIAN_POINT('Origin',(65.4714187197387,40.85,25.5142562776804)) ;
#11887=CARTESIAN_POINT('Origin',(55.25,25.5,25.5)) ;
#11888=CARTESIAN_POINT('',(76.5,10.,25.5)) ;
#11889=CARTESIAN_POINT('Origin',(76.5,25.5,25.5)) ;
#11890=CARTESIAN_POINT('',(45.75,10.,25.5)) ;
#11891=CARTESIAN_POINT('',(55.25,10.,25.5)) ;
#11892=CARTESIAN_POINT('Origin',(45.75,25.5,25.5)) ;
#11893=CARTESIAN_POINT('',(48.2806275524199,40.9807202883652,24.7271485567093)) ;
#11894=CARTESIAN_POINT('',(48.2806275524199,40.9609184856404,26.5999998092651)) ;
#11895=CARTESIAN_POINT('Origin',(48.2806275524199,25.5,25.5)) ;
#11896=CARTESIAN_POINT('',(48.,40.9609184856404,26.5999998092651)) ;
#11897=CARTESIAN_POINT('',(55.25,40.9609184856404,26.5999998092651)) ;
#11898=CARTESIAN_POINT('',(48.,40.960918459348,24.3999998211861)) ;
#11899=CARTESIAN_POINT('Origin',(48.,25.5,25.5)) ;
#11900=CARTESIAN_POINT('',(48.438199210912,40.960918459348,24.3999998211861)) ;
#11901=CARTESIAN_POINT('',(55.25,40.960918459348,24.3999998211861)) ;
#11902=CARTESIAN_POINT('',(48.9589358605444,40.99324057365,25.9577079057693)) ;
#11903=CARTESIAN_POINT('Origin',(48.8059256247246,25.5,25.5)) ;
#11904=CARTESIAN_POINT('',(49.0639836080372,40.9801923016591,26.2833557963371)) ;
#11905=CARTESIAN_POINT('Ctrl Pts',(48.9589358605444,40.99324057365,25.9577079057693)) ;
#11906=CARTESIAN_POINT('Ctrl Pts',(48.9648960688367,40.9927086680923,25.975712708973)) ;
#11907=CARTESIAN_POINT('Ctrl Pts',(48.9708344768427,40.9921439425243,25.9936940683478)) ;
#11908=CARTESIAN_POINT('Ctrl Pts',(48.9767569444717,40.991548248129,26.0116790190537)) ;
#11909=CARTESIAN_POINT('Ctrl Pts',(48.9825218268715,40.9909684039913,26.0291854255518)) ;
#11910=CARTESIAN_POINT('Ctrl Pts',(48.9882716861526,40.99035921714,26.046695460152)) ;
#11911=CARTESIAN_POINT('Ctrl Pts',(48.9939957694241,40.9897223948859,26.0641886918098)) ;
#11912=CARTESIAN_POINT('Ctrl Pts',(48.9994822498152,40.9891120066991,26.0809557910841)) ;
#11913=CARTESIAN_POINT('Ctrl Pts',(49.0049450898077,40.9884762297473,26.0977075661051)) ;
#11914=CARTESIAN_POINT('Ctrl Pts',(49.0103589727826,40.9878165674366,26.114381529626)) ;
#11915=CARTESIAN_POINT('Ctrl Pts',(49.0139965926115,40.9873733364482,26.1255848638339)) ;
#11916=CARTESIAN_POINT('Ctrl Pts',(49.0176117903286,40.986919322235,26.1367521707152)) ;
#11917=CARTESIAN_POINT('Ctrl Pts',(49.0211924119893,40.9864549808355,26.1478519325859)) ;
#11918=CARTESIAN_POINT('Ctrl Pts',(49.0253129741132,40.9859206189943,26.1606254849691)) ;
#11919=CARTESIAN_POINT('Ctrl Pts',(49.0294779792121,40.9853585879042,26.1735890327011)) ;
#11920=CARTESIAN_POINT('Ctrl Pts',(49.0336464350274,40.984777385263,26.1866349356787)) ;
#11921=CARTESIAN_POINT('Ctrl Pts',(49.0377005191652,40.9842121293234,26.1993228927225)) ;
#11922=CARTESIAN_POINT('Ctrl Pts',(49.0417579539094,40.9836287394359,26.2120889910656)) ;
#11923=CARTESIAN_POINT('Ctrl Pts',(49.0457648803463,40.9830350328495,26.2247888680327)) ;
#11924=CARTESIAN_POINT('Ctrl Pts',(49.0496161917,40.9824643837614,26.2369955259596)) ;
#11925=CARTESIAN_POINT('Ctrl Pts',(49.0534208832824,40.9818842037434,26.249141122998)) ;
#11926=CARTESIAN_POINT('Ctrl Pts',(49.0571151352053,40.9813014341738,26.2610525607634)) ;
#11927=CARTESIAN_POINT('Ctrl Pts',(49.059455920885,40.9809321743909,26.2685999948659)) ;
#11928=CARTESIAN_POINT('Ctrl Pts',(49.0617520462778,40.9805618749396,26.2760525179566)) ;
#11929=CARTESIAN_POINT('Ctrl Pts',(49.0639836080372,40.9801923016591,26.2833557963371)) ;
#11930=CARTESIAN_POINT('',(49.1810368485749,40.9940150133522,25.9306956768036)) ;
#11931=CARTESIAN_POINT('Ctrl Pts',(49.0639836080372,40.9801923016591,26.2833557963371)) ;
#11932=CARTESIAN_POINT('Ctrl Pts',(49.0681377308435,40.9808649857505,26.2700626297562)) ;
#11933=CARTESIAN_POINT('Ctrl Pts',(49.0724784462548,40.9815364180603,26.2563729913517)) ;
#11934=CARTESIAN_POINT('Ctrl Pts',(49.0769179212993,40.9821984510247,26.2425153748387)) ;
#11935=CARTESIAN_POINT('Ctrl Pts',(49.0814599230219,40.9828757731934,26.2283377260306)) ;
#11936=CARTESIAN_POINT('Ctrl Pts',(49.0861053808611,40.9835432568605,26.2139840305657)) ;
#11937=CARTESIAN_POINT('Ctrl Pts',(49.0907797150059,40.984192176838,26.1996468023641)) ;
#11938=CARTESIAN_POINT('Ctrl Pts',(49.0956286721937,40.9848653390664,26.1847739662365)) ;
#11939=CARTESIAN_POINT('Ctrl Pts',(49.1005087548046,40.9855185246986,26.1699187132935)) ;
#11940=CARTESIAN_POINT('Ctrl Pts',(49.1053564565797,40.9861419936983,26.1552430524173)) ;
#11941=CARTESIAN_POINT('Ctrl Pts',(49.1075732656997,40.986427100297,26.1485320086314)) ;
#11942=CARTESIAN_POINT('Ctrl Pts',(49.1097835645299,40.9867059927074,26.1418578210392)) ;
#11943=CARTESIAN_POINT('Ctrl Pts',(49.1119825312423,40.9869777395263,26.1352326309442)) ;
#11944=CARTESIAN_POINT('Ctrl Pts',(49.1180615069825,40.9877289752363,26.116917497007)) ;
#11945=CARTESIAN_POINT('Ctrl Pts',(49.124231241269,40.9884516561393,26.0984420610299)) ;
#11946=CARTESIAN_POINT('Ctrl Pts',(49.1304495084946,40.9891439670279,26.0799090634785)) ;
#11947=CARTESIAN_POINT('Ctrl Pts',(49.1368305907441,40.98985440493,26.0608908100947)) ;
#11948=CARTESIAN_POINT('Ctrl Pts',(49.1432628771849,40.9905328616201,26.0418116829618)) ;
#11949=CARTESIAN_POINT('Ctrl Pts',(49.1497204499148,40.9911773755401,26.0227299055392)) ;
#11950=CARTESIAN_POINT('Ctrl Pts',(49.1564364380756,40.9918476812474,26.0028845245242)) ;
#11951=CARTESIAN_POINT('Ctrl Pts',(49.1631798324207,40.9924812732244,25.9830361278838)) ;
#11952=CARTESIAN_POINT('Ctrl Pts',(49.1699413896424,40.9930759448742,25.9631968758645)) ;
#11953=CARTESIAN_POINT('Ctrl Pts',(49.1736338692995,40.9934006944693,25.9523626801179)) ;
#11954=CARTESIAN_POINT('Ctrl Pts',(49.1773321021792,40.993713837084,25.9415303098698)) ;
#11955=CARTESIAN_POINT('Ctrl Pts',(49.1810368485749,40.9940150133522,25.9306956768036)) ;
#11956=CARTESIAN_POINT('',(49.7077762074769,40.960918459348,24.3999998211861)) ;
#11957=CARTESIAN_POINT('Origin',(49.3292468040986,25.5,25.5)) ;
#11958=CARTESIAN_POINT('',(50.0994542725384,40.960918459348,24.3999998211861)) ;
#11959=CARTESIAN_POINT('',(55.25,40.960918459348,24.3999998211861)) ;
#11960=CARTESIAN_POINT('',(50.0994542725384,40.9609184856404,26.5999998092651)) ;
#11961=CARTESIAN_POINT('Origin',(50.0994542725384,25.5,25.5)) ;
#11962=CARTESIAN_POINT('',(49.8188268132508,40.9609184856404,26.5999998092651)) ;
#11963=CARTESIAN_POINT('',(55.25,40.9609184856404,26.5999998092651)) ;
#11964=CARTESIAN_POINT('',(49.8188268132508,40.9822614389786,24.7586628735065)) ;
#11965=CARTESIAN_POINT('Origin',(49.8188268132508,25.5,25.5)) ;
#11966=CARTESIAN_POINT('',(49.179536152631,40.9609184856404,26.5999998092651)) ;
#11967=CARTESIAN_POINT('Origin',(49.5614432284574,25.5,25.5)) ;
#11968=CARTESIAN_POINT('',(48.916916821152,40.9609184856404,26.5999998092651)) ;
#11969=CARTESIAN_POINT('',(55.25,40.9609184856404,26.5999998092651)) ;
#11970=CARTESIAN_POINT('Origin',(48.5431989013291,25.5,25.5)) ;
#11971=CARTESIAN_POINT('',(51.7614599056542,40.9643621744601,26.5504772901535)) ;
#11972=CARTESIAN_POINT('',(51.4448158927262,40.9799256191272,26.2886081576347)) ;
#11973=CARTESIAN_POINT('Ctrl Pts',(51.7614599056542,40.9643621744601,26.5504772901535)) ;
#11974=CARTESIAN_POINT('Ctrl Pts',(51.6964813536973,40.9662655725095,26.5224568492794)) ;
#11975=CARTESIAN_POINT('Ctrl Pts',(51.6359558815656,40.9686336795545,26.4866160640346)) ;
#11976=CARTESIAN_POINT('Ctrl Pts',(51.581440855625,40.9713767366872,26.4415422834339)) ;
#11977=CARTESIAN_POINT('Ctrl Pts',(51.5281656401324,40.9740574097187,26.3974935953311)) ;
#11978=CARTESIAN_POINT('Ctrl Pts',(51.4827528621409,40.9769824160316,26.3463815455476)) ;
#11979=CARTESIAN_POINT('Ctrl Pts',(51.4448158927262,40.9799256191272,26.2886081576347)) ;
#11980=CARTESIAN_POINT('',(51.3240109868348,40.9950124467317,25.8931784272194)) ;
#11981=CARTESIAN_POINT('Ctrl Pts',(51.4448158927262,40.9799256191272,26.2886081576347)) ;
#11982=CARTESIAN_POINT('Ctrl Pts',(51.4068025882613,40.9828747393755,26.2307186194111)) ;
#11983=CARTESIAN_POINT('Ctrl Pts',(51.3775082128716,40.9857098719761,26.1687185433935)) ;
#11984=CARTESIAN_POINT('Ctrl Pts',(51.3572563430792,40.9882866323644,26.1024758864232)) ;
#11985=CARTESIAN_POINT('Ctrl Pts',(51.3364460712854,40.9909344414101,26.0344067298455)) ;
#11986=CARTESIAN_POINT('Ctrl Pts',(51.3259478200354,40.9932063396208,25.9643564223097)) ;
#11987=CARTESIAN_POINT('Ctrl Pts',(51.3240109868348,40.9950124467317,25.8931784272194)) ;
#11988=CARTESIAN_POINT('',(51.5986358113587,40.9956030954071,25.8691675901413)) ;
#11989=CARTESIAN_POINT('Origin',(55.8210035835746,25.5,25.5)) ;
#11990=CARTESIAN_POINT('',(51.6894270963967,40.9867797701289,26.1400408983231)) ;
#11991=CARTESIAN_POINT('Ctrl Pts',(51.5986358113587,40.9956030954071,25.8691675901413)) ;
#11992=CARTESIAN_POINT('Ctrl Pts',(51.6046370539695,40.9943933193175,25.9199472647895)) ;
#11993=CARTESIAN_POINT('Ctrl Pts',(51.6148318747084,40.9929206486228,25.9709173464044)) ;
#11994=CARTESIAN_POINT('Ctrl Pts',(51.6310807803016,40.9912950366146,26.019401663994)) ;
#11995=CARTESIAN_POINT('Ctrl Pts',(51.6453470747562,40.9898677737479,26.0619701648198)) ;
#11996=CARTESIAN_POINT('Ctrl Pts',(51.6643402765475,40.9883185923293,26.1028067144042)) ;
#11997=CARTESIAN_POINT('Ctrl Pts',(51.6894270963967,40.9867797701289,26.1400408983231)) ;
#11998=CARTESIAN_POINT('',(51.9107775874436,40.9787624461282,26.3111184477806)) ;
#11999=CARTESIAN_POINT('Ctrl Pts',(51.6894270963967,40.9867797701289,26.1400408983231)) ;
#12000=CARTESIAN_POINT('Ctrl Pts',(51.7142620765023,40.9852564000361,26.1769011945908)) ;
#12001=CARTESIAN_POINT('Ctrl Pts',(51.7452172284269,40.9838223504436,26.2085097613467)) ;
#12002=CARTESIAN_POINT('Ctrl Pts',(51.7803864227145,40.9825306087772,26.235694194809)) ;
#12003=CARTESIAN_POINT('Ctrl Pts',(51.8201118378289,40.9810715200789,26.2664004115936)) ;
#12004=CARTESIAN_POINT('Ctrl Pts',(51.8647416209425,40.979811830078,26.2910928092094)) ;
#12005=CARTESIAN_POINT('Ctrl Pts',(51.9107775874436,40.9787624461282,26.3111184477806)) ;
#12006=CARTESIAN_POINT('',(52.248431045562,40.9752035998426,26.3763980507851)) ;
#12007=CARTESIAN_POINT('Ctrl Pts',(51.9107775874436,40.9787624461282,26.3111184477806)) ;
#12008=CARTESIAN_POINT('Ctrl Pts',(51.9620215954958,40.9775943478592,26.3334095393825)) ;
#12009=CARTESIAN_POINT('Ctrl Pts',(52.0153352704738,40.9767090178051,26.3494650680102)) ;
#12010=CARTESIAN_POINT('Ctrl Pts',(52.070210135829,40.9761193640483,26.3600752465508)) ;
#12011=CARTESIAN_POINT('Ctrl Pts',(52.128909533513,40.9754886140657,26.3714249070122)) ;
#12012=CARTESIAN_POINT('Ctrl Pts',(52.1886446082517,40.9752035998426,26.3763980507851)) ;
#12013=CARTESIAN_POINT('Ctrl Pts',(52.248431045562,40.9752035998426,26.3763980507851)) ;
#12014=CARTESIAN_POINT('',(52.5425647683442,40.9779286844934,26.3268758296967)) ;
#12015=CARTESIAN_POINT('Ctrl Pts',(52.248431045562,40.9752035998426,26.3763980507851)) ;
#12016=CARTESIAN_POINT('Ctrl Pts',(52.3008462457101,40.9752035998426,26.3763980507851)) ;
#12017=CARTESIAN_POINT('Ctrl Pts',(52.3535603822056,40.9754138750608,26.3727206746845)) ;
#12018=CARTESIAN_POINT('Ctrl Pts',(52.4052520979163,40.97589976934,26.3640175515236)) ;
#12019=CARTESIAN_POINT('Ctrl Pts',(52.4521459373439,40.9763405643107,26.3561222272069)) ;
#12020=CARTESIAN_POINT('Ctrl Pts',(52.4982385886269,40.9770093346525,26.3440847391397)) ;
#12021=CARTESIAN_POINT('Ctrl Pts',(52.5425647683442,40.9779286844934,26.3268758296967)) ;
#12022=CARTESIAN_POINT('',(52.7324010916054,40.9845868720206,26.1910639643669)) ;
#12023=CARTESIAN_POINT('Ctrl Pts',(52.5425647683442,40.9779286844934,26.3268758296967)) ;
#12024=CARTESIAN_POINT('Ctrl Pts',(52.5816398844146,40.9787391273113,26.3117055034049)) ;
#12025=CARTESIAN_POINT('Ctrl Pts',(52.6197003909076,40.9797431606842,26.292557929649)) ;
#12026=CARTESIAN_POINT('Ctrl Pts',(52.6537956587279,40.9809534520937,26.2681667879486)) ;
#12027=CARTESIAN_POINT('Ctrl Pts',(52.6839651701171,40.9820243895815,26.2465840618294)) ;
#12028=CARTESIAN_POINT('Ctrl Pts',(52.7106959059527,40.9832447154609,26.2211375044691)) ;
#12029=CARTESIAN_POINT('Ctrl Pts',(52.7324010916054,40.9845868720206,26.1910639643669)) ;
#12030=CARTESIAN_POINT('',(52.7946796007454,40.9918450924657,26.0027281880379)) ;
#12031=CARTESIAN_POINT('Ctrl Pts',(52.7324010916054,40.9845868720206,26.1910639643669)) ;
#12032=CARTESIAN_POINT('Ctrl Pts',(52.7524211406543,40.9858248209608,26.1633253918234)) ;
#12033=CARTESIAN_POINT('Ctrl Pts',(52.7683641209573,40.987089895988,26.1333269333519)) ;
#12034=CARTESIAN_POINT('Ctrl Pts',(52.7791056990498,40.9883498589597,26.100848272414)) ;
#12035=CARTESIAN_POINT('Ctrl Pts',(52.7896347238596,40.989584889909,26.0690122959998)) ;
#12036=CARTESIAN_POINT('Ctrl Pts',(52.7946796007454,40.9907567799209,26.036265136544)) ;
#12037=CARTESIAN_POINT('Ctrl Pts',(52.7946796007454,40.9918450924657,26.0027281880379)) ;
#12038=CARTESIAN_POINT('',(52.7346523590386,40.9966571536944,25.8218960404396)) ;
#12039=CARTESIAN_POINT('Ctrl Pts',(52.7946796007454,40.9918450924657,26.0027281880379)) ;
#12040=CARTESIAN_POINT('Ctrl Pts',(52.7946796007454,40.9929177965443,25.9696722229826)) ;
#12041=CARTESIAN_POINT('Ctrl Pts',(52.7900915130482,40.993866440127,25.9371363688912)) ;
#12042=CARTESIAN_POINT('Ctrl Pts',(52.7796755372991,40.9946882166121,25.9057549383327)) ;
#12043=CARTESIAN_POINT('Ctrl Pts',(52.769538117278,40.9954880162271,25.8752127452538)) ;
#12044=CARTESIAN_POINT('Ctrl Pts',(52.7543956539943,40.9961291401958,25.8473155645521)) ;
#12045=CARTESIAN_POINT('Ctrl Pts',(52.7346523590386,40.9966571536944,25.8218960404396)) ;
#12046=CARTESIAN_POINT('',(52.5365622825921,40.9988097137483,25.6920871078968)) ;
#12047=CARTESIAN_POINT('Ctrl Pts',(52.7346523590386,40.9966571536944,25.8218960404396)) ;
#12048=CARTESIAN_POINT('Ctrl Pts',(52.7129787665804,40.997236790954,25.7939912551781)) ;
#12049=CARTESIAN_POINT('Ctrl Pts',(52.6854008743602,40.9976474971274,25.7707383845552)) ;
#12050=CARTESIAN_POINT('Ctrl Pts',(52.6559042636246,40.9979624094066,25.7513188345919)) ;
#12051=CARTESIAN_POINT('Ctrl Pts',(52.6233974190617,40.9983094596017,25.7299174506227)) ;
#12052=CARTESIAN_POINT('Ctrl Pts',(52.5871671231961,40.9985539368512,25.7122615418921)) ;
#12053=CARTESIAN_POINT('Ctrl Pts',(52.5507998661306,40.9987398284926,25.697652703815)) ;
#12054=CARTESIAN_POINT('Ctrl Pts',(52.546053648936,40.9987640888349,25.6957461338928)) ;
#12055=CARTESIAN_POINT('Ctrl Pts',(52.5413051382014,40.9987873513276,25.6938914502431)) ;
#12056=CARTESIAN_POINT('Ctrl Pts',(52.5365622825921,40.9988097137483,25.6920871078968)) ;
#12057=CARTESIAN_POINT('',(52.1448840685189,40.9997680931486,25.5847883164883)) ;
#12058=CARTESIAN_POINT('Ctrl Pts',(52.5365622825921,40.9988097137483,25.6920871078968)) ;
#12059=CARTESIAN_POINT('Ctrl Pts',(52.5182257411425,40.9988983054462,25.684938966189)) ;
#12060=CARTESIAN_POINT('Ctrl Pts',(52.4945785983502,40.9989879874405,25.6771819864424)) ;
#12061=CARTESIAN_POINT('Ctrl Pts',(52.4695770160932,40.9990711361368,25.6695822803517)) ;
#12062=CARTESIAN_POINT('Ctrl Pts',(52.4546928281606,40.9991206370368,25.6650579485504)) ;
#12063=CARTESIAN_POINT('Ctrl Pts',(52.4393314158557,40.9991678224209,25.6605898588925)) ;
#12064=CARTESIAN_POINT('Ctrl Pts',(52.4243063105268,40.9992110837459,25.6563358768948)) ;
#12065=CARTESIAN_POINT('Ctrl Pts',(52.4140931288561,40.9992404902467,25.653444270479)) ;
#12066=CARTESIAN_POINT('Ctrl Pts',(52.4040348829017,40.9992680836439,25.6506515110719)) ;
#12067=CARTESIAN_POINT('Ctrl Pts',(52.3943729570076,40.9992933587377,25.6480046613764)) ;
#12068=CARTESIAN_POINT('Ctrl Pts',(52.3677500724645,40.9993630028139,25.6407114183296)) ;
#12069=CARTESIAN_POINT('Ctrl Pts',(52.3394635166996,40.999428272284,25.6332473779268)) ;
#12070=CARTESIAN_POINT('Ctrl Pts',(52.3106235865612,40.9994881370534,25.6258289117774)) ;
#12071=CARTESIAN_POINT('Ctrl Pts',(52.268939054618,40.9995746641316,25.6151064416574)) ;
#12072=CARTESIAN_POINT('Ctrl Pts',(52.2261050593121,40.9996499001918,25.6044803575766)) ;
#12073=CARTESIAN_POINT('Ctrl Pts',(52.1855915980078,40.9997107348117,25.5946249394643)) ;
#12074=CARTESIAN_POINT('Ctrl Pts',(52.1717040291299,40.9997315882502,25.5912466105472)) ;
#12075=CARTESIAN_POINT('Ctrl Pts',(52.1580891323526,40.9997507494576,25.5879588380836)) ;
#12076=CARTESIAN_POINT('Ctrl Pts',(52.1448840685189,40.9997680931486,25.5847883164883)) ;
#12077=CARTESIAN_POINT('',(51.7201911397278,40.9999110068208,25.4474759042263)) ;
#12078=CARTESIAN_POINT('Ctrl Pts',(52.1448840685189,40.9997680931486,25.5847883164883)) ;
#12079=CARTESIAN_POINT('Ctrl Pts',(52.096230338235,40.9998319955481,25.5731066082814)) ;
#12080=CARTESIAN_POINT('Ctrl Pts',(52.0446116326547,40.9998898156088,25.5600316125952)) ;
#12081=CARTESIAN_POINT('Ctrl Pts',(51.9937884549582,40.9999317100544,25.5459097913523)) ;
#12082=CARTESIAN_POINT('Ctrl Pts',(51.9573724589345,40.999961728405,25.5357911759974)) ;
#12083=CARTESIAN_POINT('Ctrl Pts',(51.9213699605045,40.9999835704527,25.5251353447576)) ;
#12084=CARTESIAN_POINT('Ctrl Pts',(51.8871420945215,40.9999936151787,25.5140687391253)) ;
#12085=CARTESIAN_POINT('Ctrl Pts',(51.8629486620922,41.0000007151363,25.506246481795)) ;
#12086=CARTESIAN_POINT('Ctrl Pts',(51.8383934367245,41.0000022794694,25.4978174129243)) ;
#12087=CARTESIAN_POINT('Ctrl Pts',(51.8145911107741,40.9999958146662,25.4888742637738)) ;
#12088=CARTESIAN_POINT('Ctrl Pts',(51.7804331295751,40.9999865372272,25.4760402272524)) ;
#12089=CARTESIAN_POINT('Ctrl Pts',(51.7478284878484,40.999960724399,25.4621476092093)) ;
#12090=CARTESIAN_POINT('Ctrl Pts',(51.7201911397278,40.9999110068208,25.4474759042263)) ;
#12091=CARTESIAN_POINT('',(51.4853342361748,40.9978631490248,25.2426329195499)) ;
#12092=CARTESIAN_POINT('Ctrl Pts',(51.7201911397278,40.9999110068208,25.4474759042263)) ;
#12093=CARTESIAN_POINT('Ctrl Pts',(51.6712001615781,40.9998240471528,25.4218140228572)) ;
#12094=CARTESIAN_POINT('Ctrl Pts',(51.6243780826768,40.9996618864735,25.3913559963214)) ;
#12095=CARTESIAN_POINT('Ctrl Pts',(51.5826913086288,40.9993217284307,25.3549966945329)) ;
#12096=CARTESIAN_POINT('Ctrl Pts',(51.5450120776924,40.9990142713597,25.3221327812161)) ;
#12097=CARTESIAN_POINT('Ctrl Pts',(51.5120411777685,40.9985650171349,25.2848972833514)) ;
#12098=CARTESIAN_POINT('Ctrl Pts',(51.4853342361748,40.9978631490248,25.2426329195499)) ;
#12099=CARTESIAN_POINT('',(51.4080490656197,40.990893529069,24.9687583684921)) ;
#12100=CARTESIAN_POINT('Ctrl Pts',(51.4853342361748,40.9978631490248,25.2426329195499)) ;
#12101=CARTESIAN_POINT('Ctrl Pts',(51.4597867312913,40.9971917513319,25.2022033916376)) ;
#12102=CARTESIAN_POINT('Ctrl Pts',(51.4403592614856,40.9963177393255,25.1590373372296)) ;
#12103=CARTESIAN_POINT('Ctrl Pts',(51.4273724576651,40.9951684612961,25.1130189202868)) ;
#12104=CARTESIAN_POINT('Ctrl Pts',(51.4140845004671,40.9939925324474,25.065933373827)) ;
#12105=CARTESIAN_POINT('Ctrl Pts',(51.4080490656197,40.9925708016359,25.0176672815208)) ;
#12106=CARTESIAN_POINT('Ctrl Pts',(51.4080490656197,40.990893529069,24.9687583684921)) ;
#12107=CARTESIAN_POINT('',(51.5025921650231,40.9770788394087,24.6573668658733)) ;
#12108=CARTESIAN_POINT('Ctrl Pts',(51.4080490656197,40.990893529069,24.9687583684921)) ;
#12109=CARTESIAN_POINT('Ctrl Pts',(51.4080490656197,40.9890120993808,24.913896277019)) ;
#12110=CARTESIAN_POINT('Ctrl Pts',(51.4157405734043,40.9868770379277,24.8601568119043)) ;
#12111=CARTESIAN_POINT('Ctrl Pts',(51.4316684952429,40.9845306068251,24.8076764583681)) ;
#12112=CARTESIAN_POINT('Ctrl Pts',(51.447903294973,40.9821389678267,24.7541849835815)) ;
#12113=CARTESIAN_POINT('Ctrl Pts',(51.4720374059445,40.9796269269382,24.704168908171)) ;
#12114=CARTESIAN_POINT('Ctrl Pts',(51.5025921650231,40.9770788394087,24.6573668658733)) ;
#12115=CARTESIAN_POINT('',(51.7787178345025,40.9635419522324,24.4375169217587)) ;
#12116=CARTESIAN_POINT('Ctrl Pts',(51.5025921650231,40.9770788394087,24.6573668658733)) ;
#12117=CARTESIAN_POINT('Ctrl Pts',(51.5344017011208,40.9744261081125,24.6086427773617)) ;
#12118=CARTESIAN_POINT('Ctrl Pts',(51.5732894347549,40.9718958869814,24.5663202911221)) ;
#12119=CARTESIAN_POINT('Ctrl Pts',(51.6188180475123,40.9696222373288,24.5300578190727)) ;
#12120=CARTESIAN_POINT('Ctrl Pts',(51.6672834699504,40.9672019265788,24.4914562470045)) ;
#12121=CARTESIAN_POINT('Ctrl Pts',(51.7214359964055,40.9651683030504,24.4611870814236)) ;
#12122=CARTESIAN_POINT('Ctrl Pts',(51.7787178345025,40.9635419522324,24.4375169217587)) ;
#12123=CARTESIAN_POINT('',(52.1824010200799,40.958203478351,24.3624828696251)) ;
#12124=CARTESIAN_POINT('Ctrl Pts',(51.7787178345025,40.9635419522324,24.4375169217587)) ;
#12125=CARTESIAN_POINT('Ctrl Pts',(51.8405473847017,40.9617864795045,24.4119675019799)) ;
#12126=CARTESIAN_POINT('Ctrl Pts',(51.90459885672,40.9604580977664,24.3934803221617)) ;
#12127=CARTESIAN_POINT('Ctrl Pts',(51.9703891248391,40.9595729585521,24.3812489377864)) ;
#12128=CARTESIAN_POINT('Ctrl Pts',(52.040299600929,40.9586323862509,24.3682515457805)) ;
#12129=CARTESIAN_POINT('Ctrl Pts',(52.1112893721457,40.958203478351,24.3624828696251)) ;
#12130=CARTESIAN_POINT('Ctrl Pts',(52.1824010200799,40.958203478351,24.3624828696251)) ;
#12131=CARTESIAN_POINT('',(52.6138474531472,40.9637992678179,24.4412685871124)) ;
#12132=CARTESIAN_POINT('Ctrl Pts',(52.1824010200799,40.958203478351,24.3624828696251)) ;
#12133=CARTESIAN_POINT('Ctrl Pts',(52.25942789036,40.958203478351,24.3624828696251)) ;
#12134=CARTESIAN_POINT('Ctrl Pts',(52.3367901435739,40.9586397198479,24.3683417117733)) ;
#12135=CARTESIAN_POINT('Ctrl Pts',(52.4125663074585,40.959640229793,24.3821789206829)) ;
#12136=CARTESIAN_POINT('Ctrl Pts',(52.481642392275,40.9605522753003,24.3947926525909)) ;
#12137=CARTESIAN_POINT('Ctrl Pts',(52.5491617482125,40.9619317389306,24.4139915161869)) ;
#12138=CARTESIAN_POINT('Ctrl Pts',(52.6138474531472,40.9637992678179,24.4412685871124)) ;
#12139=CARTESIAN_POINT('',(52.901227671653,40.9779286727117,24.6731239497662)) ;
#12140=CARTESIAN_POINT('Ctrl Pts',(52.6138474531472,40.9637992678179,24.4412685871124)) ;
#12141=CARTESIAN_POINT('Ctrl Pts',(52.6731688875777,40.9655119290941,24.4662836663549)) ;
#12142=CARTESIAN_POINT('Ctrl Pts',(52.728970455649,40.9676436064132,24.4981815551952)) ;
#12143=CARTESIAN_POINT('Ctrl Pts',(52.7790628186729,40.9701546747433,24.5385873209086)) ;
#12144=CARTESIAN_POINT('Ctrl Pts',(52.8267918049618,40.9725472699148,24.5770867272315)) ;
#12145=CARTESIAN_POINT('Ctrl Pts',(52.8675699374113,40.9751912656509,24.6218836324023)) ;
#12146=CARTESIAN_POINT('Ctrl Pts',(52.901227671653,40.9779286727117,24.6731239497662)) ;
#12147=CARTESIAN_POINT('',(53.0092771835625,40.9925591905437,25.0197815835476)) ;
#12148=CARTESIAN_POINT('Ctrl Pts',(52.901227671653,40.9779286727117,24.6731239497662)) ;
#12149=CARTESIAN_POINT('Ctrl Pts',(52.9345738501646,40.9806407272898,24.7238897051711)) ;
#12150=CARTESIAN_POINT('Ctrl Pts',(52.9603936002435,40.9832945476178,24.778224903136)) ;
#12151=CARTESIAN_POINT('Ctrl Pts',(52.9784800908764,40.9857803484854,24.8362176573139)) ;
#12152=CARTESIAN_POINT('Ctrl Pts',(52.9970861473933,40.9883375583042,24.8958763541669)) ;
#12153=CARTESIAN_POINT('Ctrl Pts',(53.0068559081193,40.9906229160949,24.957314494657)) ;
#12154=CARTESIAN_POINT('Ctrl Pts',(53.0092771835625,40.9925591905437,25.0197815835475)) ;
#12155=CARTESIAN_POINT('',(52.7301501221955,40.993196160172,25.0407911777496)) ;
#12156=CARTESIAN_POINT('Origin',(46.6292417526227,25.5,25.5)) ;
#12157=CARTESIAN_POINT('',(52.5778307504952,40.9806452954799,24.7256478607655)) ;
#12158=CARTESIAN_POINT('Ctrl Pts',(52.7301501221955,40.993196160172,25.0407911777496)) ;
#12159=CARTESIAN_POINT('Ctrl Pts',(52.7233426866318,40.9913264464056,24.9777091097621)) ;
#12160=CARTESIAN_POINT('Ctrl Pts',(52.7084515806111,40.9890587023187,24.9149092071746)) ;
#12161=CARTESIAN_POINT('Ctrl Pts',(52.680844208208,40.986689065273,24.8577681138769)) ;
#12162=CARTESIAN_POINT('Ctrl Pts',(52.6684313800218,40.9856236289438,24.8320763325977)) ;
#12163=CARTESIAN_POINT('Ctrl Pts',(52.6535949220013,40.9845538245761,24.8078292757448)) ;
#12164=CARTESIAN_POINT('Ctrl Pts',(52.6360497020993,40.9835151584649,24.7853264118589)) ;
#12165=CARTESIAN_POINT('Ctrl Pts',(52.6188579928331,40.9824974199636,24.7632769479167)) ;
#12166=CARTESIAN_POINT('Ctrl Pts',(52.5994458221421,40.9815327548068,24.7433897153539)) ;
#12167=CARTESIAN_POINT('Ctrl Pts',(52.5778307504952,40.9806452954799,24.7256478607655)) ;
#12168=CARTESIAN_POINT('',(52.1944065876305,40.9749479577385,24.6190994918346)) ;
#12169=CARTESIAN_POINT('Ctrl Pts',(52.5778307504952,40.9806452954799,24.7256478607655)) ;
#12170=CARTESIAN_POINT('Ctrl Pts',(52.5404445771057,40.9791103138436,24.6949609096451)) ;
#12171=CARTESIAN_POINT('Ctrl Pts',(52.4974914881731,40.977912081391,24.6726577834149)) ;
#12172=CARTESIAN_POINT('Ctrl Pts',(52.451846940174,40.9770388904196,24.656633422266)) ;
#12173=CARTESIAN_POINT('Ctrl Pts',(52.4149548595667,40.9763331362143,24.6436817763608)) ;
#12174=CARTESIAN_POINT('Ctrl Pts',(52.3760168414359,40.9758364044645,24.6347357031708)) ;
#12175=CARTESIAN_POINT('Ctrl Pts',(52.3364479207098,40.9755047478818,24.6288393623379)) ;
#12176=CARTESIAN_POINT('Ctrl Pts',(52.2891833143096,40.9751085880283,24.6217962531615)) ;
#12177=CARTESIAN_POINT('Ctrl Pts',(52.2410243634678,40.9749479577385,24.6190994918346)) ;
#12178=CARTESIAN_POINT('Ctrl Pts',(52.1944065876305,40.9749479577385,24.6190994918346)) ;
#12179=CARTESIAN_POINT('',(51.8094815798104,40.9801542905129,24.7158934116364)) ;
#12180=CARTESIAN_POINT('Ctrl Pts',(52.1944065876305,40.9749479577385,24.6190994918346)) ;
#12181=CARTESIAN_POINT('Ctrl Pts',(52.1439402727095,40.9749479577385,24.6190994918346)) ;
#12182=CARTESIAN_POINT('Ctrl Pts',(52.0910857438607,40.9751032396394,24.6217463705642)) ;
#12183=CARTESIAN_POINT('Ctrl Pts',(52.0397048022768,40.975513640306,24.6290595674904)) ;
#12184=CARTESIAN_POINT('Ctrl Pts',(52.0146784903811,40.9757135357296,24.632621634311)) ;
#12185=CARTESIAN_POINT('Ctrl Pts',(51.9900025942792,40.9759739557623,24.6372912969542)) ;
#12186=CARTESIAN_POINT('Ctrl Pts',(51.9661169206961,40.9763064369372,24.6432975603998)) ;
#12187=CARTESIAN_POINT('Ctrl Pts',(51.9363088470246,40.9767213560861,24.6507930636208)) ;
#12188=CARTESIAN_POINT('Ctrl Pts',(51.9067290064541,40.9772610647307,24.6606207748326)) ;
#12189=CARTESIAN_POINT('Ctrl Pts',(51.8788404119519,40.9779512382307,24.6735464520297)) ;
#12190=CARTESIAN_POINT('Ctrl Pts',(51.8541742294851,40.9785616650302,24.6849786205538)) ;
#12191=CARTESIAN_POINT('Ctrl Pts',(51.830695022219,40.9792933473658,24.6988963184466)) ;
#12192=CARTESIAN_POINT('Ctrl Pts',(51.8094815798104,40.9801542905129,24.7158934116364)) ;
#12193=CARTESIAN_POINT('',(51.688676673919,40.9902121952529,24.9492494702339)) ;
#12194=CARTESIAN_POINT('Ctrl Pts',(51.8094815798104,40.9801542905129,24.7158934116364)) ;
#12195=CARTESIAN_POINT('Ctrl Pts',(51.7743817719654,40.9815788111055,24.7440168822091)) ;
#12196=CARTESIAN_POINT('Ctrl Pts',(51.743699410759,40.9831904309469,24.7772470381369)) ;
#12197=CARTESIAN_POINT('Ctrl Pts',(51.7220520990965,40.9849304145919,24.8166771954285)) ;
#12198=CARTESIAN_POINT('Ctrl Pts',(51.7110076789359,40.9858181511731,24.8367943920077)) ;
#12199=CARTESIAN_POINT('Ctrl Pts',(51.7026233497426,40.9867130969639,24.8579614264901)) ;
#12200=CARTESIAN_POINT('Ctrl Pts',(51.6970205795988,40.9876036979261,24.8802164119748)) ;
#12201=CARTESIAN_POINT('Ctrl Pts',(51.6913231790868,40.9885093410718,24.9028472824976)) ;
#12202=CARTESIAN_POINT('Ctrl Pts',(51.688676673919,40.9893823612855,24.9259098572)) ;
#12203=CARTESIAN_POINT('Ctrl Pts',(51.688676673919,40.9902121952529,24.9492494702339)) ;
#12204=CARTESIAN_POINT('',(51.7742155976593,40.9959189676464,25.1443381547928)) ;
#12205=CARTESIAN_POINT('Ctrl Pts',(51.688676673919,40.9902121952529,24.9492494702339)) ;
#12206=CARTESIAN_POINT('Ctrl Pts',(51.688676673919,40.9914864166818,24.9850877658867)) ;
#12207=CARTESIAN_POINT('Ctrl Pts',(51.6945391874085,40.9926057767986,25.0201432961235)) ;
#12208=CARTESIAN_POINT('Ctrl Pts',(51.7083258839055,40.9935600903843,25.0532386256064)) ;
#12209=CARTESIAN_POINT('Ctrl Pts',(51.7154858640819,40.9940557034093,25.0704263473408)) ;
#12210=CARTESIAN_POINT('Ctrl Pts',(51.7245587420721,40.9944920818065,25.0865475195267)) ;
#12211=CARTESIAN_POINT('Ctrl Pts',(51.7354721183132,40.9948800090314,25.1016364653763)) ;
#12212=CARTESIAN_POINT('Ctrl Pts',(51.7467870555517,40.9952822101566,25.1172806135766)) ;
#12213=CARTESIAN_POINT('Ctrl Pts',(51.759825949631,40.9956234625419,25.1314632197502)) ;
#12214=CARTESIAN_POINT('Ctrl Pts',(51.7742155976593,40.9959189676464,25.1443381547928)) ;
#12215=CARTESIAN_POINT('',(52.213165063411,40.9987245424185,25.301159465313)) ;
#12216=CARTESIAN_POINT('Ctrl Pts',(51.7742155976593,40.9959189676464,25.1443381547928)) ;
#12217=CARTESIAN_POINT('Ctrl Pts',(51.7845766428338,40.9961355419343,25.1537741335494)) ;
#12218=CARTESIAN_POINT('Ctrl Pts',(51.7972705332651,40.9963287165035,25.1625669264881)) ;
#12219=CARTESIAN_POINT('Ctrl Pts',(51.81087410563,40.9964999073154,25.1706209396928)) ;
#12220=CARTESIAN_POINT('Ctrl Pts',(51.8177681697437,40.9965866639703,25.1747025795677)) ;
#12221=CARTESIAN_POINT('Ctrl Pts',(51.8248962317976,40.9966677745506,25.1785944841596)) ;
#12222=CARTESIAN_POINT('Ctrl Pts',(51.8320789274207,40.9967434233534,25.1822842925641)) ;
#12223=CARTESIAN_POINT('Ctrl Pts',(51.8666642598451,40.9971076792165,25.2000510554829)) ;
#12224=CARTESIAN_POINT('Ctrl Pts',(51.9106531996414,40.9974307096486,25.2173079842982)) ;
#12225=CARTESIAN_POINT('Ctrl Pts',(51.961637056368,40.9977170699623,25.2339935089345)) ;
#12226=CARTESIAN_POINT('Ctrl Pts',(52.0071481792142,40.9979726916482,25.2488879678913)) ;
#12227=CARTESIAN_POINT('Ctrl Pts',(52.0582327363947,40.9981990932109,25.2633271053793)) ;
#12228=CARTESIAN_POINT('Ctrl Pts',(52.1132190775607,40.9983995148573,25.2772677033774)) ;
#12229=CARTESIAN_POINT('Ctrl Pts',(52.1453123943052,40.9985164929149,25.2854042699805)) ;
#12230=CARTESIAN_POINT('Ctrl Pts',(52.17873570998,40.9986246206864,25.2933710161247)) ;
#12231=CARTESIAN_POINT('Ctrl Pts',(52.213165063411,40.9987245424185,25.301159465313)) ;
#12232=CARTESIAN_POINT('',(52.7001365013421,40.9998895035356,25.4414732694626)) ;
#12233=CARTESIAN_POINT('Ctrl Pts',(52.213165063411,40.9987245424185,25.301159465313)) ;
#12234=CARTESIAN_POINT('Ctrl Pts',(52.2588316805259,40.9988570774647,25.3114899755225)) ;
#12235=CARTESIAN_POINT('Ctrl Pts',(52.307250337576,40.9989911466368,25.3228165607694)) ;
#12236=CARTESIAN_POINT('Ctrl Pts',(52.3556913472795,40.9991187993419,25.3347995517285)) ;
#12237=CARTESIAN_POINT('Ctrl Pts',(52.3948926984319,40.9992221035164,25.3444969019555)) ;
#12238=CARTESIAN_POINT('Ctrl Pts',(52.4341033743883,40.9993212055398,25.354623649893)) ;
#12239=CARTESIAN_POINT('Ctrl Pts',(52.4718855245653,40.9994118917176,25.3650005797862)) ;
#12240=CARTESIAN_POINT('Ctrl Pts',(52.4855872668106,40.9994447791692,25.3687637859041)) ;
#12241=CARTESIAN_POINT('Ctrl Pts',(52.4991015449596,40.9994765598033,25.3725599321762)) ;
#12242=CARTESIAN_POINT('Ctrl Pts',(52.5123617001045,40.9995070326502,25.3763806454261)) ;
#12243=CARTESIAN_POINT('Ctrl Pts',(52.5357625667123,40.9995608096249,25.3831232513858)) ;
#12244=CARTESIAN_POINT('Ctrl Pts',(52.5597894438442,40.9996136590807,25.3903496797628)) ;
#12245=CARTESIAN_POINT('Ctrl Pts',(52.583398610579,40.9996634459259,25.3979347181335)) ;
#12246=CARTESIAN_POINT('Ctrl Pts',(52.6148861793824,40.99972984669,25.4080508912394)) ;
#12247=CARTESIAN_POINT('Ctrl Pts',(52.645628605886,40.9997907998102,25.4188047506243)) ;
#12248=CARTESIAN_POINT('Ctrl Pts',(52.6730448795419,40.9998412401404,25.4298897091704)) ;
#12249=CARTESIAN_POINT('Ctrl Pts',(52.6825076792224,40.9998586497543,25.4337157120585)) ;
#12250=CARTESIAN_POINT('Ctrl Pts',(52.6915737547063,40.9998748069759,25.4375811154143)) ;
#12251=CARTESIAN_POINT('Ctrl Pts',(52.7001365013421,40.9998895035356,25.4414732694626)) ;
#12252=CARTESIAN_POINT('',(52.9837652035058,40.9991129429665,25.6658251523972)) ;
#12253=CARTESIAN_POINT('Ctrl Pts',(52.7001365013421,40.9998895035356,25.4414732694626)) ;
#12254=CARTESIAN_POINT('Ctrl Pts',(52.759051244481,40.999992043072,25.4686292624549)) ;
#12255=CARTESIAN_POINT('Ctrl Pts',(52.8161909873028,41.0000522044823,25.5015720568016)) ;
#12256=CARTESIAN_POINT('Ctrl Pts',(52.8670872082483,40.9999435530579,25.5418312325623)) ;
#12257=CARTESIAN_POINT('Ctrl Pts',(52.9119925723242,40.9998476906997,25.5773516093475)) ;
#12258=CARTESIAN_POINT('Ctrl Pts',(52.9517624575517,40.9996209274521,25.6183455704352)) ;
#12259=CARTESIAN_POINT('Ctrl Pts',(52.9837652035057,40.9991129429665,25.6658251523971)) ;
#12260=CARTESIAN_POINT('',(53.0753072090447,40.9926056458522,25.9787173509598)) ;
#12261=CARTESIAN_POINT('Ctrl Pts',(52.9837652035058,40.9991129429665,25.6658251523972)) ;
#12262=CARTESIAN_POINT('Ctrl Pts',(53.0142076130435,40.9986297290861,25.7109895101566)) ;
#12263=CARTESIAN_POINT('Ctrl Pts',(53.0371279248959,40.9979127094772,25.7596817012363)) ;
#12264=CARTESIAN_POINT('Ctrl Pts',(53.052420112575,40.9968605874156,25.8119486082757)) ;
#12265=CARTESIAN_POINT('Ctrl Pts',(53.0683053848871,40.995767660373,25.8662426091512)) ;
#12266=CARTESIAN_POINT('Ctrl Pts',(53.0753072090447,40.9943530563869,25.9221663563878)) ;
#12267=CARTESIAN_POINT('Ctrl Pts',(53.0753072090447,40.9926056458522,25.9787173509598)) ;
#12268=CARTESIAN_POINT('',(52.974761325866,40.9788410048888,26.3096179008484)) ;
#12269=CARTESIAN_POINT('Ctrl Pts',(53.0753072090447,40.9926056458522,25.9787173509598)) ;
#12270=CARTESIAN_POINT('Ctrl Pts',(53.0753072090447,40.9908113092192,26.0367870026948)) ;
#12271=CARTESIAN_POINT('Ctrl Pts',(53.0670587148995,40.9887277985932,26.0936344221622)) ;
#12272=CARTESIAN_POINT('Ctrl Pts',(53.0501868887134,40.9863993988086,26.1491792206938)) ;
#12273=CARTESIAN_POINT('Ctrl Pts',(53.0328659874607,40.9840090243286,26.2062024474536)) ;
#12274=CARTESIAN_POINT('Ctrl Pts',(53.007140893577,40.9814572470054,26.2595987551357)) ;
#12275=CARTESIAN_POINT('Ctrl Pts',(52.974761325866,40.9788410048888,26.3096179008484)) ;
#12276=CARTESIAN_POINT('',(52.6858799643815,40.9643111807864,26.5512277126312)) ;
#12277=CARTESIAN_POINT('Ctrl Pts',(52.974761325866,40.9788410048888,26.3096179008484)) ;
#12278=CARTESIAN_POINT('Ctrl Pts',(52.9409768447557,40.9761112521767,26.361807221475)) ;
#12279=CARTESIAN_POINT('Ctrl Pts',(52.9000470821262,40.9734504375446,26.4077057301649)) ;
#12280=CARTESIAN_POINT('Ctrl Pts',(52.8523552454749,40.9710064235648,26.4476076413884)) ;
#12281=CARTESIAN_POINT('Ctrl Pts',(52.8019258671075,40.9684221216301,26.4897999476604)) ;
#12282=CARTESIAN_POINT('Ctrl Pts',(52.7456750630569,40.9661735116778,26.5238314938297)) ;
#12283=CARTESIAN_POINT('Ctrl Pts',(52.6858799643815,40.9643111807864,26.5512277126312)) ;
#12284=CARTESIAN_POINT('',(52.2619374580681,40.9582035055449,26.6375167608261)) ;
#12285=CARTESIAN_POINT('Ctrl Pts',(52.6858799643815,40.9643111807864,26.5512277126312)) ;
#12286=CARTESIAN_POINT('Ctrl Pts',(52.6217774636278,40.9623147018492,26.5805973450908)) ;
#12287=CARTESIAN_POINT('Ctrl Pts',(52.5548956312819,40.9607923362899,26.6018617749191)) ;
#12288=CARTESIAN_POINT('Ctrl Pts',(52.485782063455,40.9597766179076,26.6159332078567)) ;
#12289=CARTESIAN_POINT('Ctrl Pts',(52.412126253308,40.9586941450635,26.6309294354505)) ;
#12290=CARTESIAN_POINT('Ctrl Pts',(52.3371081527218,40.9582035055449,26.6375167608261)) ;
#12291=CARTESIAN_POINT('Ctrl Pts',(52.2619374580681,40.9582035055449,26.6375167608261)) ;
#12292=CARTESIAN_POINT('Ctrl Pts',(52.2619374580681,40.9582035055449,26.6375167608261)) ;
#12293=CARTESIAN_POINT('Ctrl Pts',(52.1706029250554,40.9582035055449,26.6375167608261)) ;
#12294=CARTESIAN_POINT('Ctrl Pts',(52.0775135059191,40.958659550423,26.631411163429)) ;
#12295=CARTESIAN_POINT('Ctrl Pts',(51.9875030125669,40.959789307142,26.6157574013999)) ;
#12296=CARTESIAN_POINT('Ctrl Pts',(51.9102085211818,40.9607594603733,26.6023150845183)) ;
#12297=CARTESIAN_POINT('Ctrl Pts',(51.8334991343029,40.9622519469216,26.5815425242443)) ;
#12298=CARTESIAN_POINT('Ctrl Pts',(51.7614599056542,40.9643621744601,26.5504772901535)) ;
#12299=CARTESIAN_POINT('',(54.7800817079842,40.9828316466601,26.2293313384056)) ;
#12300=CARTESIAN_POINT('',(54.9166436977684,40.9990723481228,25.6695769667625)) ;
#12301=CARTESIAN_POINT('Ctrl Pts',(54.7800817079842,40.9828316466601,26.2293313384056)) ;
#12302=CARTESIAN_POINT('Ctrl Pts',(54.8073320969825,40.9841999355338,26.2002842028176)) ;
#12303=CARTESIAN_POINT('Ctrl Pts',(54.8283420621742,40.9857487026283,26.1655109637859)) ;
#12304=CARTESIAN_POINT('Ctrl Pts',(54.8447345970925,40.9872223620408,26.1292404220201)) ;
#12305=CARTESIAN_POINT('Ctrl Pts',(54.8590713359577,40.9885112090848,26.0975185871489)) ;
#12306=CARTESIAN_POINT('Ctrl Pts',(54.8704235300848,40.9897852011198,26.0634298467531)) ;
#12307=CARTESIAN_POINT('Ctrl Pts',(54.879448285824,40.9909699924001,26.0287344920374)) ;
#12308=CARTESIAN_POINT('Ctrl Pts',(54.887578869659,40.9920373946778,25.9974767496277)) ;
#12309=CARTESIAN_POINT('Ctrl Pts',(54.8938224906964,40.9930323965364,25.9657308124313)) ;
#12310=CARTESIAN_POINT('Ctrl Pts',(54.898663241216,40.9939006335321,25.9347909362348)) ;
#12311=CARTESIAN_POINT('Ctrl Pts',(54.9097428391148,40.9958878701713,25.8639751844412)) ;
#12312=CARTESIAN_POINT('Ctrl Pts',(54.9147621112728,40.9974615661979,25.7890726554941)) ;
#12313=CARTESIAN_POINT('Ctrl Pts',(54.9161937701846,40.998487528179,25.7162401478558)) ;
#12314=CARTESIAN_POINT('Ctrl Pts',(54.9165017990757,40.9987082692569,25.7005698534987)) ;
#12315=CARTESIAN_POINT('Ctrl Pts',(54.9166436977684,40.9989036547566,25.6849952793808)) ;
#12316=CARTESIAN_POINT('Ctrl Pts',(54.9166436977684,40.9990723481228,25.6695769667625)) ;
#12317=CARTESIAN_POINT('',(54.9166436977684,40.960918459348,24.3999998211861)) ;
#12318=CARTESIAN_POINT('Origin',(54.9166436977684,25.5,25.5)) ;
#12319=CARTESIAN_POINT('',(55.2077760286629,40.960918459348,24.3999998211861)) ;
#12320=CARTESIAN_POINT('',(55.25,40.960918459348,24.3999998211861)) ;
#12321=CARTESIAN_POINT('',(55.2077760286629,40.9990558578356,25.6710775136948)) ;
#12322=CARTESIAN_POINT('Origin',(55.2077760286629,25.5,25.5)) ;
#12323=CARTESIAN_POINT('',(55.132742125541,40.9842840200094,26.1978168725967)) ;
#12324=CARTESIAN_POINT('Ctrl Pts',(55.2077760286629,40.9990558578356,25.6710775136948)) ;
#12325=CARTESIAN_POINT('Ctrl Pts',(55.2077760286629,40.9983582600139,25.7342775647813)) ;
#12326=CARTESIAN_POINT('Ctrl Pts',(55.2057352440292,40.9972316311301,25.7991446431383)) ;
#12327=CARTESIAN_POINT('Ctrl Pts',(55.2005903188716,40.9957334148724,25.8632654607297)) ;
#12328=CARTESIAN_POINT('Ctrl Pts',(55.197745628471,40.9949050332584,25.8987186245171)) ;
#12329=CARTESIAN_POINT('Ctrl Pts',(55.1939513161689,40.9939630530806,25.9339424643913)) ;
#12330=CARTESIAN_POINT('Ctrl Pts',(55.1890262614623,40.9929171841363,25.9685265472663)) ;
#12331=CARTESIAN_POINT('Ctrl Pts',(55.1795591851992,40.9909067859485,26.0350050271158)) ;
#12332=CARTESIAN_POINT('Ctrl Pts',(55.165290479564,40.9883698379393,26.1035339046001)) ;
#12333=CARTESIAN_POINT('Ctrl Pts',(55.1435864745192,40.985607725278,26.1677518901363)) ;
#12334=CARTESIAN_POINT('Ctrl Pts',(55.140160340722,40.9851717058649,26.177889162505)) ;
#12335=CARTESIAN_POINT('Ctrl Pts',(55.1365489609818,40.9847300755964,26.1879190732343)) ;
#12336=CARTESIAN_POINT('Ctrl Pts',(55.132742125541,40.9842840200094,26.1978168725967)) ;
#12337=CARTESIAN_POINT('',(54.8618688173592,40.966717363426,26.5152113080025)) ;
#12338=CARTESIAN_POINT('Ctrl Pts',(55.132742125541,40.9842840200094,26.1978168725967)) ;
#12339=CARTESIAN_POINT('Ctrl Pts',(55.1077726684432,40.9813583150401,26.2627371238591)) ;
#12340=CARTESIAN_POINT('Ctrl Pts',(55.0727465253504,40.9782964863988,26.321673362836)) ;
#12341=CARTESIAN_POINT('Ctrl Pts',(55.0276078044709,40.9753058232692,26.3745911480752)) ;
#12342=CARTESIAN_POINT('Ctrl Pts',(54.9801914455488,40.9721642553734,26.430179092292)) ;
#12343=CARTESIAN_POINT('Ctrl Pts',(54.9238555967464,40.9692583682441,26.476499166963)) ;
#12344=CARTESIAN_POINT('Ctrl Pts',(54.8618688173592,40.966717363426,26.5152113080025)) ;
#12345=CARTESIAN_POINT('',(54.3478848524392,40.9582035055449,26.6375167608261)) ;
#12346=CARTESIAN_POINT('Ctrl Pts',(54.8618688173592,40.966717363426,26.5152113080025)) ;
#12347=CARTESIAN_POINT('Ctrl Pts',(54.7923268047314,40.9638666562218,26.558641756684)) ;
#12348=CARTESIAN_POINT('Ctrl Pts',(54.7153634299227,40.9617853612427,26.5879136704149)) ;
#12349=CARTESIAN_POINT('Ctrl Pts',(54.63558100691,40.9604252913207,26.6069100286337)) ;
#12350=CARTESIAN_POINT('Ctrl Pts',(54.551584937626,40.9589933903696,26.6269096646542)) ;
#12351=CARTESIAN_POINT('Ctrl Pts',(54.4637386379212,40.9583406143964,26.6356835108198)) ;
#12352=CARTESIAN_POINT('Ctrl Pts',(54.3770957099285,40.9582231658519,26.6372543437853)) ;
#12353=CARTESIAN_POINT('Ctrl Pts',(54.3673410931221,40.9582099430122,26.6374311946143)) ;
#12354=CARTESIAN_POINT('Ctrl Pts',(54.357601744153,40.9582035055449,26.6375167608261)) ;
#12355=CARTESIAN_POINT('Ctrl Pts',(54.3478848524392,40.9582035055449,26.6375167608261)) ;
#12356=CARTESIAN_POINT('',(53.8421555347741,40.9656750313367,26.5309683918953)) ;
#12357=CARTESIAN_POINT('Ctrl Pts',(54.3478848524392,40.9582035055449,26.6375167608261)) ;
#12358=CARTESIAN_POINT('Ctrl Pts',(54.2542634562801,40.9582035055449,26.6375167608261)) ;
#12359=CARTESIAN_POINT('Ctrl Pts',(54.1585331971118,40.9587531431116,26.6301884706742)) ;
#12360=CARTESIAN_POINT('Ctrl Pts',(54.0668868671023,40.9601405009254,26.6108805928832)) ;
#12361=CARTESIAN_POINT('Ctrl Pts',(53.9887808020307,40.9613228838935,26.5944253528428)) ;
#12362=CARTESIAN_POINT('Ctrl Pts',(53.9123211210366,40.9631399744502,26.5689970708552)) ;
#12363=CARTESIAN_POINT('Ctrl Pts',(53.8421555347741,40.9656750313367,26.5309683918953)) ;
#12364=CARTESIAN_POINT('',(53.5615279264748,40.9831482719841,26.2225784301758)) ;
#12365=CARTESIAN_POINT('Ctrl Pts',(53.8421555347741,40.9656750313367,26.5309683918953)) ;
#12366=CARTESIAN_POINT('Ctrl Pts',(53.7789593365146,40.9679582798693,26.4967171189199)) ;
#12367=CARTESIAN_POINT('Ctrl Pts',(53.7221495836717,40.9707165493839,26.4538145079086)) ;
#12368=CARTESIAN_POINT('Ctrl Pts',(53.6737810081152,40.9738092463041,26.4006816357596)) ;
#12369=CARTESIAN_POINT('Ctrl Pts',(53.6258672853775,40.9768728598391,26.3480484193559)) ;
#12370=CARTESIAN_POINT('Ctrl Pts',(53.5888854642734,40.9800818012948,26.2882856508328)) ;
#12371=CARTESIAN_POINT('Ctrl Pts',(53.5615279264748,40.9831482719841,26.2225784301758)) ;
#12372=CARTESIAN_POINT('',(53.4774895496666,40.9990558578356,25.6710775136948)) ;
#12373=CARTESIAN_POINT('Ctrl Pts',(53.5615279264748,40.9831482719841,26.2225784301758)) ;
#12374=CARTESIAN_POINT('Ctrl Pts',(53.5408779349284,40.9854628895734,26.1729816447871)) ;
#12375=CARTESIAN_POINT('Ctrl Pts',(53.5253751590079,40.987678182784,26.1198997215806)) ;
#12376=CARTESIAN_POINT('Ctrl Pts',(53.513696600705,40.9896391569837,26.0664129848815)) ;
#12377=CARTESIAN_POINT('Ctrl Pts',(53.5076920063279,40.990647402552,26.0389124878081)) ;
#12378=CARTESIAN_POINT('Ctrl Pts',(53.5026976867563,40.9915884174085,26.0113061709377)) ;
#12379=CARTESIAN_POINT('Ctrl Pts',(53.4985341824635,40.9924411346845,25.9840120745748)) ;
#12380=CARTESIAN_POINT('Ctrl Pts',(53.4874089677846,40.9947196630803,25.9110800778353)) ;
#12381=CARTESIAN_POINT('Ctrl Pts',(53.4814376784056,40.9965384732081,25.8352569009168)) ;
#12382=CARTESIAN_POINT('Ctrl Pts',(53.4789345818655,40.9978067335497,25.7602369385911)) ;
#12383=CARTESIAN_POINT('Ctrl Pts',(53.477936122294,40.9983126296096,25.7303122440243)) ;
#12384=CARTESIAN_POINT('Ctrl Pts',(53.4774895496666,40.9987309260202,25.7005152594796)) ;
#12385=CARTESIAN_POINT('Ctrl Pts',(53.4774895496666,40.9990558578356,25.6710775136948)) ;
#12386=CARTESIAN_POINT('',(53.4774895496666,40.960918459348,24.3999998211861)) ;
#12387=CARTESIAN_POINT('Origin',(53.4774895496666,25.5,25.5)) ;
#12388=CARTESIAN_POINT('',(53.7686218805611,40.960918459348,24.3999998211861)) ;
#12389=CARTESIAN_POINT('',(55.25,40.960918459348,24.3999998211861)) ;
#12390=CARTESIAN_POINT('',(53.7686218805611,40.9990723481228,25.6695769667625)) ;
#12391=CARTESIAN_POINT('Origin',(53.7686218805611,25.5,25.5)) ;
#12392=CARTESIAN_POINT('',(53.8218959160149,40.9886898603816,26.0920189261436)) ;
#12393=CARTESIAN_POINT('Ctrl Pts',(53.7686218805611,40.9990723481228,25.6695769667625)) ;
#12394=CARTESIAN_POINT('Ctrl Pts',(53.7686218805611,40.9986536207666,25.7078479991484)) ;
#12395=CARTESIAN_POINT('Ctrl Pts',(53.7693327864037,40.9980612736987,25.747554686281)) ;
#12396=CARTESIAN_POINT('Ctrl Pts',(53.7711491226713,40.9973239200892,25.7872806686854)) ;
#12397=CARTESIAN_POINT('Ctrl Pts',(53.7731780641889,40.9965002579853,25.8316566449114)) ;
#12398=CARTESIAN_POINT('Ctrl Pts',(53.7765880391652,40.9954956560657,25.8760519633279)) ;
#12399=CARTESIAN_POINT('Ctrl Pts',(53.7819364452524,40.9943499971454,25.9184712247707)) ;
#12400=CARTESIAN_POINT('Ctrl Pts',(53.7853878563205,40.9936106853179,25.9458450453181)) ;
#12401=CARTESIAN_POINT('Ctrl Pts',(53.7899552866281,40.9927391021004,25.9748706921076)) ;
#12402=CARTESIAN_POINT('Ctrl Pts',(53.7961183617569,40.9918055707888,26.0035785313425)) ;
#12403=CARTESIAN_POINT('Ctrl Pts',(53.8013922531887,40.9910067256209,26.0281445189712)) ;
#12404=CARTESIAN_POINT('Ctrl Pts',(53.8078364687857,40.9901625181187,26.0524724327561)) ;
#12405=CARTESIAN_POINT('Ctrl Pts',(53.8157490150832,40.9893170139533,26.0753352441417)) ;
#12406=CARTESIAN_POINT('Ctrl Pts',(53.817706733993,40.9891078196648,26.0809919514137)) ;
#12407=CARTESIAN_POINT('Ctrl Pts',(53.819754261106,40.9888985459991,26.0865591905408)) ;
#12408=CARTESIAN_POINT('Ctrl Pts',(53.8218959160149,40.9886898603816,26.0920189261436)) ;
#12409=CARTESIAN_POINT('',(54.0049793310463,40.979270509389,26.3013641476631)) ;
#12410=CARTESIAN_POINT('Ctrl Pts',(53.8218959160149,40.9886898603816,26.0920189261436)) ;
#12411=CARTESIAN_POINT('Ctrl Pts',(53.8392210714188,40.9870016937733,26.1361855699338)) ;
#12412=CARTESIAN_POINT('Ctrl Pts',(53.863050596707,40.9852704674679,26.1765182482562)) ;
#12413=CARTESIAN_POINT('Ctrl Pts',(53.8942812696197,40.9836275207232,26.2122350732055)) ;
#12414=CARTESIAN_POINT('Ctrl Pts',(53.9258591431538,40.9819663088538,26.2483489726542)) ;
#12415=CARTESIAN_POINT('Ctrl Pts',(53.9632279991133,40.9804949283934,26.2777130858558)) ;
#12416=CARTESIAN_POINT('Ctrl Pts',(54.0049793310463,40.979270509389,26.3013641476631)) ;
#12417=CARTESIAN_POINT('',(54.3223734684289,40.9752885064464,26.3748975038528)) ;
#12418=CARTESIAN_POINT('Ctrl Pts',(54.0049793310463,40.979270509389,26.3013641476631)) ;
#12419=CARTESIAN_POINT('Ctrl Pts',(54.0501187277971,40.9779467304179,26.3269344615446)) ;
#12420=CARTESIAN_POINT('Ctrl Pts',(54.0986649923769,40.9769653080002,26.344797292249)) ;
#12421=CARTESIAN_POINT('Ctrl Pts',(54.1492147081544,40.9763170829053,26.3565100988152)) ;
#12422=CARTESIAN_POINT('Ctrl Pts',(54.2057771722795,40.9755917532351,26.3696161112036)) ;
#12423=CARTESIAN_POINT('Ctrl Pts',(54.2643222776773,40.9752885064464,26.3748975038528)) ;
#12424=CARTESIAN_POINT('Ctrl Pts',(54.3223734684289,40.9752885064464,26.3748975038528)) ;
#12425=CARTESIAN_POINT('Ctrl Pts',(54.3223734684289,40.9752885064464,26.3748975038528)) ;
#12426=CARTESIAN_POINT('Ctrl Pts',(54.3786363553446,40.9752885064464,26.3748975038528)) ;
#12427=CARTESIAN_POINT('Ctrl Pts',(54.437258969987,40.9754864304333,26.3715512815695)) ;
#12428=CARTESIAN_POINT('Ctrl Pts',(54.4943479752787,40.9759914778937,26.3624599312309)) ;
#12429=CARTESIAN_POINT('Ctrl Pts',(54.5295757696573,40.9763031264851,26.3568499504874)) ;
#12430=CARTESIAN_POINT('Ctrl Pts',(54.564217237808,40.9767317193511,26.3490505124776)) ;
#12431=CARTESIAN_POINT('Ctrl Pts',(54.5973694346344,40.9773029142982,26.3385073041163)) ;
#12432=CARTESIAN_POINT('Ctrl Pts',(54.6331824164753,40.9779199531743,26.3271179011285)) ;
#12433=CARTESIAN_POINT('Ctrl Pts',(54.668007874159,40.9787129882677,26.3122910476793)) ;
#12434=CARTESIAN_POINT('Ctrl Pts',(54.7002658204309,40.9797004593973,26.2930155656316)) ;
#12435=CARTESIAN_POINT('Ctrl Pts',(54.7297345351508,40.9806025473594,26.2754067669572)) ;
#12436=CARTESIAN_POINT('Ctrl Pts',(54.7565994843863,40.9816525638485,26.2543618556874)) ;
#12437=CARTESIAN_POINT('Ctrl Pts',(54.7800817079842,40.9828316466601,26.2293313384056)) ;
#12438=CARTESIAN_POINT('',(55.9641196317971,40.9807202883652,24.7271485567093)) ;
#12439=CARTESIAN_POINT('',(55.9641196317971,40.9609184856404,26.5999998092651)) ;
#12440=CARTESIAN_POINT('Origin',(55.9641196317971,25.5,25.5)) ;
#12441=CARTESIAN_POINT('',(55.6834920234978,40.9609184856404,26.5999998092651)) ;
#12442=CARTESIAN_POINT('',(55.25,40.9609184856404,26.5999998092651)) ;
#12443=CARTESIAN_POINT('',(55.6834920234978,40.960918459348,24.3999998211861)) ;
#12444=CARTESIAN_POINT('Origin',(55.6834920234978,25.5,25.5)) ;
#12445=CARTESIAN_POINT('',(56.1216910667717,40.960918459348,24.3999998211861)) ;
#12446=CARTESIAN_POINT('',(55.25,40.960918459348,24.3999998211861)) ;
#12447=CARTESIAN_POINT('',(56.6424276418984,40.99324057365,25.9577079057693)) ;
#12448=CARTESIAN_POINT('Origin',(56.4894174279709,25.5,25.5)) ;
#12449=CARTESIAN_POINT('',(56.747475463897,40.9801923016591,26.2833557963371)) ;
#12450=CARTESIAN_POINT('Ctrl Pts',(56.6424276418984,40.99324057365,25.9577079057693)) ;
#12451=CARTESIAN_POINT('Ctrl Pts',(56.6483878638642,40.9927086674222,25.9757127316555)) ;
#12452=CARTESIAN_POINT('Ctrl Pts',(56.6543262857709,40.9921439410553,25.993694115101)) ;
#12453=CARTESIAN_POINT('Ctrl Pts',(56.6602487671082,40.9915482457722,26.0116790901449)) ;
#12454=CARTESIAN_POINT('Ctrl Pts',(56.6660136628558,40.9909684007698,26.0291855203464)) ;
#12455=CARTESIAN_POINT('Ctrl Pts',(56.6717635353025,40.9903592129697,26.0466955789032)) ;
#12456=CARTESIAN_POINT('Ctrl Pts',(56.6774876311401,40.9897223897193,26.0641888337385)) ;
#12457=CARTESIAN_POINT('Ctrl Pts',(56.6829741240545,40.9891120005242,26.0809559566915)) ;
#12458=CARTESIAN_POINT('Ctrl Pts',(56.6884369760154,40.9884762225162,26.0977077546731)) ;
#12459=CARTESIAN_POINT('Ctrl Pts',(56.69385087,40.987816559134,26.1143817395123)) ;
#12460=CARTESIAN_POINT('Ctrl Pts',(56.697488469878,40.987373330758,26.1255850038151)) ;
#12461=CARTESIAN_POINT('Ctrl Pts',(56.7011036475429,40.9869193193124,26.1367522405779)) ;
#12462=CARTESIAN_POINT('Ctrl Pts',(56.7046842492072,40.9864549808355,26.1478519325859)) ;
#12463=CARTESIAN_POINT('Ctrl Pts',(56.7088048246254,40.9859206176494,26.1606255171189)) ;
#12464=CARTESIAN_POINT('Ctrl Pts',(56.7129698449496,40.9853585848336,26.1735891038181)) ;
#12465=CARTESIAN_POINT('Ctrl Pts',(56.717138316371,40.9847773802594,26.1866350483889)) ;
#12466=CARTESIAN_POINT('Ctrl Pts',(56.7211924167408,40.9842121222929,26.1993230491842)) ;
#12467=CARTESIAN_POINT('Ctrl Pts',(56.7252498680784,40.9836287301731,26.2120891938011)) ;
#12468=CARTESIAN_POINT('Ctrl Pts',(56.7292568099678,40.9830350213146,26.2247891155873)) ;
#12469=CARTESIAN_POINT('Ctrl Pts',(56.7331081381488,40.9824643697502,26.2369958228523)) ;
#12470=CARTESIAN_POINT('Ctrl Pts',(56.7369128454569,40.9818841872093,26.2491414678219)) ;
#12471=CARTESIAN_POINT('Ctrl Pts',(56.7406071105412,40.9813014152283,26.2610529483142)) ;
#12472=CARTESIAN_POINT('Ctrl Pts',(56.7429478552524,40.9809321616958,26.2686002505048)) ;
#12473=CARTESIAN_POINT('Ctrl Pts',(56.745243940517,40.9805618685835,26.2760526435616)) ;
#12474=CARTESIAN_POINT('Ctrl Pts',(56.747475463897,40.9801923016591,26.2833557963371)) ;
#12475=CARTESIAN_POINT('',(56.8645288534462,40.9940150133522,25.9306956768036)) ;
#12476=CARTESIAN_POINT('Ctrl Pts',(56.747475463897,40.9801923016591,26.2833557963371)) ;
#12477=CARTESIAN_POINT('Ctrl Pts',(56.7516296828433,40.9808650039904,26.270062269309)) ;
#12478=CARTESIAN_POINT('Ctrl Pts',(56.7559705130544,40.9815364551589,26.2563722372977)) ;
#12479=CARTESIAN_POINT('Ctrl Pts',(56.7604101116033,40.9821985064012,26.2425142185715)) ;
#12480=CARTESIAN_POINT('Ctrl Pts',(56.7649522311146,40.9828758459922,26.2283361850062)) ;
#12481=CARTESIAN_POINT('Ctrl Pts',(56.7695978154572,40.9835433465108,26.2139820964589)) ;
#12482=CARTESIAN_POINT('Ctrl Pts',(56.7742722747122,40.9841922815339,26.1996444922584)) ;
#12483=CARTESIAN_POINT('Ctrl Pts',(56.7791213439405,40.9848654569067,26.1847713205086)) ;
#12484=CARTESIAN_POINT('Ctrl Pts',(56.7840015368633,40.9855186538863,26.1699157502043)) ;
#12485=CARTESIAN_POINT('Ctrl Pts',(56.7888493368058,40.9861421311643,26.1552398169195)) ;
#12486=CARTESIAN_POINT('Ctrl Pts',(56.7910657916994,40.986427190218,26.1485298568278)) ;
#12487=CARTESIAN_POINT('Ctrl Pts',(56.7932757361307,40.9867060366793,26.1418567490044)) ;
#12488=CARTESIAN_POINT('Ctrl Pts',(56.79547434982,40.9869777395263,26.1352326309442)) ;
#12489=CARTESIAN_POINT('Ctrl Pts',(56.8015533905598,40.9877289823135,26.1169173244634)) ;
#12490=CARTESIAN_POINT('Ctrl Pts',(56.8077231978965,40.9884516701256,26.0984417037313)) ;
#12491=CARTESIAN_POINT('Ctrl Pts',(56.8139415434462,40.9891439875036,26.0799085148923)) ;
#12492=CARTESIAN_POINT('Ctrl Pts',(56.8203227048416,40.9898544319281,26.0608900688751)) ;
#12493=CARTESIAN_POINT('Ctrl Pts',(56.8267550759624,40.990532894711,26.0418107422561)) ;
#12494=CARTESIAN_POINT('Ctrl Pts',(56.8332127360803,40.9911774140237,26.0227287647321)) ;
#12495=CARTESIAN_POINT('Ctrl Pts',(56.8399288127184,40.9918477250992,26.0028831827229)) ;
#12496=CARTESIAN_POINT('Ctrl Pts',(56.8466722984513,40.9924813217134,25.9830345844242)) ;
#12497=CARTESIAN_POINT('Ctrl Pts',(56.8534339469647,40.9930759969675,25.9631951372186)) ;
#12498=CARTESIAN_POINT('Ctrl Pts',(56.8571262434297,40.9934007280348,25.9523615186654)) ;
#12499=CARTESIAN_POINT('Ctrl Pts',(56.8608242923809,40.9937138532788,25.941529727271)) ;
#12500=CARTESIAN_POINT('Ctrl Pts',(56.8645288534462,40.9940150133522,25.9306956768036)) ;
#12501=CARTESIAN_POINT('',(57.3912682123482,40.960918459348,24.3999998211861)) ;
#12502=CARTESIAN_POINT('Origin',(57.0127388089699,25.5,25.5)) ;
#12503=CARTESIAN_POINT('',(57.782945830375,40.960918459348,24.3999998211861)) ;
#12504=CARTESIAN_POINT('',(55.25,40.960918459348,24.3999998211861)) ;
#12505=CARTESIAN_POINT('',(57.782945830375,40.9609184856404,26.5999998092651)) ;
#12506=CARTESIAN_POINT('Origin',(57.782945830375,25.5,25.5)) ;
#12507=CARTESIAN_POINT('',(57.5023188181221,40.9609184856404,26.5999998092651)) ;
#12508=CARTESIAN_POINT('',(55.25,40.9609184856404,26.5999998092651)) ;
#12509=CARTESIAN_POINT('',(57.5023188181221,40.9822614389786,24.7586628735065)) ;
#12510=CARTESIAN_POINT('Origin',(57.5023188181221,25.5,25.5)) ;
#12511=CARTESIAN_POINT('',(56.8630280084908,40.9609184856404,26.5999998092651)) ;
#12512=CARTESIAN_POINT('Origin',(57.2449351733355,25.5,25.5)) ;
#12513=CARTESIAN_POINT('',(56.6004087515175,40.9609184856404,26.5999998092651)) ;
#12514=CARTESIAN_POINT('',(55.25,40.9609184856404,26.5999998092651)) ;
#12515=CARTESIAN_POINT('Origin',(56.2266909192151,25.5,25.5)) ;
#12516=CARTESIAN_POINT('',(58.5933150835335,40.960918459348,24.3999998211861)) ;
#12517=CARTESIAN_POINT('',(58.5933150835335,40.9609184856404,26.5999998092651)) ;
#12518=CARTESIAN_POINT('Origin',(58.5933150835335,25.5,25.5)) ;
#12519=CARTESIAN_POINT('',(58.3021833486855,40.9609184856404,26.5999998092651)) ;
#12520=CARTESIAN_POINT('',(55.25,40.9609184856404,26.5999998092651)) ;
#12521=CARTESIAN_POINT('',(58.3021833486855,40.960918459348,24.3999998211861)) ;
#12522=CARTESIAN_POINT('Origin',(58.3021833486855,25.5,25.5)) ;
#12523=CARTESIAN_POINT('',(55.25,40.960918459348,24.3999998211861)) ;
#12524=CARTESIAN_POINT('',(50.9098227806389,40.960918459348,24.3999998211861)) ;
#12525=CARTESIAN_POINT('',(50.9098227806389,40.9609184856404,26.5999998092651)) ;
#12526=CARTESIAN_POINT('Origin',(50.9098227806389,25.5,25.5)) ;
#12527=CARTESIAN_POINT('',(50.6186904497445,40.9609184856404,26.5999998092651)) ;
#12528=CARTESIAN_POINT('',(55.25,40.9609184856404,26.5999998092651)) ;
#12529=CARTESIAN_POINT('',(50.6186904497445,40.960918459348,24.3999998211861)) ;
#12530=CARTESIAN_POINT('Origin',(50.6186904497445,25.5,25.5)) ;
#12531=CARTESIAN_POINT('',(55.25,40.960918459348,24.3999998211861)) ;
#12532=CARTESIAN_POINT('Origin',(50.6186904497445,41.5,26.5999998092651)) ;
#12533=CARTESIAN_POINT('',(50.6186904497445,40.85,26.5999998092651)) ;
#12534=CARTESIAN_POINT('',(50.6186904497445,41.5,26.5999998092651)) ;
#12535=CARTESIAN_POINT('',(50.6186904497445,40.85,24.3999998211861)) ;
#12536=CARTESIAN_POINT('',(50.6186904497445,40.85,26.5999998092651)) ;
#12537=CARTESIAN_POINT('',(50.6186904497445,41.5,24.3999998211861)) ;
#12538=CARTESIAN_POINT('Origin',(50.6186904497445,41.5,24.3999998211861)) ;
#12539=CARTESIAN_POINT('',(50.9098227806389,40.85,24.3999998211861)) ;
#12540=CARTESIAN_POINT('',(50.6186904497445,40.85,24.3999998211861)) ;
#12541=CARTESIAN_POINT('',(50.9098227806389,41.5,24.3999998211861)) ;
#12542=CARTESIAN_POINT('Origin',(50.9098227806389,41.5,24.3999998211861)) ;
#12543=CARTESIAN_POINT('',(50.9098227806389,40.85,26.5999998092651)) ;
#12544=CARTESIAN_POINT('',(50.9098227806389,40.85,24.3999998211861)) ;
#12545=CARTESIAN_POINT('',(50.9098227806389,41.5,26.5999998092651)) ;
#12546=CARTESIAN_POINT('Origin',(50.9098227806389,41.5,26.5999998092651)) ;
#12547=CARTESIAN_POINT('',(50.9098227806389,40.85,26.5999998092651)) ;
#12548=CARTESIAN_POINT('Origin',(53.2966575417668,40.85,25.4999998152256)) ;
#12549=CARTESIAN_POINT('Origin',(58.3021833486855,41.5,26.5999998092651)) ;
#12550=CARTESIAN_POINT('',(58.3021833486855,40.85,26.5999998092651)) ;
#12551=CARTESIAN_POINT('',(58.3021833486855,41.5,26.5999998092651)) ;
#12552=CARTESIAN_POINT('',(58.3021833486855,40.85,24.3999998211861)) ;
#12553=CARTESIAN_POINT('',(58.3021833486855,40.85,26.5999998092651)) ;
#12554=CARTESIAN_POINT('',(58.3021833486855,41.5,24.3999998211861)) ;
#12555=CARTESIAN_POINT('Origin',(58.3021833486855,41.5,24.3999998211861)) ;
#12556=CARTESIAN_POINT('',(58.5933150835335,40.85,24.3999998211861)) ;
#12557=CARTESIAN_POINT('',(58.3021833486855,40.85,24.3999998211861)) ;
#12558=CARTESIAN_POINT('',(58.5933150835335,41.5,24.3999998211861)) ;
#12559=CARTESIAN_POINT('Origin',(58.5933150835335,41.5,24.3999998211861)) ;
#12560=CARTESIAN_POINT('',(58.5933150835335,40.85,26.5999998092651)) ;
#12561=CARTESIAN_POINT('',(58.5933150835335,40.85,24.3999998211861)) ;
#12562=CARTESIAN_POINT('',(58.5933150835335,41.5,26.5999998092651)) ;
#12563=CARTESIAN_POINT('Origin',(58.5933150835335,41.5,26.5999998092651)) ;
#12564=CARTESIAN_POINT('',(58.5933150835335,40.85,26.5999998092651)) ;
#12565=CARTESIAN_POINT('Origin',(53.2966575417668,40.85,25.4999998152256)) ;
#12566=CARTESIAN_POINT('Origin',(57.3912682123482,41.5,24.3999998211861)) ;
#12567=CARTESIAN_POINT('',(57.3912682123482,40.85,24.3999998211861)) ;
#12568=CARTESIAN_POINT('',(57.3912682123482,41.5,24.3999998211861)) ;
#12569=CARTESIAN_POINT('',(57.782945830375,40.85,24.3999998211861)) ;
#12570=CARTESIAN_POINT('',(57.3912682123482,40.85,24.3999998211861)) ;
#12571=CARTESIAN_POINT('',(57.782945830375,41.5,24.3999998211861)) ;
#12572=CARTESIAN_POINT('Origin',(57.782945830375,41.5,24.3999998211861)) ;
#12573=CARTESIAN_POINT('',(57.782945830375,40.85,26.5999998092651)) ;
#12574=CARTESIAN_POINT('',(57.782945830375,40.85,24.3999998211861)) ;
#12575=CARTESIAN_POINT('',(57.782945830375,41.5,26.5999998092651)) ;
#12576=CARTESIAN_POINT('Origin',(57.782945830375,41.5,26.5999998092651)) ;
#12577=CARTESIAN_POINT('',(57.5023188181221,40.85,26.5999998092651)) ;
#12578=CARTESIAN_POINT('',(57.782945830375,40.85,26.5999998092651)) ;
#12579=CARTESIAN_POINT('',(57.5023188181221,41.5,26.5999998092651)) ;
#12580=CARTESIAN_POINT('Origin',(57.5023188181221,41.5,26.5999998092651)) ;
#12581=CARTESIAN_POINT('',(57.5023188181221,40.85,24.7586628735065)) ;
#12582=CARTESIAN_POINT('',(57.5023188181221,40.85,26.5999998092651)) ;
#12583=CARTESIAN_POINT('',(57.5023188181221,41.5,24.7586628735065)) ;
#12584=CARTESIAN_POINT('Origin',(57.5023188181221,41.5,24.7586628735065)) ;
#12585=CARTESIAN_POINT('',(56.8630280084908,40.85,26.5999998092651)) ;
#12586=CARTESIAN_POINT('',(57.5023188181221,40.85,24.7586628735065)) ;
#12587=CARTESIAN_POINT('',(56.8630280084908,41.5,26.5999998092651)) ;
#12588=CARTESIAN_POINT('Origin',(56.8630280084908,41.5,26.5999998092651)) ;
#12589=CARTESIAN_POINT('',(56.6004087515175,40.85,26.5999998092651)) ;
#12590=CARTESIAN_POINT('',(56.8630280084908,40.85,26.5999998092651)) ;
#12591=CARTESIAN_POINT('',(56.6004087515175,41.5,26.5999998092651)) ;
#12592=CARTESIAN_POINT('Origin',(56.6004087515175,41.5,26.5999998092651)) ;
#12593=CARTESIAN_POINT('',(55.9641196317971,40.85,24.7271485567093)) ;
#12594=CARTESIAN_POINT('',(56.6004087515175,40.85,26.5999998092651)) ;
#12595=CARTESIAN_POINT('',(55.9641196317971,41.5,24.7271485567093)) ;
#12596=CARTESIAN_POINT('Origin',(55.9641196317971,41.5,24.7271485567093)) ;
#12597=CARTESIAN_POINT('',(55.9641196317971,40.85,26.5999998092651)) ;
#12598=CARTESIAN_POINT('',(55.9641196317971,40.85,24.7271485567093)) ;
#12599=CARTESIAN_POINT('',(55.9641196317971,41.5,26.5999998092651)) ;
#12600=CARTESIAN_POINT('Origin',(56.8645288534462,41.5,25.9306956768036)) ;
#12601=CARTESIAN_POINT('',(56.8645288534462,40.85,25.9306956768036)) ;
#12602=CARTESIAN_POINT('',(56.8645288534462,41.5,25.9306956768036)) ;
#12603=CARTESIAN_POINT('',(56.8645288534462,40.85,25.9306956768036)) ;
#12604=CARTESIAN_POINT('Ctrl Pts',(56.747475463897,41.5,26.2833557963371)) ;
#12605=CARTESIAN_POINT('Ctrl Pts',(56.747475463897,40.85,26.2833557963371)) ;
#12606=CARTESIAN_POINT('Ctrl Pts',(56.784992415458,41.5,26.1633013129234)) ;
#12607=CARTESIAN_POINT('Ctrl Pts',(56.784992415458,40.85,26.1633013129234)) ;
#12608=CARTESIAN_POINT('Ctrl Pts',(56.8645288534462,41.5,25.9306956768036)) ;
#12609=CARTESIAN_POINT('Ctrl Pts',(56.8645288534462,40.85,25.9306956768036)) ;
#12610=CARTESIAN_POINT('',(56.747475463897,40.85,26.2833557963371)) ;
#12611=CARTESIAN_POINT('',(56.747475463897,41.5,26.2833557963371)) ;
#12612=CARTESIAN_POINT('Ctrl Pts',(56.747475463897,40.85,26.2833557963371)) ;
#12613=CARTESIAN_POINT('Ctrl Pts',(56.784992415458,40.85,26.1633013129234)) ;
#12614=CARTESIAN_POINT('Ctrl Pts',(56.8645288534462,40.85,25.9306956768036)) ;
#12615=CARTESIAN_POINT('Ctrl Pts',(56.6424276418984,41.5,25.9577079057693)) ;
#12616=CARTESIAN_POINT('Ctrl Pts',(56.6424276418984,40.85,25.9577079057693)) ;
#12617=CARTESIAN_POINT('Ctrl Pts',(56.7144604511559,41.5,26.1753068804741)) ;
#12618=CARTESIAN_POINT('Ctrl Pts',(56.7144604511559,40.85,26.1753068804741)) ;
#12619=CARTESIAN_POINT('Ctrl Pts',(56.747475463897,41.5,26.2833557963371)) ;
#12620=CARTESIAN_POINT('Ctrl Pts',(56.747475463897,40.85,26.2833557963371)) ;
#12621=CARTESIAN_POINT('',(56.6424276418984,40.85,25.9577079057693)) ;
#12622=CARTESIAN_POINT('',(56.6424276418984,41.5,25.9577079057693)) ;
#12623=CARTESIAN_POINT('Ctrl Pts',(56.6424276418984,40.85,25.9577079057693)) ;
#12624=CARTESIAN_POINT('Ctrl Pts',(56.7144604511559,40.85,26.1753068804741)) ;
#12625=CARTESIAN_POINT('Ctrl Pts',(56.747475463897,40.85,26.2833557963371)) ;
#12626=CARTESIAN_POINT('Origin',(56.1216910667717,41.5,24.3999998211861)) ;
#12627=CARTESIAN_POINT('',(56.1216910667717,40.85,24.3999998211861)) ;
#12628=CARTESIAN_POINT('',(56.1216910667717,41.5,24.3999998211861)) ;
#12629=CARTESIAN_POINT('',(56.1216910667717,40.85,24.3999998211861)) ;
#12630=CARTESIAN_POINT('Origin',(55.6834920234978,41.5,24.3999998211861)) ;
#12631=CARTESIAN_POINT('',(55.6834920234978,40.85,24.3999998211861)) ;
#12632=CARTESIAN_POINT('',(55.6834920234978,41.5,24.3999998211861)) ;
#12633=CARTESIAN_POINT('',(55.6834920234978,40.85,24.3999998211861)) ;
#12634=CARTESIAN_POINT('Origin',(55.6834920234978,41.5,26.5999998092651)) ;
#12635=CARTESIAN_POINT('',(55.6834920234978,40.85,26.5999998092651)) ;
#12636=CARTESIAN_POINT('',(55.6834920234978,41.5,26.5999998092651)) ;
#12637=CARTESIAN_POINT('',(55.6834920234978,40.85,26.5999998092651)) ;
#12638=CARTESIAN_POINT('Origin',(55.9641196317971,41.5,26.5999998092651)) ;
#12639=CARTESIAN_POINT('',(55.9641196317971,40.85,26.5999998092651)) ;
#12640=CARTESIAN_POINT('Origin',(53.2966575417668,40.85,25.4999998152256)) ;
#12641=CARTESIAN_POINT('Ctrl Pts',(53.5615279264748,41.5,26.2225784301758)) ;
#12642=CARTESIAN_POINT('Ctrl Pts',(53.5615279264748,40.85,26.2225784301758)) ;
#12643=CARTESIAN_POINT('Ctrl Pts',(53.4774895496666,41.5,26.0207365393639)) ;
#12644=CARTESIAN_POINT('Ctrl Pts',(53.4774895496666,40.85,26.0207365393639)) ;
#12645=CARTESIAN_POINT('Ctrl Pts',(53.4774895496666,41.5,25.6710775136948)) ;
#12646=CARTESIAN_POINT('Ctrl Pts',(53.4774895496666,40.85,25.6710775136948)) ;
#12647=CARTESIAN_POINT('',(53.5615279264748,40.85,26.2225784301758)) ;
#12648=CARTESIAN_POINT('',(53.5615279264748,41.5,26.2225784301758)) ;
#12649=CARTESIAN_POINT('',(53.4774895496666,40.85,25.6710775136948)) ;
#12650=CARTESIAN_POINT('Ctrl Pts',(53.5615279264748,40.85,26.2225784301758)) ;
#12651=CARTESIAN_POINT('Ctrl Pts',(53.4774895496666,40.85,26.0207365393639)) ;
#12652=CARTESIAN_POINT('Ctrl Pts',(53.4774895496666,40.85,25.6710775136948)) ;
#12653=CARTESIAN_POINT('',(53.4774895496666,41.5,25.6710775136948)) ;
#12654=CARTESIAN_POINT('Origin',(53.4774895496666,41.5,25.6710775136948)) ;
#12655=CARTESIAN_POINT('',(53.4774895496666,40.85,24.3999998211861)) ;
#12656=CARTESIAN_POINT('',(53.4774895496666,40.85,25.6710775136948)) ;
#12657=CARTESIAN_POINT('',(53.4774895496666,41.5,24.3999998211861)) ;
#12658=CARTESIAN_POINT('Origin',(53.4774895496666,41.5,24.3999998211861)) ;
#12659=CARTESIAN_POINT('',(53.7686218805611,40.85,24.3999998211861)) ;
#12660=CARTESIAN_POINT('',(53.4774895496666,40.85,24.3999998211861)) ;
#12661=CARTESIAN_POINT('',(53.7686218805611,41.5,24.3999998211861)) ;
#12662=CARTESIAN_POINT('Origin',(53.7686218805611,41.5,24.3999998211861)) ;
#12663=CARTESIAN_POINT('',(53.7686218805611,40.85,25.6695769667625)) ;
#12664=CARTESIAN_POINT('',(53.7686218805611,40.85,24.3999998211861)) ;
#12665=CARTESIAN_POINT('',(53.7686218805611,41.5,25.6695769667625)) ;
#12666=CARTESIAN_POINT('Ctrl Pts',(53.7686218805611,41.5,25.6695769667625)) ;
#12667=CARTESIAN_POINT('Ctrl Pts',(53.7686218805611,40.85,25.6695769667625)) ;
#12668=CARTESIAN_POINT('Ctrl Pts',(53.7686218805611,41.5,25.9562070608139)) ;
#12669=CARTESIAN_POINT('Ctrl Pts',(53.7686218805611,40.85,25.9562070608139)) ;
#12670=CARTESIAN_POINT('Ctrl Pts',(53.8218959160149,41.5,26.0920189261436)) ;
#12671=CARTESIAN_POINT('Ctrl Pts',(53.8218959160149,40.85,26.0920189261436)) ;
#12672=CARTESIAN_POINT('',(53.8218959160149,40.85,26.0920189261436)) ;
#12673=CARTESIAN_POINT('Ctrl Pts',(53.7686218805611,40.85,25.6695769667625)) ;
#12674=CARTESIAN_POINT('Ctrl Pts',(53.7686218805611,40.85,25.9562070608139)) ;
#12675=CARTESIAN_POINT('Ctrl Pts',(53.8218959160149,40.85,26.0920189261436)) ;
#12676=CARTESIAN_POINT('',(53.8218959160149,41.5,26.0920189261436)) ;
#12677=CARTESIAN_POINT('Ctrl Pts',(53.8218959160149,41.5,26.0920189261436)) ;
#12678=CARTESIAN_POINT('Ctrl Pts',(53.8218959160149,40.85,26.0920189261436)) ;
#12679=CARTESIAN_POINT('Ctrl Pts',(53.8751705475152,41.5,26.2278307914734)) ;
#12680=CARTESIAN_POINT('Ctrl Pts',(53.8751705475152,40.85,26.2278307914734)) ;
#12681=CARTESIAN_POINT('Ctrl Pts',(54.0049793310463,41.5,26.3013641476631)) ;
#12682=CARTESIAN_POINT('Ctrl Pts',(54.0049793310463,40.85,26.3013641476631)) ;
#12683=CARTESIAN_POINT('',(54.0049793310463,40.85,26.3013641476631)) ;
#12684=CARTESIAN_POINT('Ctrl Pts',(53.8218959160149,40.85,26.0920189261436)) ;
#12685=CARTESIAN_POINT('Ctrl Pts',(53.8751705475152,40.85,26.2278307914734)) ;
#12686=CARTESIAN_POINT('Ctrl Pts',(54.0049793310463,40.85,26.3013641476631)) ;
#12687=CARTESIAN_POINT('',(54.0049793310463,41.5,26.3013641476631)) ;
#12688=CARTESIAN_POINT('Ctrl Pts',(54.0049793310463,41.5,26.3013641476631)) ;
#12689=CARTESIAN_POINT('Ctrl Pts',(54.0049793310463,40.85,26.3013641476631)) ;
#12690=CARTESIAN_POINT('Ctrl Pts',(54.1347881145775,41.5,26.3748975038528)) ;
#12691=CARTESIAN_POINT('Ctrl Pts',(54.1347881145775,40.85,26.3748975038528)) ;
#12692=CARTESIAN_POINT('Ctrl Pts',(54.3223734684289,41.5,26.3748975038528)) ;
#12693=CARTESIAN_POINT('Ctrl Pts',(54.3223734684289,40.85,26.3748975038528)) ;
#12694=CARTESIAN_POINT('',(54.3223734684289,40.85,26.3748975038528)) ;
#12695=CARTESIAN_POINT('Ctrl Pts',(54.0049793310463,40.85,26.3013641476631)) ;
#12696=CARTESIAN_POINT('Ctrl Pts',(54.1347881145775,40.85,26.3748975038528)) ;
#12697=CARTESIAN_POINT('Ctrl Pts',(54.3223734684289,40.85,26.3748975038528)) ;
#12698=CARTESIAN_POINT('',(54.3223734684289,41.5,26.3748975038528)) ;
#12699=CARTESIAN_POINT('Ctrl Pts',(54.3223734684289,41.5,26.3748975038528)) ;
#12700=CARTESIAN_POINT('Ctrl Pts',(54.3223734684289,40.85,26.3748975038528)) ;
#12701=CARTESIAN_POINT('Ctrl Pts',(54.6435197182,41.5,26.3748975038528)) ;
#12702=CARTESIAN_POINT('Ctrl Pts',(54.6435197182,40.85,26.3748975038528)) ;
#12703=CARTESIAN_POINT('Ctrl Pts',(54.7800817079842,41.5,26.2293313384056)) ;
#12704=CARTESIAN_POINT('Ctrl Pts',(54.7800817079842,40.85,26.2293313384056)) ;
#12705=CARTESIAN_POINT('',(54.7800817079842,40.85,26.2293313384056)) ;
#12706=CARTESIAN_POINT('Ctrl Pts',(54.3223734684289,40.85,26.3748975038528)) ;
#12707=CARTESIAN_POINT('Ctrl Pts',(54.6435197182,40.85,26.3748975038528)) ;
#12708=CARTESIAN_POINT('Ctrl Pts',(54.7800817079842,40.85,26.2293313384056)) ;
#12709=CARTESIAN_POINT('',(54.7800817079842,41.5,26.2293313384056)) ;
#12710=CARTESIAN_POINT('Ctrl Pts',(54.7800817079842,41.5,26.2293313384056)) ;
#12711=CARTESIAN_POINT('Ctrl Pts',(54.7800817079842,40.85,26.2293313384056)) ;
#12712=CARTESIAN_POINT('Ctrl Pts',(54.9166436977684,41.5,26.0837651729584)) ;
#12713=CARTESIAN_POINT('Ctrl Pts',(54.9166436977684,40.85,26.0837651729584)) ;
#12714=CARTESIAN_POINT('Ctrl Pts',(54.9166436977684,41.5,25.6695769667625)) ;
#12715=CARTESIAN_POINT('Ctrl Pts',(54.9166436977684,40.85,25.6695769667625)) ;
#12716=CARTESIAN_POINT('',(54.9166436977684,40.85,25.6695769667625)) ;
#12717=CARTESIAN_POINT('Ctrl Pts',(54.7800817079842,40.85,26.2293313384056)) ;
#12718=CARTESIAN_POINT('Ctrl Pts',(54.9166436977684,40.85,26.0837651729584)) ;
#12719=CARTESIAN_POINT('Ctrl Pts',(54.9166436977684,40.85,25.6695769667625)) ;
#12720=CARTESIAN_POINT('',(54.9166436977684,41.5,25.6695769667625)) ;
#12721=CARTESIAN_POINT('Ctrl Pts',(53.8421555347741,41.5,26.5309683918953)) ;
#12722=CARTESIAN_POINT('Ctrl Pts',(53.8421555347741,40.85,26.5309683918953)) ;
#12723=CARTESIAN_POINT('Ctrl Pts',(53.6455657072365,41.5,26.4244200229645)) ;
#12724=CARTESIAN_POINT('Ctrl Pts',(53.6455657072365,40.85,26.4244200229645)) ;
#12725=CARTESIAN_POINT('Ctrl Pts',(53.5615279264748,41.5,26.2225784301758)) ;
#12726=CARTESIAN_POINT('Ctrl Pts',(53.5615279264748,40.85,26.2225784301758)) ;
#12727=CARTESIAN_POINT('',(53.8421555347741,40.85,26.5309683918953)) ;
#12728=CARTESIAN_POINT('',(53.8421555347741,41.5,26.5309683918953)) ;
#12729=CARTESIAN_POINT('Ctrl Pts',(53.8421555347741,40.85,26.5309683918953)) ;
#12730=CARTESIAN_POINT('Ctrl Pts',(53.6455657072365,40.85,26.4244200229645)) ;
#12731=CARTESIAN_POINT('Ctrl Pts',(53.5615279264748,40.85,26.2225784301758)) ;
#12732=CARTESIAN_POINT('Ctrl Pts',(54.3478848524392,41.5,26.6375167608261)) ;
#12733=CARTESIAN_POINT('Ctrl Pts',(54.3478848524392,40.85,26.6375167608261)) ;
#12734=CARTESIAN_POINT('Ctrl Pts',(54.0387447662652,41.5,26.6375167608261)) ;
#12735=CARTESIAN_POINT('Ctrl Pts',(54.0387447662652,40.85,26.6375167608261)) ;
#12736=CARTESIAN_POINT('Ctrl Pts',(53.8421555347741,41.5,26.5309683918953)) ;
#12737=CARTESIAN_POINT('Ctrl Pts',(53.8421555347741,40.85,26.5309683918953)) ;
#12738=CARTESIAN_POINT('',(54.3478848524392,40.85,26.6375167608261)) ;
#12739=CARTESIAN_POINT('',(54.3478848524392,41.5,26.6375167608261)) ;
#12740=CARTESIAN_POINT('Ctrl Pts',(54.3478848524392,40.85,26.6375167608261)) ;
#12741=CARTESIAN_POINT('Ctrl Pts',(54.0387447662652,40.85,26.6375167608261)) ;
#12742=CARTESIAN_POINT('Ctrl Pts',(53.8421555347741,40.85,26.5309683918953)) ;
#12743=CARTESIAN_POINT('Ctrl Pts',(54.8618688173592,41.5,26.5152113080025)) ;
#12744=CARTESIAN_POINT('Ctrl Pts',(54.8618688173592,40.85,26.5152113080025)) ;
#12745=CARTESIAN_POINT('Ctrl Pts',(54.6660300083458,41.5,26.6375167608261)) ;
#12746=CARTESIAN_POINT('Ctrl Pts',(54.6660300083458,40.85,26.6375167608261)) ;
#12747=CARTESIAN_POINT('Ctrl Pts',(54.3478848524392,41.5,26.6375167608261)) ;
#12748=CARTESIAN_POINT('Ctrl Pts',(54.3478848524392,40.85,26.6375167608261)) ;
#12749=CARTESIAN_POINT('',(54.8618688173592,40.85,26.5152113080025)) ;
#12750=CARTESIAN_POINT('',(54.8618688173592,41.5,26.5152113080025)) ;
#12751=CARTESIAN_POINT('Ctrl Pts',(54.8618688173592,40.85,26.5152113080025)) ;
#12752=CARTESIAN_POINT('Ctrl Pts',(54.6660300083458,40.85,26.6375167608261)) ;
#12753=CARTESIAN_POINT('Ctrl Pts',(54.3478848524392,40.85,26.6375167608261)) ;
#12754=CARTESIAN_POINT('Ctrl Pts',(55.132742125541,41.5,26.1978168725967)) ;
#12755=CARTESIAN_POINT('Ctrl Pts',(55.132742125541,40.85,26.1978168725967)) ;
#12756=CARTESIAN_POINT('Ctrl Pts',(55.0577076263726,41.5,26.3929055571556)) ;
#12757=CARTESIAN_POINT('Ctrl Pts',(55.0577076263726,40.85,26.3929055571556)) ;
#12758=CARTESIAN_POINT('Ctrl Pts',(54.8618688173592,41.5,26.5152113080025)) ;
#12759=CARTESIAN_POINT('Ctrl Pts',(54.8618688173592,40.85,26.5152113080025)) ;
#12760=CARTESIAN_POINT('',(55.132742125541,40.85,26.1978168725967)) ;
#12761=CARTESIAN_POINT('',(55.132742125541,41.5,26.1978168725967)) ;
#12762=CARTESIAN_POINT('Ctrl Pts',(55.132742125541,40.85,26.1978168725967)) ;
#12763=CARTESIAN_POINT('Ctrl Pts',(55.0577076263726,40.85,26.3929055571556)) ;
#12764=CARTESIAN_POINT('Ctrl Pts',(54.8618688173592,40.85,26.5152113080025)) ;
#12765=CARTESIAN_POINT('Ctrl Pts',(55.2077760286629,41.5,25.6710775136948)) ;
#12766=CARTESIAN_POINT('Ctrl Pts',(55.2077760286629,40.85,25.6710775136948)) ;
#12767=CARTESIAN_POINT('Ctrl Pts',(55.2077760286629,41.5,26.0027281880379)) ;
#12768=CARTESIAN_POINT('Ctrl Pts',(55.2077760286629,40.85,26.0027281880379)) ;
#12769=CARTESIAN_POINT('Ctrl Pts',(55.132742125541,41.5,26.1978168725967)) ;
#12770=CARTESIAN_POINT('Ctrl Pts',(55.132742125541,40.85,26.1978168725967)) ;
#12771=CARTESIAN_POINT('',(55.2077760286629,40.85,25.6710775136948)) ;
#12772=CARTESIAN_POINT('',(55.2077760286629,41.5,25.6710775136948)) ;
#12773=CARTESIAN_POINT('Ctrl Pts',(55.2077760286629,40.85,25.6710775136948)) ;
#12774=CARTESIAN_POINT('Ctrl Pts',(55.2077760286629,40.85,26.0027281880379)) ;
#12775=CARTESIAN_POINT('Ctrl Pts',(55.132742125541,40.85,26.1978168725967)) ;
#12776=CARTESIAN_POINT('Origin',(55.2077760286629,41.5,24.3999998211861)) ;
#12777=CARTESIAN_POINT('',(55.2077760286629,40.85,24.3999998211861)) ;
#12778=CARTESIAN_POINT('',(55.2077760286629,41.5,24.3999998211861)) ;
#12779=CARTESIAN_POINT('',(55.2077760286629,40.85,24.3999998211861)) ;
#12780=CARTESIAN_POINT('Origin',(54.9166436977684,41.5,24.3999998211861)) ;
#12781=CARTESIAN_POINT('',(54.9166436977684,40.85,24.3999998211861)) ;
#12782=CARTESIAN_POINT('',(54.9166436977684,41.5,24.3999998211861)) ;
#12783=CARTESIAN_POINT('',(54.9166436977684,40.85,24.3999998211861)) ;
#12784=CARTESIAN_POINT('Origin',(54.9166436977684,41.5,25.6695769667625)) ;
#12785=CARTESIAN_POINT('',(54.9166436977684,40.85,25.6695769667625)) ;
#12786=CARTESIAN_POINT('Origin',(53.2966575417668,40.85,25.4999998152256)) ;
#12787=CARTESIAN_POINT('Ctrl Pts',(52.1824010200799,41.5,24.3624828696251)) ;
#12788=CARTESIAN_POINT('Ctrl Pts',(52.1824010200799,40.85,24.3624828696251)) ;
#12789=CARTESIAN_POINT('Ctrl Pts',(52.4270125217736,41.5,24.3624828696251)) ;
#12790=CARTESIAN_POINT('Ctrl Pts',(52.4270125217736,40.85,24.3624828696251)) ;
#12791=CARTESIAN_POINT('Ctrl Pts',(52.6138474531472,41.5,24.4412685871124)) ;
#12792=CARTESIAN_POINT('Ctrl Pts',(52.6138474531472,40.85,24.4412685871124)) ;
#12793=CARTESIAN_POINT('',(52.1824010200799,40.85,24.3624828696251)) ;
#12794=CARTESIAN_POINT('',(52.1824010200799,41.5,24.3624828696251)) ;
#12795=CARTESIAN_POINT('',(52.6138474531472,40.85,24.4412685871124)) ;
#12796=CARTESIAN_POINT('Ctrl Pts',(52.1824010200799,40.85,24.3624828696251)) ;
#12797=CARTESIAN_POINT('Ctrl Pts',(52.4270125217736,40.85,24.3624828696251)) ;
#12798=CARTESIAN_POINT('Ctrl Pts',(52.6138474531472,40.85,24.4412685871124)) ;
#12799=CARTESIAN_POINT('',(52.6138474531472,41.5,24.4412685871124)) ;
#12800=CARTESIAN_POINT('Ctrl Pts',(52.6138474531472,41.5,24.4412685871124)) ;
#12801=CARTESIAN_POINT('Ctrl Pts',(52.6138474531472,40.85,24.4412685871124)) ;
#12802=CARTESIAN_POINT('Ctrl Pts',(52.8006823845208,41.5,24.5200544536114)) ;
#12803=CARTESIAN_POINT('Ctrl Pts',(52.8006823845208,40.85,24.5200544536114)) ;
#12804=CARTESIAN_POINT('Ctrl Pts',(52.901227671653,41.5,24.6731239497662)) ;
#12805=CARTESIAN_POINT('Ctrl Pts',(52.901227671653,40.85,24.6731239497662)) ;
#12806=CARTESIAN_POINT('',(52.901227671653,40.85,24.6731239497662)) ;
#12807=CARTESIAN_POINT('Ctrl Pts',(52.6138474531472,40.85,24.4412685871124)) ;
#12808=CARTESIAN_POINT('Ctrl Pts',(52.8006823845208,40.85,24.5200544536114)) ;
#12809=CARTESIAN_POINT('Ctrl Pts',(52.901227671653,40.85,24.6731239497662)) ;
#12810=CARTESIAN_POINT('',(52.901227671653,41.5,24.6731239497662)) ;
#12811=CARTESIAN_POINT('Ctrl Pts',(52.901227671653,41.5,24.6731239497662)) ;
#12812=CARTESIAN_POINT('Ctrl Pts',(52.901227671653,40.85,24.6731239497662)) ;
#12813=CARTESIAN_POINT('Ctrl Pts',(53.0017735548317,41.5,24.8261935949326)) ;
#12814=CARTESIAN_POINT('Ctrl Pts',(53.0017735548317,40.85,24.8261935949326)) ;
#12815=CARTESIAN_POINT('Ctrl Pts',(53.0092771835625,41.5,25.0197815835476)) ;
#12816=CARTESIAN_POINT('Ctrl Pts',(53.0092771835625,40.85,25.0197815835476)) ;
#12817=CARTESIAN_POINT('',(53.0092771835625,40.85,25.0197815835476)) ;
#12818=CARTESIAN_POINT('Ctrl Pts',(52.901227671653,40.85,24.6731239497662)) ;
#12819=CARTESIAN_POINT('Ctrl Pts',(53.0017735548317,40.85,24.8261935949326)) ;
#12820=CARTESIAN_POINT('Ctrl Pts',(53.0092771835625,40.85,25.0197815835476)) ;
#12821=CARTESIAN_POINT('',(53.0092771835625,41.5,25.0197815835476)) ;
#12822=CARTESIAN_POINT('Origin',(53.0092771835625,41.5,25.0197815835476)) ;
#12823=CARTESIAN_POINT('',(52.7301501221955,40.85,25.0407911777496)) ;
#12824=CARTESIAN_POINT('',(53.0092771835625,40.85,25.0197815835476)) ;
#12825=CARTESIAN_POINT('',(52.7301501221955,41.5,25.0407911777496)) ;
#12826=CARTESIAN_POINT('Ctrl Pts',(52.7301501221955,41.5,25.0407911777496)) ;
#12827=CARTESIAN_POINT('Ctrl Pts',(52.7301501221955,40.85,25.0407911777496)) ;
#12828=CARTESIAN_POINT('Ctrl Pts',(52.7076398320496,41.5,24.8321963787079)) ;
#12829=CARTESIAN_POINT('Ctrl Pts',(52.7076398320496,40.85,24.8321963787079)) ;
#12830=CARTESIAN_POINT('Ctrl Pts',(52.5778307504952,41.5,24.7256478607655)) ;
#12831=CARTESIAN_POINT('Ctrl Pts',(52.5778307504952,40.85,24.7256478607655)) ;
#12832=CARTESIAN_POINT('',(52.5778307504952,40.85,24.7256478607655)) ;
#12833=CARTESIAN_POINT('Ctrl Pts',(52.7301501221955,40.85,25.0407911777496)) ;
#12834=CARTESIAN_POINT('Ctrl Pts',(52.7076398320496,40.85,24.8321963787079)) ;
#12835=CARTESIAN_POINT('Ctrl Pts',(52.5778307504952,40.85,24.7256478607655)) ;
#12836=CARTESIAN_POINT('',(52.5778307504952,41.5,24.7256478607655)) ;
#12837=CARTESIAN_POINT('Ctrl Pts',(52.5778307504952,41.5,24.7256478607655)) ;
#12838=CARTESIAN_POINT('Ctrl Pts',(52.5778307504952,40.85,24.7256478607655)) ;
#12839=CARTESIAN_POINT('Ctrl Pts',(52.448021966964,41.5,24.6190994918346)) ;
#12840=CARTESIAN_POINT('Ctrl Pts',(52.448021966964,40.85,24.6190994918346)) ;
#12841=CARTESIAN_POINT('Ctrl Pts',(52.1944065876305,41.5,24.6190994918346)) ;
#12842=CARTESIAN_POINT('Ctrl Pts',(52.1944065876305,40.85,24.6190994918346)) ;
#12843=CARTESIAN_POINT('',(52.1944065876305,40.85,24.6190994918346)) ;
#12844=CARTESIAN_POINT('Ctrl Pts',(52.5778307504952,40.85,24.7256478607655)) ;
#12845=CARTESIAN_POINT('Ctrl Pts',(52.448021966964,40.85,24.6190994918346)) ;
#12846=CARTESIAN_POINT('Ctrl Pts',(52.1944065876305,40.85,24.6190994918346)) ;
#12847=CARTESIAN_POINT('',(52.1944065876305,41.5,24.6190994918346)) ;
#12848=CARTESIAN_POINT('Ctrl Pts',(52.1944065876305,41.5,24.6190994918346)) ;
#12849=CARTESIAN_POINT('Ctrl Pts',(52.1944065876305,40.85,24.6190994918346)) ;
#12850=CARTESIAN_POINT('Ctrl Pts',(51.9302864857018,41.5,24.6190994918346)) ;
#12851=CARTESIAN_POINT('Ctrl Pts',(51.9302864857018,40.85,24.6190994918346)) ;
#12852=CARTESIAN_POINT('Ctrl Pts',(51.8094815798104,41.5,24.7158934116364)) ;
#12853=CARTESIAN_POINT('Ctrl Pts',(51.8094815798104,40.85,24.7158934116364)) ;
#12854=CARTESIAN_POINT('',(51.8094815798104,40.85,24.7158934116364)) ;
#12855=CARTESIAN_POINT('Ctrl Pts',(52.1944065876305,40.85,24.6190994918346)) ;
#12856=CARTESIAN_POINT('Ctrl Pts',(51.9302864857018,40.85,24.6190994918346)) ;
#12857=CARTESIAN_POINT('Ctrl Pts',(51.8094815798104,40.85,24.7158934116364)) ;
#12858=CARTESIAN_POINT('',(51.8094815798104,41.5,24.7158934116364)) ;
#12859=CARTESIAN_POINT('Ctrl Pts',(51.8094815798104,41.5,24.7158934116364)) ;
#12860=CARTESIAN_POINT('Ctrl Pts',(51.8094815798104,40.85,24.7158934116364)) ;
#12861=CARTESIAN_POINT('Ctrl Pts',(51.688676673919,41.5,24.8126874804497)) ;
#12862=CARTESIAN_POINT('Ctrl Pts',(51.688676673919,40.85,24.8126874804497)) ;
#12863=CARTESIAN_POINT('Ctrl Pts',(51.688676673919,41.5,24.9492494702339)) ;
#12864=CARTESIAN_POINT('Ctrl Pts',(51.688676673919,40.85,24.9492494702339)) ;
#12865=CARTESIAN_POINT('',(51.688676673919,40.85,24.9492494702339)) ;
#12866=CARTESIAN_POINT('Ctrl Pts',(51.8094815798104,40.85,24.7158934116364)) ;
#12867=CARTESIAN_POINT('Ctrl Pts',(51.688676673919,40.85,24.8126874804497)) ;
#12868=CARTESIAN_POINT('Ctrl Pts',(51.688676673919,40.85,24.9492494702339)) ;
#12869=CARTESIAN_POINT('',(51.688676673919,41.5,24.9492494702339)) ;
#12870=CARTESIAN_POINT('Ctrl Pts',(51.688676673919,41.5,24.9492494702339)) ;
#12871=CARTESIAN_POINT('Ctrl Pts',(51.688676673919,40.85,24.9492494702339)) ;
#12872=CARTESIAN_POINT('Ctrl Pts',(51.688676673919,41.5,25.0678034067154)) ;
#12873=CARTESIAN_POINT('Ctrl Pts',(51.688676673919,40.85,25.0678034067154)) ;
#12874=CARTESIAN_POINT('Ctrl Pts',(51.7742155976593,41.5,25.1443381547928)) ;
#12875=CARTESIAN_POINT('Ctrl Pts',(51.7742155976593,40.85,25.1443381547928)) ;
#12876=CARTESIAN_POINT('',(51.7742155976593,40.85,25.1443381547928)) ;
#12877=CARTESIAN_POINT('Ctrl Pts',(51.688676673919,40.85,24.9492494702339)) ;
#12878=CARTESIAN_POINT('Ctrl Pts',(51.688676673919,40.85,25.0678034067154)) ;
#12879=CARTESIAN_POINT('Ctrl Pts',(51.7742155976593,40.85,25.1443381547928)) ;
#12880=CARTESIAN_POINT('',(51.7742155976593,41.5,25.1443381547928)) ;
#12881=CARTESIAN_POINT('Ctrl Pts',(51.7742155976593,41.5,25.1443381547928)) ;
#12882=CARTESIAN_POINT('Ctrl Pts',(51.7742155976593,40.85,25.1443381547928)) ;
#12883=CARTESIAN_POINT('Ctrl Pts',(51.8582536764443,41.5,25.2208730518818)) ;
#12884=CARTESIAN_POINT('Ctrl Pts',(51.8582536764443,40.85,25.2208730518818)) ;
#12885=CARTESIAN_POINT('Ctrl Pts',(52.213165063411,41.5,25.301159465313)) ;
#12886=CARTESIAN_POINT('Ctrl Pts',(52.213165063411,40.85,25.301159465313)) ;
#12887=CARTESIAN_POINT('',(52.213165063411,40.85,25.301159465313)) ;
#12888=CARTESIAN_POINT('Ctrl Pts',(51.7742155976593,40.85,25.1443381547928)) ;
#12889=CARTESIAN_POINT('Ctrl Pts',(51.8582536764443,40.85,25.2208730518818)) ;
#12890=CARTESIAN_POINT('Ctrl Pts',(52.213165063411,40.85,25.301159465313)) ;
#12891=CARTESIAN_POINT('',(52.213165063411,41.5,25.301159465313)) ;
#12892=CARTESIAN_POINT('Ctrl Pts',(52.213165063411,41.5,25.301159465313)) ;
#12893=CARTESIAN_POINT('Ctrl Pts',(52.213165063411,40.85,25.301159465313)) ;
#12894=CARTESIAN_POINT('Ctrl Pts',(52.5680764503777,41.5,25.3814460277557)) ;
#12895=CARTESIAN_POINT('Ctrl Pts',(52.5680764503777,40.85,25.3814460277557)) ;
#12896=CARTESIAN_POINT('Ctrl Pts',(52.7001365013421,41.5,25.4414732694626)) ;
#12897=CARTESIAN_POINT('Ctrl Pts',(52.7001365013421,40.85,25.4414732694626)) ;
#12898=CARTESIAN_POINT('',(52.7001365013421,40.85,25.4414732694626)) ;
#12899=CARTESIAN_POINT('Ctrl Pts',(52.213165063411,40.85,25.301159465313)) ;
#12900=CARTESIAN_POINT('Ctrl Pts',(52.5680764503777,40.85,25.3814460277557)) ;
#12901=CARTESIAN_POINT('Ctrl Pts',(52.7001365013421,40.85,25.4414732694626)) ;
#12902=CARTESIAN_POINT('',(52.7001365013421,41.5,25.4414732694626)) ;
#12903=CARTESIAN_POINT('Ctrl Pts',(52.7001365013421,41.5,25.4414732694626)) ;
#12904=CARTESIAN_POINT('Ctrl Pts',(52.7001365013421,40.85,25.4414732694626)) ;
#12905=CARTESIAN_POINT('Ctrl Pts',(52.8922237940133,41.5,25.530013436079)) ;
#12906=CARTESIAN_POINT('Ctrl Pts',(52.8922237940133,40.85,25.530013436079)) ;
#12907=CARTESIAN_POINT('Ctrl Pts',(52.9837652035058,41.5,25.6658251523972)) ;
#12908=CARTESIAN_POINT('Ctrl Pts',(52.9837652035058,40.85,25.6658251523972)) ;
#12909=CARTESIAN_POINT('',(52.9837652035058,40.85,25.6658251523972)) ;
#12910=CARTESIAN_POINT('Ctrl Pts',(52.7001365013421,40.85,25.4414732694626)) ;
#12911=CARTESIAN_POINT('Ctrl Pts',(52.8922237940133,40.85,25.530013436079)) ;
#12912=CARTESIAN_POINT('Ctrl Pts',(52.9837652035058,40.85,25.6658251523972)) ;
#12913=CARTESIAN_POINT('',(52.9837652035058,41.5,25.6658251523972)) ;
#12914=CARTESIAN_POINT('Ctrl Pts',(52.9837652035058,41.5,25.6658251523972)) ;
#12915=CARTESIAN_POINT('Ctrl Pts',(52.9837652035058,40.85,25.6658251523972)) ;
#12916=CARTESIAN_POINT('Ctrl Pts',(53.0753072090447,41.5,25.8016368687153)) ;
#12917=CARTESIAN_POINT('Ctrl Pts',(53.0753072090447,40.85,25.8016368687153)) ;
#12918=CARTESIAN_POINT('Ctrl Pts',(53.0753072090447,41.5,25.9787173509598)) ;
#12919=CARTESIAN_POINT('Ctrl Pts',(53.0753072090447,40.85,25.9787173509598)) ;
#12920=CARTESIAN_POINT('',(53.0753072090447,40.85,25.9787173509598)) ;
#12921=CARTESIAN_POINT('Ctrl Pts',(52.9837652035058,40.85,25.6658251523972)) ;
#12922=CARTESIAN_POINT('Ctrl Pts',(53.0753072090447,40.85,25.8016368687153)) ;
#12923=CARTESIAN_POINT('Ctrl Pts',(53.0753072090447,40.85,25.9787173509598)) ;
#12924=CARTESIAN_POINT('',(53.0753072090447,41.5,25.9787173509598)) ;
#12925=CARTESIAN_POINT('Ctrl Pts',(53.0753072090447,41.5,25.9787173509598)) ;
#12926=CARTESIAN_POINT('Ctrl Pts',(53.0753072090447,40.85,25.9787173509598)) ;
#12927=CARTESIAN_POINT('Ctrl Pts',(53.0753072090447,41.5,26.1542971372604)) ;
#12928=CARTESIAN_POINT('Ctrl Pts',(53.0753072090447,40.85,26.1542971372604)) ;
#12929=CARTESIAN_POINT('Ctrl Pts',(52.974761325866,41.5,26.3096179008484)) ;
#12930=CARTESIAN_POINT('Ctrl Pts',(52.974761325866,40.85,26.3096179008484)) ;
#12931=CARTESIAN_POINT('',(52.974761325866,40.85,26.3096179008484)) ;
#12932=CARTESIAN_POINT('Ctrl Pts',(53.0753072090447,40.85,25.9787173509598)) ;
#12933=CARTESIAN_POINT('Ctrl Pts',(53.0753072090447,40.85,26.1542971372604)) ;
#12934=CARTESIAN_POINT('Ctrl Pts',(52.974761325866,40.85,26.3096179008484)) ;
#12935=CARTESIAN_POINT('',(52.974761325866,41.5,26.3096179008484)) ;
#12936=CARTESIAN_POINT('Ctrl Pts',(52.974761325866,41.5,26.3096179008484)) ;
#12937=CARTESIAN_POINT('Ctrl Pts',(52.974761325866,40.85,26.3096179008484)) ;
#12938=CARTESIAN_POINT('Ctrl Pts',(52.8742154426873,41.5,26.4649383664131)) ;
#12939=CARTESIAN_POINT('Ctrl Pts',(52.8742154426873,40.85,26.4649383664131)) ;
#12940=CARTESIAN_POINT('Ctrl Pts',(52.6858799643815,41.5,26.5512277126312)) ;
#12941=CARTESIAN_POINT('Ctrl Pts',(52.6858799643815,40.85,26.5512277126312)) ;
#12942=CARTESIAN_POINT('',(52.6858799643815,40.85,26.5512277126312)) ;
#12943=CARTESIAN_POINT('Ctrl Pts',(52.974761325866,40.85,26.3096179008484)) ;
#12944=CARTESIAN_POINT('Ctrl Pts',(52.8742154426873,40.85,26.4649383664131)) ;
#12945=CARTESIAN_POINT('Ctrl Pts',(52.6858799643815,40.85,26.5512277126312)) ;
#12946=CARTESIAN_POINT('',(52.6858799643815,41.5,26.5512277126312)) ;
#12947=CARTESIAN_POINT('Ctrl Pts',(52.6858799643815,41.5,26.5512277126312)) ;
#12948=CARTESIAN_POINT('Ctrl Pts',(52.6858799643815,40.85,26.5512277126312)) ;
#12949=CARTESIAN_POINT('Ctrl Pts',(52.4975444860756,41.5,26.6375167608261)) ;
#12950=CARTESIAN_POINT('Ctrl Pts',(52.4975444860756,40.85,26.6375167608261)) ;
#12951=CARTESIAN_POINT('Ctrl Pts',(52.2619374580681,41.5,26.6375167608261)) ;
#12952=CARTESIAN_POINT('Ctrl Pts',(52.2619374580681,40.85,26.6375167608261)) ;
#12953=CARTESIAN_POINT('',(52.2619374580681,40.85,26.6375167608261)) ;
#12954=CARTESIAN_POINT('Ctrl Pts',(52.6858799643815,40.85,26.5512277126312)) ;
#12955=CARTESIAN_POINT('Ctrl Pts',(52.4975444860756,40.85,26.6375167608261)) ;
#12956=CARTESIAN_POINT('Ctrl Pts',(52.2619374580681,40.85,26.6375167608261)) ;
#12957=CARTESIAN_POINT('',(52.2619374580681,41.5,26.6375167608261)) ;
#12958=CARTESIAN_POINT('Ctrl Pts',(52.2619374580681,41.5,26.6375167608261)) ;
#12959=CARTESIAN_POINT('Ctrl Pts',(52.2619374580681,40.85,26.6375167608261)) ;
#12960=CARTESIAN_POINT('Ctrl Pts',(51.9633014984429,41.5,26.6375167608261)) ;
#12961=CARTESIAN_POINT('Ctrl Pts',(51.9633014984429,40.85,26.6375167608261)) ;
#12962=CARTESIAN_POINT('Ctrl Pts',(51.7614599056542,41.5,26.5504772901535)) ;
#12963=CARTESIAN_POINT('Ctrl Pts',(51.7614599056542,40.85,26.5504772901535)) ;
#12964=CARTESIAN_POINT('',(51.7614599056542,40.85,26.5504772901535)) ;
#12965=CARTESIAN_POINT('Ctrl Pts',(52.2619374580681,40.85,26.6375167608261)) ;
#12966=CARTESIAN_POINT('Ctrl Pts',(51.9633014984429,40.85,26.6375167608261)) ;
#12967=CARTESIAN_POINT('Ctrl Pts',(51.7614599056542,40.85,26.5504772901535)) ;
#12968=CARTESIAN_POINT('',(51.7614599056542,41.5,26.5504772901535)) ;
#12969=CARTESIAN_POINT('Ctrl Pts',(51.7614599056542,41.5,26.5504772901535)) ;
#12970=CARTESIAN_POINT('Ctrl Pts',(51.7614599056542,40.85,26.5504772901535)) ;
#12971=CARTESIAN_POINT('Ctrl Pts',(51.5596180148423,41.5,26.4634378194809)) ;
#12972=CARTESIAN_POINT('Ctrl Pts',(51.5596180148423,40.85,26.4634378194809)) ;
#12973=CARTESIAN_POINT('Ctrl Pts',(51.4448158927262,41.5,26.2886081576347)) ;
#12974=CARTESIAN_POINT('Ctrl Pts',(51.4448158927262,40.85,26.2886081576347)) ;
#12975=CARTESIAN_POINT('',(51.4448158927262,40.85,26.2886081576347)) ;
#12976=CARTESIAN_POINT('Ctrl Pts',(51.7614599056542,40.85,26.5504772901535)) ;
#12977=CARTESIAN_POINT('Ctrl Pts',(51.5596180148423,40.85,26.4634378194809)) ;
#12978=CARTESIAN_POINT('Ctrl Pts',(51.4448158927262,40.85,26.2886081576347)) ;
#12979=CARTESIAN_POINT('',(51.4448158927262,41.5,26.2886081576347)) ;
#12980=CARTESIAN_POINT('Ctrl Pts',(51.7787178345025,41.5,24.4375169217587)) ;
#12981=CARTESIAN_POINT('Ctrl Pts',(51.7787178345025,40.85,24.4375169217587)) ;
#12982=CARTESIAN_POINT('Ctrl Pts',(51.9603001065552,41.5,24.3624828696251)) ;
#12983=CARTESIAN_POINT('Ctrl Pts',(51.9603001065552,40.85,24.3624828696251)) ;
#12984=CARTESIAN_POINT('Ctrl Pts',(52.1824010200799,41.5,24.3624828696251)) ;
#12985=CARTESIAN_POINT('Ctrl Pts',(52.1824010200799,40.85,24.3624828696251)) ;
#12986=CARTESIAN_POINT('',(51.7787178345025,40.85,24.4375169217587)) ;
#12987=CARTESIAN_POINT('',(51.7787178345025,41.5,24.4375169217587)) ;
#12988=CARTESIAN_POINT('Ctrl Pts',(51.7787178345025,40.85,24.4375169217587)) ;
#12989=CARTESIAN_POINT('Ctrl Pts',(51.9603001065552,40.85,24.3624828696251)) ;
#12990=CARTESIAN_POINT('Ctrl Pts',(52.1824010200799,40.85,24.3624828696251)) ;
#12991=CARTESIAN_POINT('Ctrl Pts',(51.5025921650231,41.5,24.6573668658733)) ;
#12992=CARTESIAN_POINT('Ctrl Pts',(51.5025921650231,40.85,24.6573668658733)) ;
#12993=CARTESIAN_POINT('Ctrl Pts',(51.5971352644265,41.5,24.5125509738922)) ;
#12994=CARTESIAN_POINT('Ctrl Pts',(51.5971352644265,40.85,24.5125509738922)) ;
#12995=CARTESIAN_POINT('Ctrl Pts',(51.7787178345025,41.5,24.4375169217587)) ;
#12996=CARTESIAN_POINT('Ctrl Pts',(51.7787178345025,40.85,24.4375169217587)) ;
#12997=CARTESIAN_POINT('',(51.5025921650231,40.85,24.6573668658733)) ;
#12998=CARTESIAN_POINT('',(51.5025921650231,41.5,24.6573668658733)) ;
#12999=CARTESIAN_POINT('Ctrl Pts',(51.5025921650231,40.85,24.6573668658733)) ;
#13000=CARTESIAN_POINT('Ctrl Pts',(51.5971352644265,40.85,24.5125509738922)) ;
#13001=CARTESIAN_POINT('Ctrl Pts',(51.7787178345025,40.85,24.4375169217587)) ;
#13002=CARTESIAN_POINT('Ctrl Pts',(51.4080490656197,41.5,24.9687583684921)) ;
#13003=CARTESIAN_POINT('Ctrl Pts',(51.4080490656197,40.85,24.9687583684921)) ;
#13004=CARTESIAN_POINT('Ctrl Pts',(51.4080490656197,41.5,24.8021826088428)) ;
#13005=CARTESIAN_POINT('Ctrl Pts',(51.4080490656197,40.85,24.8021826088428)) ;
#13006=CARTESIAN_POINT('Ctrl Pts',(51.5025921650231,41.5,24.6573668658733)) ;
#13007=CARTESIAN_POINT('Ctrl Pts',(51.5025921650231,40.85,24.6573668658733)) ;
#13008=CARTESIAN_POINT('',(51.4080490656197,40.85,24.9687583684921)) ;
#13009=CARTESIAN_POINT('',(51.4080490656197,41.5,24.9687583684921)) ;
#13010=CARTESIAN_POINT('Ctrl Pts',(51.4080490656197,40.85,24.9687583684921)) ;
#13011=CARTESIAN_POINT('Ctrl Pts',(51.4080490656197,40.85,24.8021826088428)) ;
#13012=CARTESIAN_POINT('Ctrl Pts',(51.5025921650231,40.85,24.6573668658733)) ;
#13013=CARTESIAN_POINT('Ctrl Pts',(51.4853342361748,41.5,25.2426329195499)) ;
#13014=CARTESIAN_POINT('Ctrl Pts',(51.4853342361748,40.85,25.2426329195499)) ;
#13015=CARTESIAN_POINT('Ctrl Pts',(51.4080490656197,41.5,25.1203273177147)) ;
#13016=CARTESIAN_POINT('Ctrl Pts',(51.4080490656197,40.85,25.1203273177147)) ;
#13017=CARTESIAN_POINT('Ctrl Pts',(51.4080490656197,41.5,24.9687583684921)) ;
#13018=CARTESIAN_POINT('Ctrl Pts',(51.4080490656197,40.85,24.9687583684921)) ;
#13019=CARTESIAN_POINT('',(51.4853342361748,40.85,25.2426329195499)) ;
#13020=CARTESIAN_POINT('',(51.4853342361748,41.5,25.2426329195499)) ;
#13021=CARTESIAN_POINT('Ctrl Pts',(51.4853342361748,40.85,25.2426329195499)) ;
#13022=CARTESIAN_POINT('Ctrl Pts',(51.4080490656197,40.85,25.1203273177147)) ;
#13023=CARTESIAN_POINT('Ctrl Pts',(51.4080490656197,40.85,24.9687583684921)) ;
#13024=CARTESIAN_POINT('Ctrl Pts',(51.7201911397278,41.5,25.4474759042263)) ;
#13025=CARTESIAN_POINT('Ctrl Pts',(51.7201911397278,40.85,25.4474759042263)) ;
#13026=CARTESIAN_POINT('Ctrl Pts',(51.5626194067299,41.5,25.3649385213852)) ;
#13027=CARTESIAN_POINT('Ctrl Pts',(51.5626194067299,40.85,25.3649385213852)) ;
#13028=CARTESIAN_POINT('Ctrl Pts',(51.4853342361748,41.5,25.2426329195499)) ;
#13029=CARTESIAN_POINT('Ctrl Pts',(51.4853342361748,40.85,25.2426329195499)) ;
#13030=CARTESIAN_POINT('',(51.7201911397278,40.85,25.4474759042263)) ;
#13031=CARTESIAN_POINT('',(51.7201911397278,41.5,25.4474759042263)) ;
#13032=CARTESIAN_POINT('Ctrl Pts',(51.7201911397278,40.85,25.4474759042263)) ;
#13033=CARTESIAN_POINT('Ctrl Pts',(51.5626194067299,40.85,25.3649385213852)) ;
#13034=CARTESIAN_POINT('Ctrl Pts',(51.4853342361748,40.85,25.2426329195499)) ;
#13035=CARTESIAN_POINT('Ctrl Pts',(52.1448840685189,41.5,25.5847883164883)) ;
#13036=CARTESIAN_POINT('Ctrl Pts',(52.1448840685189,40.85,25.5847883164883)) ;
#13037=CARTESIAN_POINT('Ctrl Pts',(51.8417461700737,41.5,25.5120052337646)) ;
#13038=CARTESIAN_POINT('Ctrl Pts',(51.8417461700737,40.85,25.5120052337646)) ;
#13039=CARTESIAN_POINT('Ctrl Pts',(51.7201911397278,41.5,25.4474759042263)) ;
#13040=CARTESIAN_POINT('Ctrl Pts',(51.7201911397278,40.85,25.4474759042263)) ;
#13041=CARTESIAN_POINT('',(52.1448840685189,40.85,25.5847883164883)) ;
#13042=CARTESIAN_POINT('',(52.1448840685189,41.5,25.5847883164883)) ;
#13043=CARTESIAN_POINT('Ctrl Pts',(52.1448840685189,40.85,25.5847883164883)) ;
#13044=CARTESIAN_POINT('Ctrl Pts',(51.8417461700737,40.85,25.5120052337646)) ;
#13045=CARTESIAN_POINT('Ctrl Pts',(51.7201911397278,40.85,25.4474759042263)) ;
#13046=CARTESIAN_POINT('Ctrl Pts',(52.5365622825921,41.5,25.6920871078968)) ;
#13047=CARTESIAN_POINT('Ctrl Pts',(52.5365622825921,40.85,25.6920871078968)) ;
#13048=CARTESIAN_POINT('Ctrl Pts',(52.448021966964,41.5,25.6575713992119)) ;
#13049=CARTESIAN_POINT('Ctrl Pts',(52.448021966964,40.85,25.6575713992119)) ;
#13050=CARTESIAN_POINT('Ctrl Pts',(52.1448840685189,41.5,25.5847883164883)) ;
#13051=CARTESIAN_POINT('Ctrl Pts',(52.1448840685189,40.85,25.5847883164883)) ;
#13052=CARTESIAN_POINT('',(52.5365622825921,40.85,25.6920871078968)) ;
#13053=CARTESIAN_POINT('',(52.5365622825921,41.5,25.6920871078968)) ;
#13054=CARTESIAN_POINT('Ctrl Pts',(52.5365622825921,40.85,25.6920871078968)) ;
#13055=CARTESIAN_POINT('Ctrl Pts',(52.448021966964,40.85,25.6575713992119)) ;
#13056=CARTESIAN_POINT('Ctrl Pts',(52.1448840685189,40.85,25.5847883164883)) ;
#13057=CARTESIAN_POINT('Ctrl Pts',(52.7346523590386,41.5,25.8218960404396)) ;
#13058=CARTESIAN_POINT('Ctrl Pts',(52.7346523590386,40.85,25.8218960404396)) ;
#13059=CARTESIAN_POINT('Ctrl Pts',(52.6746251173317,41.5,25.7446108698845)) ;
#13060=CARTESIAN_POINT('Ctrl Pts',(52.6746251173317,40.85,25.7446108698845)) ;
#13061=CARTESIAN_POINT('Ctrl Pts',(52.5365622825921,41.5,25.6920871078968)) ;
#13062=CARTESIAN_POINT('Ctrl Pts',(52.5365622825921,40.85,25.6920871078968)) ;
#13063=CARTESIAN_POINT('',(52.7346523590386,40.85,25.8218960404396)) ;
#13064=CARTESIAN_POINT('',(52.7346523590386,41.5,25.8218960404396)) ;
#13065=CARTESIAN_POINT('Ctrl Pts',(52.7346523590386,40.85,25.8218960404396)) ;
#13066=CARTESIAN_POINT('Ctrl Pts',(52.6746251173317,40.85,25.7446108698845)) ;
#13067=CARTESIAN_POINT('Ctrl Pts',(52.5365622825921,40.85,25.6920871078968)) ;
#13068=CARTESIAN_POINT('Ctrl Pts',(52.7946796007454,41.5,26.0027281880379)) ;
#13069=CARTESIAN_POINT('Ctrl Pts',(52.7946796007454,40.85,26.0027281880379)) ;
#13070=CARTESIAN_POINT('Ctrl Pts',(52.7946796007454,41.5,25.8991812109947)) ;
#13071=CARTESIAN_POINT('Ctrl Pts',(52.7946796007454,40.85,25.8991812109947)) ;
#13072=CARTESIAN_POINT('Ctrl Pts',(52.7346523590386,41.5,25.8218960404396)) ;
#13073=CARTESIAN_POINT('Ctrl Pts',(52.7346523590386,40.85,25.8218960404396)) ;
#13074=CARTESIAN_POINT('',(52.7946796007454,40.85,26.0027281880379)) ;
#13075=CARTESIAN_POINT('',(52.7946796007454,41.5,26.0027281880379)) ;
#13076=CARTESIAN_POINT('Ctrl Pts',(52.7946796007454,40.85,26.0027281880379)) ;
#13077=CARTESIAN_POINT('Ctrl Pts',(52.7946796007454,40.85,25.8991812109947)) ;
#13078=CARTESIAN_POINT('Ctrl Pts',(52.7346523590386,40.85,25.8218960404396)) ;
#13079=CARTESIAN_POINT('Ctrl Pts',(52.7324010916054,41.5,26.1910639643669)) ;
#13080=CARTESIAN_POINT('Ctrl Pts',(52.7324010916054,40.85,26.1910639643669)) ;
#13081=CARTESIAN_POINT('Ctrl Pts',(52.7946796007454,41.5,26.1047746181488)) ;
#13082=CARTESIAN_POINT('Ctrl Pts',(52.7946796007454,40.85,26.1047746181488)) ;
#13083=CARTESIAN_POINT('Ctrl Pts',(52.7946796007454,41.5,26.0027281880379)) ;
#13084=CARTESIAN_POINT('Ctrl Pts',(52.7946796007454,40.85,26.0027281880379)) ;
#13085=CARTESIAN_POINT('',(52.7324010916054,40.85,26.1910639643669)) ;
#13086=CARTESIAN_POINT('',(52.7324010916054,41.5,26.1910639643669)) ;
#13087=CARTESIAN_POINT('Ctrl Pts',(52.7324010916054,40.85,26.1910639643669)) ;
#13088=CARTESIAN_POINT('Ctrl Pts',(52.7946796007454,40.85,26.1047746181488)) ;
#13089=CARTESIAN_POINT('Ctrl Pts',(52.7946796007454,40.85,26.0027281880379)) ;
#13090=CARTESIAN_POINT('Ctrl Pts',(52.5425647683442,41.5,26.3268758296967)) ;
#13091=CARTESIAN_POINT('Ctrl Pts',(52.5425647683442,40.85,26.3268758296967)) ;
#13092=CARTESIAN_POINT('Ctrl Pts',(52.6701228804886,41.5,26.277353310585)) ;
#13093=CARTESIAN_POINT('Ctrl Pts',(52.6701228804886,40.85,26.277353310585)) ;
#13094=CARTESIAN_POINT('Ctrl Pts',(52.7324010916054,41.5,26.1910639643669)) ;
#13095=CARTESIAN_POINT('Ctrl Pts',(52.7324010916054,40.85,26.1910639643669)) ;
#13096=CARTESIAN_POINT('',(52.5425647683442,40.85,26.3268758296967)) ;
#13097=CARTESIAN_POINT('',(52.5425647683442,41.5,26.3268758296967)) ;
#13098=CARTESIAN_POINT('Ctrl Pts',(52.5425647683442,40.85,26.3268758296967)) ;
#13099=CARTESIAN_POINT('Ctrl Pts',(52.6701228804886,40.85,26.277353310585)) ;
#13100=CARTESIAN_POINT('Ctrl Pts',(52.7324010916054,40.85,26.1910639643669)) ;
#13101=CARTESIAN_POINT('Ctrl Pts',(52.248431045562,41.5,26.3763980507851)) ;
#13102=CARTESIAN_POINT('Ctrl Pts',(52.248431045562,40.85,26.3763980507851)) ;
#13103=CARTESIAN_POINT('Ctrl Pts',(52.4150069542229,41.5,26.3763980507851)) ;
#13104=CARTESIAN_POINT('Ctrl Pts',(52.4150069542229,40.85,26.3763980507851)) ;
#13105=CARTESIAN_POINT('Ctrl Pts',(52.5425647683442,41.5,26.3268758296967)) ;
#13106=CARTESIAN_POINT('Ctrl Pts',(52.5425647683442,40.85,26.3268758296967)) ;
#13107=CARTESIAN_POINT('',(52.248431045562,40.85,26.3763980507851)) ;
#13108=CARTESIAN_POINT('',(52.248431045562,41.5,26.3763980507851)) ;
#13109=CARTESIAN_POINT('Ctrl Pts',(52.248431045562,40.85,26.3763980507851)) ;
#13110=CARTESIAN_POINT('Ctrl Pts',(52.4150069542229,40.85,26.3763980507851)) ;
#13111=CARTESIAN_POINT('Ctrl Pts',(52.5425647683442,40.85,26.3268758296967)) ;
#13112=CARTESIAN_POINT('Ctrl Pts',(51.9107775874436,41.5,26.3111184477806)) ;
#13113=CARTESIAN_POINT('Ctrl Pts',(51.9107775874436,40.85,26.3111184477806)) ;
#13114=CARTESIAN_POINT('Ctrl Pts',(52.0608459897339,41.5,26.3763980507851)) ;
#13115=CARTESIAN_POINT('Ctrl Pts',(52.0608459897339,40.85,26.3763980507851)) ;
#13116=CARTESIAN_POINT('Ctrl Pts',(52.248431045562,41.5,26.3763980507851)) ;
#13117=CARTESIAN_POINT('Ctrl Pts',(52.248431045562,40.85,26.3763980507851)) ;
#13118=CARTESIAN_POINT('',(51.9107775874436,40.85,26.3111184477806)) ;
#13119=CARTESIAN_POINT('',(51.9107775874436,41.5,26.3111184477806)) ;
#13120=CARTESIAN_POINT('Ctrl Pts',(51.9107775874436,40.85,26.3111184477806)) ;
#13121=CARTESIAN_POINT('Ctrl Pts',(52.0608459897339,40.85,26.3763980507851)) ;
#13122=CARTESIAN_POINT('Ctrl Pts',(52.248431045562,40.85,26.3763980507851)) ;
#13123=CARTESIAN_POINT('Ctrl Pts',(51.6894270963967,41.5,26.1400408983231)) ;
#13124=CARTESIAN_POINT('Ctrl Pts',(51.6894270963967,40.85,26.1400408983231)) ;
#13125=CARTESIAN_POINT('Ctrl Pts',(51.7607094831765,41.5,26.2458388447762)) ;
#13126=CARTESIAN_POINT('Ctrl Pts',(51.7607094831765,40.85,26.2458388447762)) ;
#13127=CARTESIAN_POINT('Ctrl Pts',(51.9107775874436,41.5,26.3111184477806)) ;
#13128=CARTESIAN_POINT('Ctrl Pts',(51.9107775874436,40.85,26.3111184477806)) ;
#13129=CARTESIAN_POINT('',(51.6894270963967,40.85,26.1400408983231)) ;
#13130=CARTESIAN_POINT('',(51.6894270963967,41.5,26.1400408983231)) ;
#13131=CARTESIAN_POINT('Ctrl Pts',(51.6894270963967,40.85,26.1400408983231)) ;
#13132=CARTESIAN_POINT('Ctrl Pts',(51.7607094831765,40.85,26.2458388447762)) ;
#13133=CARTESIAN_POINT('Ctrl Pts',(51.9107775874436,40.85,26.3111184477806)) ;
#13134=CARTESIAN_POINT('Ctrl Pts',(51.5986358113587,41.5,25.8691675901413)) ;
#13135=CARTESIAN_POINT('Ctrl Pts',(51.5986358113587,40.85,25.8691675901413)) ;
#13136=CARTESIAN_POINT('Ctrl Pts',(51.6181447096169,41.5,26.0342426538467)) ;
#13137=CARTESIAN_POINT('Ctrl Pts',(51.6181447096169,40.85,26.0342426538467)) ;
#13138=CARTESIAN_POINT('Ctrl Pts',(51.6894270963967,41.5,26.1400408983231)) ;
#13139=CARTESIAN_POINT('Ctrl Pts',(51.6894270963967,40.85,26.1400408983231)) ;
#13140=CARTESIAN_POINT('',(51.5986358113587,40.85,25.8691675901413)) ;
#13141=CARTESIAN_POINT('',(51.5986358113587,41.5,25.8691675901413)) ;
#13142=CARTESIAN_POINT('Ctrl Pts',(51.5986358113587,40.85,25.8691675901413)) ;
#13143=CARTESIAN_POINT('Ctrl Pts',(51.6181447096169,40.85,26.0342426538467)) ;
#13144=CARTESIAN_POINT('Ctrl Pts',(51.6894270963967,40.85,26.1400408983231)) ;
#13145=CARTESIAN_POINT('Origin',(51.3240109868348,41.5,25.8931784272194)) ;
#13146=CARTESIAN_POINT('',(51.3240109868348,40.85,25.8931784272194)) ;
#13147=CARTESIAN_POINT('',(51.3240109868348,41.5,25.8931784272194)) ;
#13148=CARTESIAN_POINT('',(51.3240109868348,40.85,25.8931784272194)) ;
#13149=CARTESIAN_POINT('Ctrl Pts',(51.4448158927262,41.5,26.2886081576347)) ;
#13150=CARTESIAN_POINT('Ctrl Pts',(51.4448158927262,40.85,26.2886081576347)) ;
#13151=CARTESIAN_POINT('Ctrl Pts',(51.3300137706101,41.5,26.1137787938118)) ;
#13152=CARTESIAN_POINT('Ctrl Pts',(51.3300137706101,40.85,26.1137787938118)) ;
#13153=CARTESIAN_POINT('Ctrl Pts',(51.3240109868348,41.5,25.8931784272194)) ;
#13154=CARTESIAN_POINT('Ctrl Pts',(51.3240109868348,40.85,25.8931784272194)) ;
#13155=CARTESIAN_POINT('Ctrl Pts',(51.4448158927262,40.85,26.2886081576347)) ;
#13156=CARTESIAN_POINT('Ctrl Pts',(51.3300137706101,40.85,26.1137787938118)) ;
#13157=CARTESIAN_POINT('Ctrl Pts',(51.3240109868348,40.85,25.8931784272194)) ;
#13158=CARTESIAN_POINT('Origin',(53.2966575417668,40.85,25.4999998152256)) ;
#13159=CARTESIAN_POINT('Origin',(49.7077762074769,41.5,24.3999998211861)) ;
#13160=CARTESIAN_POINT('',(49.7077762074769,40.85,24.3999998211861)) ;
#13161=CARTESIAN_POINT('',(49.7077762074769,41.5,24.3999998211861)) ;
#13162=CARTESIAN_POINT('',(50.0994542725384,40.85,24.3999998211861)) ;
#13163=CARTESIAN_POINT('',(49.7077762074769,40.85,24.3999998211861)) ;
#13164=CARTESIAN_POINT('',(50.0994542725384,41.5,24.3999998211861)) ;
#13165=CARTESIAN_POINT('Origin',(50.0994542725384,41.5,24.3999998211861)) ;
#13166=CARTESIAN_POINT('',(50.0994542725384,40.85,26.5999998092651)) ;
#13167=CARTESIAN_POINT('',(50.0994542725384,40.85,24.3999998211861)) ;
#13168=CARTESIAN_POINT('',(50.0994542725384,41.5,26.5999998092651)) ;
#13169=CARTESIAN_POINT('Origin',(50.0994542725384,41.5,26.5999998092651)) ;
#13170=CARTESIAN_POINT('',(49.8188268132508,40.85,26.5999998092651)) ;
#13171=CARTESIAN_POINT('',(50.0994542725384,40.85,26.5999998092651)) ;
#13172=CARTESIAN_POINT('',(49.8188268132508,41.5,26.5999998092651)) ;
#13173=CARTESIAN_POINT('Origin',(49.8188268132508,41.5,26.5999998092651)) ;
#13174=CARTESIAN_POINT('',(49.8188268132508,40.85,24.7586628735065)) ;
#13175=CARTESIAN_POINT('',(49.8188268132508,40.85,26.5999998092651)) ;
#13176=CARTESIAN_POINT('',(49.8188268132508,41.5,24.7586628735065)) ;
#13177=CARTESIAN_POINT('Origin',(49.8188268132508,41.5,24.7586628735065)) ;
#13178=CARTESIAN_POINT('',(49.179536152631,40.85,26.5999998092651)) ;
#13179=CARTESIAN_POINT('',(49.8188268132508,40.85,24.7586628735065)) ;
#13180=CARTESIAN_POINT('',(49.179536152631,41.5,26.5999998092651)) ;
#13181=CARTESIAN_POINT('Origin',(49.179536152631,41.5,26.5999998092651)) ;
#13182=CARTESIAN_POINT('',(48.916916821152,40.85,26.5999998092651)) ;
#13183=CARTESIAN_POINT('',(49.179536152631,40.85,26.5999998092651)) ;
#13184=CARTESIAN_POINT('',(48.916916821152,41.5,26.5999998092651)) ;
#13185=CARTESIAN_POINT('Origin',(48.916916821152,41.5,26.5999998092651)) ;
#13186=CARTESIAN_POINT('',(48.2806275524199,40.85,24.7271485567093)) ;
#13187=CARTESIAN_POINT('',(48.916916821152,40.85,26.5999998092651)) ;
#13188=CARTESIAN_POINT('',(48.2806275524199,41.5,24.7271485567093)) ;
#13189=CARTESIAN_POINT('Origin',(48.2806275524199,41.5,24.7271485567093)) ;
#13190=CARTESIAN_POINT('',(48.2806275524199,40.85,26.5999998092651)) ;
#13191=CARTESIAN_POINT('',(48.2806275524199,40.85,24.7271485567093)) ;
#13192=CARTESIAN_POINT('',(48.2806275524199,41.5,26.5999998092651)) ;
#13193=CARTESIAN_POINT('Origin',(49.1810368485749,41.5,25.9306956768036)) ;
#13194=CARTESIAN_POINT('',(49.1810368485749,40.85,25.9306956768036)) ;
#13195=CARTESIAN_POINT('',(49.1810368485749,41.5,25.9306956768036)) ;
#13196=CARTESIAN_POINT('',(49.1810368485749,40.85,25.9306956768036)) ;
#13197=CARTESIAN_POINT('Ctrl Pts',(49.0639836080372,41.5,26.2833557963371)) ;
#13198=CARTESIAN_POINT('Ctrl Pts',(49.0639836080372,40.85,26.2833557963371)) ;
#13199=CARTESIAN_POINT('Ctrl Pts',(49.1015007086098,41.5,26.1633013129234)) ;
#13200=CARTESIAN_POINT('Ctrl Pts',(49.1015007086098,40.85,26.1633013129234)) ;
#13201=CARTESIAN_POINT('Ctrl Pts',(49.1810368485749,41.5,25.9306956768036)) ;
#13202=CARTESIAN_POINT('Ctrl Pts',(49.1810368485749,40.85,25.9306956768036)) ;
#13203=CARTESIAN_POINT('',(49.0639836080372,40.85,26.2833557963371)) ;
#13204=CARTESIAN_POINT('',(49.0639836080372,41.5,26.2833557963371)) ;
#13205=CARTESIAN_POINT('Ctrl Pts',(49.0639836080372,40.85,26.2833557963371)) ;
#13206=CARTESIAN_POINT('Ctrl Pts',(49.1015007086098,40.85,26.1633013129234)) ;
#13207=CARTESIAN_POINT('Ctrl Pts',(49.1810368485749,40.85,25.9306956768036)) ;
#13208=CARTESIAN_POINT('Ctrl Pts',(48.9589358605444,41.5,25.9577079057693)) ;
#13209=CARTESIAN_POINT('Ctrl Pts',(48.9589358605444,40.85,25.9577079057693)) ;
#13210=CARTESIAN_POINT('Ctrl Pts',(49.0309685952961,41.5,26.1753068804741)) ;
#13211=CARTESIAN_POINT('Ctrl Pts',(49.0309685952961,40.85,26.1753068804741)) ;
#13212=CARTESIAN_POINT('Ctrl Pts',(49.0639836080372,41.5,26.2833557963371)) ;
#13213=CARTESIAN_POINT('Ctrl Pts',(49.0639836080372,40.85,26.2833557963371)) ;
#13214=CARTESIAN_POINT('',(48.9589358605444,40.85,25.9577079057693)) ;
#13215=CARTESIAN_POINT('',(48.9589358605444,41.5,25.9577079057693)) ;
#13216=CARTESIAN_POINT('Ctrl Pts',(48.9589358605444,40.85,25.9577079057693)) ;
#13217=CARTESIAN_POINT('Ctrl Pts',(49.0309685952961,40.85,26.1753068804741)) ;
#13218=CARTESIAN_POINT('Ctrl Pts',(49.0639836080372,40.85,26.2833557963371)) ;
#13219=CARTESIAN_POINT('Origin',(48.438199210912,41.5,24.3999998211861)) ;
#13220=CARTESIAN_POINT('',(48.438199210912,40.85,24.3999998211861)) ;
#13221=CARTESIAN_POINT('',(48.438199210912,41.5,24.3999998211861)) ;
#13222=CARTESIAN_POINT('',(48.438199210912,40.85,24.3999998211861)) ;
#13223=CARTESIAN_POINT('Origin',(48.,41.5,24.3999998211861)) ;
#13224=CARTESIAN_POINT('',(48.,40.85,24.3999998211861)) ;
#13225=CARTESIAN_POINT('',(48.,41.5,24.3999998211861)) ;
#13226=CARTESIAN_POINT('',(48.,40.85,24.3999998211861)) ;
#13227=CARTESIAN_POINT('Origin',(48.,41.5,26.5999998092651)) ;
#13228=CARTESIAN_POINT('',(48.,40.85,26.5999998092651)) ;
#13229=CARTESIAN_POINT('',(48.,41.5,26.5999998092651)) ;
#13230=CARTESIAN_POINT('',(48.,40.85,26.5999998092651)) ;
#13231=CARTESIAN_POINT('Origin',(48.2806275524199,41.5,26.5999998092651)) ;
#13232=CARTESIAN_POINT('',(48.2806275524199,40.85,26.5999998092651)) ;
#13233=CARTESIAN_POINT('Origin',(53.2966575417668,40.85,25.4999998152256)) ;
#13234=CARTESIAN_POINT('Origin',(45.,25.5,25.5)) ;
#13235=CARTESIAN_POINT('',(44.25,10.4,25.5)) ;
#13236=CARTESIAN_POINT('Origin',(44.25,25.5,25.5)) ;
#13237=CARTESIAN_POINT('',(45.75,10.4,25.5)) ;
#13238=CARTESIAN_POINT('',(45.,10.4,25.5)) ;
#13239=CARTESIAN_POINT('Origin',(45.75,25.5,25.5)) ;
#13240=CARTESIAN_POINT('Origin',(44.25,41.1,25.5)) ;
#13241=CARTESIAN_POINT('',(44.25,10.,25.5)) ;
#13242=CARTESIAN_POINT('Origin',(44.25,25.5,25.5)) ;
#13243=CARTESIAN_POINT('Origin',(45.75,40.6,25.5)) ;
#13244=CARTESIAN_POINT('Origin',(55.25,25.5,25.5)) ;
#13245=CARTESIAN_POINT('Origin',(33.85,11.357864376269,39.642135623731)) ;
#13246=CARTESIAN_POINT('',(34.,13.4700501879138,35.8966488600263)) ;
#13247=CARTESIAN_POINT('',(33.7,13.3226883871013,36.1579618900522)) ;
#13248=CARTESIAN_POINT('',(34.,13.4700501879138,35.8966488600263)) ;
#13249=CARTESIAN_POINT('',(33.7,11.357864376269,43.642135623731)) ;
#13250=CARTESIAN_POINT('Origin',(33.7,11.357864376269,39.642135623731)) ;
#13251=CARTESIAN_POINT('',(33.7,14.8420381099478,37.6773116128987)) ;
#13252=CARTESIAN_POINT('Origin',(33.7,11.357864376269,39.642135623731)) ;
#13253=CARTESIAN_POINT('',(34.,15.1033511399737,37.5299498120862)) ;
#13254=CARTESIAN_POINT('',(33.7,14.8420381099478,37.6773116128987)) ;
#13255=CARTESIAN_POINT('Origin',(34.,11.357864376269,39.642135623731)) ;
#13256=CARTESIAN_POINT('Ctrl Pts',(34.,15.1033511399737,37.5299498120862)) ;
#13257=CARTESIAN_POINT('Ctrl Pts',(34.,14.9939502140824,37.3359518609572)) ;
#13258=CARTESIAN_POINT('Ctrl Pts',(34.0395441492995,14.7425871058727,36.9664669273901)) ;
#13259=CARTESIAN_POINT('Ctrl Pts',(34.0658646655374,14.2092063101249,36.3963307672773)) ;
#13260=CARTESIAN_POINT('Ctrl Pts',(34.,13.7610471146074,36.0607502488633)) ;
#13261=CARTESIAN_POINT('Ctrl Pts',(34.,13.4700501879138,35.8966488600263)) ;
#13262=CARTESIAN_POINT('Ctrl Pts',(33.9,15.0162467966317,37.579070412357)) ;
#13263=CARTESIAN_POINT('Ctrl Pts',(33.9,14.9093900783193,37.3895840414868)) ;
#13264=CARTESIAN_POINT('Ctrl Pts',(33.9263627661997,14.66459918252,37.0282402745978)) ;
#13265=CARTESIAN_POINT('Ctrl Pts',(33.9439097770249,14.1443737517734,36.4701794174857)) ;
#13266=CARTESIAN_POINT('Ctrl Pts',(33.9,13.7051591439483,36.1440382808369)) ;
#13267=CARTESIAN_POINT('Ctrl Pts',(33.9,13.4209295876429,35.9837532033683)) ;
#13268=CARTESIAN_POINT('Ctrl Pts',(33.8,14.9291424532898,37.6281910126279)) ;
#13269=CARTESIAN_POINT('Ctrl Pts',(33.8,14.8248299425562,37.4432162220164)) ;
#13270=CARTESIAN_POINT('Ctrl Pts',(33.8131813830998,14.5866112591672,37.0900136218054)) ;
#13271=CARTESIAN_POINT('Ctrl Pts',(33.8219548885125,14.0795411934218,36.5440280676941)) ;
#13272=CARTESIAN_POINT('Ctrl Pts',(33.8,13.6492711732893,36.2273263128106)) ;
#13273=CARTESIAN_POINT('Ctrl Pts',(33.8,13.3718089873721,36.0708575467102)) ;
#13274=CARTESIAN_POINT('Ctrl Pts',(33.7,14.8420381099478,37.6773116128987)) ;
#13275=CARTESIAN_POINT('Ctrl Pts',(33.7,14.7402698067931,37.496848402546)) ;
#13276=CARTESIAN_POINT('Ctrl Pts',(33.7,14.5086233358145,37.151786969013)) ;
#13277=CARTESIAN_POINT('Ctrl Pts',(33.7,14.0147086350703,36.6178767179025)) ;
#13278=CARTESIAN_POINT('Ctrl Pts',(33.7,13.5933832026303,36.3106143447843)) ;
#13279=CARTESIAN_POINT('Ctrl Pts',(33.7,13.3226883871013,36.1579618900522)) ;
#13280=CARTESIAN_POINT('Ctrl Pts',(34.,13.4700501879138,35.8966488600263)) ;
#13281=CARTESIAN_POINT('Ctrl Pts',(34.,13.7610471146074,36.0607502488633)) ;
#13282=CARTESIAN_POINT('Ctrl Pts',(34.0658646655374,14.2092063101249,36.3963307672773)) ;
#13283=CARTESIAN_POINT('Ctrl Pts',(34.0395441492995,14.7425871058727,36.9664669273901)) ;
#13284=CARTESIAN_POINT('Ctrl Pts',(34.,14.9939502140824,37.3359518609572)) ;
#13285=CARTESIAN_POINT('Ctrl Pts',(34.,15.1033511399737,37.5299498120862)) ;
#13286=CARTESIAN_POINT('Ctrl Pts',(33.7,14.8420381099478,37.6773116128987)) ;
#13287=CARTESIAN_POINT('Ctrl Pts',(33.7,14.7402698067931,37.496848402546)) ;
#13288=CARTESIAN_POINT('Ctrl Pts',(33.7,14.5086233358145,37.151786969013)) ;
#13289=CARTESIAN_POINT('Ctrl Pts',(33.7,14.0147086350703,36.6178767179025)) ;
#13290=CARTESIAN_POINT('Ctrl Pts',(33.7,13.5933832026303,36.3106143447843)) ;
#13291=CARTESIAN_POINT('Ctrl Pts',(33.7,13.3226883871013,36.1579618900522)) ;
#13292=CARTESIAN_POINT('Origin',(34.4,25.5,25.5)) ;
#13293=CARTESIAN_POINT('',(34.,13.4700501879138,15.1033511399737)) ;
#13294=CARTESIAN_POINT('Origin',(34.,25.5,25.5)) ;
#13295=CARTESIAN_POINT('',(34.,15.1033511399737,13.4700501879138)) ;
#13296=CARTESIAN_POINT('Ctrl Pts',(34.,15.1033511399737,13.4700501879138)) ;
#13297=CARTESIAN_POINT('Ctrl Pts',(34.,14.9939502140824,13.6640481390428)) ;
#13298=CARTESIAN_POINT('Ctrl Pts',(34.0395562744413,14.7425990198672,14.0335422105128)) ;
#13299=CARTESIAN_POINT('Ctrl Pts',(34.0658862423307,14.2092225347123,14.6036824431284)) ;
#13300=CARTESIAN_POINT('Ctrl Pts',(34.,13.7610471146074,14.9392497511367)) ;
#13301=CARTESIAN_POINT('Ctrl Pts',(34.,13.4700501879138,15.1033511399737)) ;
#13302=CARTESIAN_POINT('',(34.,35.8966488600263,13.4700501879138)) ;
#13303=CARTESIAN_POINT('Origin',(34.,25.5,25.5)) ;
#13304=CARTESIAN_POINT('',(34.,37.5299498120862,15.1033511399737)) ;
#13305=CARTESIAN_POINT('Ctrl Pts',(34.,37.5299498120862,15.1033511399737)) ;
#13306=CARTESIAN_POINT('Ctrl Pts',(34.,37.2389528853926,14.9392497511367)) ;
#13307=CARTESIAN_POINT('Ctrl Pts',(34.0658646655374,36.790793689875,14.6036692327227)) ;
#13308=CARTESIAN_POINT('Ctrl Pts',(34.0395441492995,36.2574128941273,14.0335330726099)) ;
#13309=CARTESIAN_POINT('Ctrl Pts',(34.,36.0060497859176,13.6640481390428)) ;
#13310=CARTESIAN_POINT('Ctrl Pts',(34.,35.8966488600263,13.4700501879138)) ;
#13311=CARTESIAN_POINT('',(34.,37.5299498120862,35.8966488600263)) ;
#13312=CARTESIAN_POINT('Origin',(34.,25.5,25.5)) ;
#13313=CARTESIAN_POINT('',(34.,35.8966488600263,37.5299498120862)) ;
#13314=CARTESIAN_POINT('Ctrl Pts',(34.,35.8966488600263,37.5299498120862)) ;
#13315=CARTESIAN_POINT('Ctrl Pts',(34.,36.0060497859176,37.3359518609572)) ;
#13316=CARTESIAN_POINT('Ctrl Pts',(34.0395377031192,36.2574192030825,36.9664717701347)) ;
#13317=CARTESIAN_POINT('Ctrl Pts',(34.0658532948882,36.7908022610815,36.3963377418929)) ;
#13318=CARTESIAN_POINT('Ctrl Pts',(34.,37.2389528853926,36.0607502488633)) ;
#13319=CARTESIAN_POINT('Ctrl Pts',(34.,37.5299498120862,35.8966488600263)) ;
#13320=CARTESIAN_POINT('',(34.,25.5,41.4)) ;
#13321=CARTESIAN_POINT('Origin',(34.,25.5,25.5)) ;
#13322=CARTESIAN_POINT('',(34.4,25.5,41.)) ;
#13323=CARTESIAN_POINT('Origin',(34.4,25.5,41.4)) ;
#13324=CARTESIAN_POINT('',(34.4,10.,25.5)) ;
#13325=CARTESIAN_POINT('Origin',(34.4,25.5,25.5)) ;
#13326=CARTESIAN_POINT('Origin',(34.4,25.5,25.5)) ;
#13327=CARTESIAN_POINT('Origin',(34.,25.5,25.5)) ;
#13328=CARTESIAN_POINT('Origin',(34.,11.357864376269,39.642135623731)) ;
#13329=CARTESIAN_POINT('',(29.6,11.357864376269,43.642135623731)) ;
#13330=CARTESIAN_POINT('',(34.,11.357864376269,43.642135623731)) ;
#13331=CARTESIAN_POINT('Origin',(29.6,11.357864376269,39.642135623731)) ;
#13332=CARTESIAN_POINT('Origin',(33.85,39.642135623731,39.642135623731)) ;
#13333=CARTESIAN_POINT('',(33.7,36.1579618900522,37.6773116128987)) ;
#13334=CARTESIAN_POINT('',(34.,35.8966488600263,37.5299498120862)) ;
#13335=CARTESIAN_POINT('',(33.7,39.642135623731,43.642135623731)) ;
#13336=CARTESIAN_POINT('Origin',(33.7,39.642135623731,39.642135623731)) ;
#13337=CARTESIAN_POINT('',(33.7,37.6773116128987,36.1579618900522)) ;
#13338=CARTESIAN_POINT('Origin',(33.7,39.642135623731,39.642135623731)) ;
#13339=CARTESIAN_POINT('',(33.7,37.6773116128987,36.1579618900522)) ;
#13340=CARTESIAN_POINT('Origin',(34.,39.642135623731,39.642135623731)) ;
#13341=CARTESIAN_POINT('Ctrl Pts',(34.,37.5299498120862,35.8966488600263)) ;
#13342=CARTESIAN_POINT('Ctrl Pts',(34.,37.2389528853926,36.0607502488633)) ;
#13343=CARTESIAN_POINT('Ctrl Pts',(34.0658532948882,36.7908022610815,36.3963377418929)) ;
#13344=CARTESIAN_POINT('Ctrl Pts',(34.0395377031192,36.2574192030825,36.9664717701347)) ;
#13345=CARTESIAN_POINT('Ctrl Pts',(34.,36.0060497859176,37.3359518609572)) ;
#13346=CARTESIAN_POINT('Ctrl Pts',(34.,35.8966488600263,37.5299498120862)) ;
#13347=CARTESIAN_POINT('Ctrl Pts',(33.9,37.579070412357,35.9837532033683)) ;
#13348=CARTESIAN_POINT('Ctrl Pts',(33.9,37.2948408560517,36.1440382808369)) ;
#13349=CARTESIAN_POINT('Ctrl Pts',(33.9439021965921,36.8556320186083,36.4701841374116)) ;
#13350=CARTESIAN_POINT('Ctrl Pts',(33.9263584687462,36.3354050597151,37.0282435448734)) ;
#13351=CARTESIAN_POINT('Ctrl Pts',(33.9,36.0906099216807,37.3895840414868)) ;
#13352=CARTESIAN_POINT('Ctrl Pts',(33.9,35.9837532033683,37.579070412357)) ;
#13353=CARTESIAN_POINT('Ctrl Pts',(33.8,37.6281910126279,36.0708575467102)) ;
#13354=CARTESIAN_POINT('Ctrl Pts',(33.8,37.3507288267107,36.2273263128106)) ;
#13355=CARTESIAN_POINT('Ctrl Pts',(33.8219510982961,36.9204617761351,36.5440305329303)) ;
#13356=CARTESIAN_POINT('Ctrl Pts',(33.8131792343731,36.4133909163477,37.090015319612)) ;
#13357=CARTESIAN_POINT('Ctrl Pts',(33.8,36.1751700574438,37.4432162220164)) ;
#13358=CARTESIAN_POINT('Ctrl Pts',(33.8,36.0708575467102,37.6281910126279)) ;
#13359=CARTESIAN_POINT('Ctrl Pts',(33.7,37.6773116128987,36.1579618900522)) ;
#13360=CARTESIAN_POINT('Ctrl Pts',(33.7,37.4066167973697,36.3106143447843)) ;
#13361=CARTESIAN_POINT('Ctrl Pts',(33.7,36.9852915336619,36.6178769284489)) ;
#13362=CARTESIAN_POINT('Ctrl Pts',(33.7,36.4913767729803,37.1517870943507)) ;
#13363=CARTESIAN_POINT('Ctrl Pts',(33.7,36.2597301932069,37.496848402546)) ;
#13364=CARTESIAN_POINT('Ctrl Pts',(33.7,36.1579618900522,37.6773116128987)) ;
#13365=CARTESIAN_POINT('Ctrl Pts',(33.7,37.6773116128987,36.1579618900522)) ;
#13366=CARTESIAN_POINT('Ctrl Pts',(33.7,37.4066167973697,36.3106143447843)) ;
#13367=CARTESIAN_POINT('Ctrl Pts',(33.7,36.9852915336619,36.6178769284489)) ;
#13368=CARTESIAN_POINT('Ctrl Pts',(33.7,36.4913767729803,37.1517870943507)) ;
#13369=CARTESIAN_POINT('Ctrl Pts',(33.7,36.2597301932069,37.496848402546)) ;
#13370=CARTESIAN_POINT('Ctrl Pts',(33.7,36.1579618900522,37.6773116128987)) ;
#13371=CARTESIAN_POINT('Origin',(34.,39.642135623731,39.642135623731)) ;
#13372=CARTESIAN_POINT('',(29.6,39.642135623731,43.642135623731)) ;
#13373=CARTESIAN_POINT('',(34.,39.642135623731,43.642135623731)) ;
#13374=CARTESIAN_POINT('Origin',(29.6,39.642135623731,39.642135623731)) ;
#13375=CARTESIAN_POINT('Origin',(33.85,39.642135623731,11.3578643762691)) ;
#13376=CARTESIAN_POINT('',(33.7,37.6773116128987,14.8420381099478)) ;
#13377=CARTESIAN_POINT('',(34.,37.5299498120862,15.1033511399737)) ;
#13378=CARTESIAN_POINT('',(33.7,39.642135623731,15.3578643762691)) ;
#13379=CARTESIAN_POINT('Origin',(33.7,39.642135623731,11.3578643762691)) ;
#13380=CARTESIAN_POINT('',(33.7,36.1579618900522,13.3226883871013)) ;
#13381=CARTESIAN_POINT('Origin',(33.7,39.642135623731,11.3578643762691)) ;
#13382=CARTESIAN_POINT('',(33.7,36.1579618900522,13.3226883871013)) ;
#13383=CARTESIAN_POINT('Origin',(34.,39.642135623731,11.3578643762691)) ;
#13384=CARTESIAN_POINT('Ctrl Pts',(34.,35.8966488600263,13.4700501879138)) ;
#13385=CARTESIAN_POINT('Ctrl Pts',(34.,36.0060497859176,13.6640481390428)) ;
#13386=CARTESIAN_POINT('Ctrl Pts',(34.0395441492995,36.2574128941273,14.0335330726099)) ;
#13387=CARTESIAN_POINT('Ctrl Pts',(34.0658646655374,36.790793689875,14.6036692327227)) ;
#13388=CARTESIAN_POINT('Ctrl Pts',(34.,37.2389528853926,14.9392497511367)) ;
#13389=CARTESIAN_POINT('Ctrl Pts',(34.,37.5299498120862,15.1033511399737)) ;
#13390=CARTESIAN_POINT('Ctrl Pts',(33.9,35.9837532033683,13.420929587643)) ;
#13391=CARTESIAN_POINT('Ctrl Pts',(33.9,36.0906099216807,13.6104159585132)) ;
#13392=CARTESIAN_POINT('Ctrl Pts',(33.9263627661997,36.33540081748,13.9717597254023)) ;
#13393=CARTESIAN_POINT('Ctrl Pts',(33.9439097770249,36.8556262482266,14.5298205825143)) ;
#13394=CARTESIAN_POINT('Ctrl Pts',(33.9,37.2948408560517,14.8559617191631)) ;
#13395=CARTESIAN_POINT('Ctrl Pts',(33.9,37.579070412357,15.0162467966317)) ;
#13396=CARTESIAN_POINT('Ctrl Pts',(33.8,36.0708575467102,13.3718089873721)) ;
#13397=CARTESIAN_POINT('Ctrl Pts',(33.8,36.1751700574438,13.5567837779836)) ;
#13398=CARTESIAN_POINT('Ctrl Pts',(33.8131813830998,36.4133887408328,13.9099863781946)) ;
#13399=CARTESIAN_POINT('Ctrl Pts',(33.8219548885125,36.9204588065782,14.4559719323059)) ;
#13400=CARTESIAN_POINT('Ctrl Pts',(33.8,37.3507288267107,14.7726736871894)) ;
#13401=CARTESIAN_POINT('Ctrl Pts',(33.8,37.6281910126279,14.9291424532898)) ;
#13402=CARTESIAN_POINT('Ctrl Pts',(33.7,36.1579618900522,13.3226883871013)) ;
#13403=CARTESIAN_POINT('Ctrl Pts',(33.7,36.2597301932069,13.503151597454)) ;
#13404=CARTESIAN_POINT('Ctrl Pts',(33.7,36.4913766641855,13.848213030987)) ;
#13405=CARTESIAN_POINT('Ctrl Pts',(33.7,36.9852913649297,14.3821232820975)) ;
#13406=CARTESIAN_POINT('Ctrl Pts',(33.7,37.4066167973697,14.6893856552157)) ;
#13407=CARTESIAN_POINT('Ctrl Pts',(33.7,37.6773116128987,14.8420381099478)) ;
#13408=CARTESIAN_POINT('Ctrl Pts',(33.7,36.1579618900522,13.3226883871013)) ;
#13409=CARTESIAN_POINT('Ctrl Pts',(33.7,36.2597301932069,13.503151597454)) ;
#13410=CARTESIAN_POINT('Ctrl Pts',(33.7,36.4913766641855,13.848213030987)) ;
#13411=CARTESIAN_POINT('Ctrl Pts',(33.7,36.9852913649297,14.3821232820975)) ;
#13412=CARTESIAN_POINT('Ctrl Pts',(33.7,37.4066167973697,14.6893856552157)) ;
#13413=CARTESIAN_POINT('Ctrl Pts',(33.7,37.6773116128987,14.8420381099478)) ;
#13414=CARTESIAN_POINT('Origin',(34.,39.642135623731,11.3578643762691)) ;
#13415=CARTESIAN_POINT('',(29.6,39.642135623731,15.3578643762691)) ;
#13416=CARTESIAN_POINT('',(34.,39.642135623731,15.3578643762691)) ;
#13417=CARTESIAN_POINT('Origin',(29.6,39.642135623731,11.3578643762691)) ;
#13418=CARTESIAN_POINT('Origin',(33.85,11.3578643762691,11.357864376269)) ;
#13419=CARTESIAN_POINT('',(33.7,14.8420381099478,13.3226883871013)) ;
#13420=CARTESIAN_POINT('',(34.,15.1033511399737,13.4700501879138)) ;
#13421=CARTESIAN_POINT('',(33.7,11.3578643762691,15.357864376269)) ;
#13422=CARTESIAN_POINT('Origin',(33.7,11.3578643762691,11.357864376269)) ;
#13423=CARTESIAN_POINT('',(33.7,13.3226883871013,14.8420381099478)) ;
#13424=CARTESIAN_POINT('Origin',(33.7,11.3578643762691,11.357864376269)) ;
#13425=CARTESIAN_POINT('',(33.7,13.3226883871013,14.8420381099478)) ;
#13426=CARTESIAN_POINT('Origin',(34.,11.3578643762691,11.357864376269)) ;
#13427=CARTESIAN_POINT('Ctrl Pts',(34.,13.4700501879138,15.1033511399737)) ;
#13428=CARTESIAN_POINT('Ctrl Pts',(34.,13.7610471146074,14.9392497511367)) ;
#13429=CARTESIAN_POINT('Ctrl Pts',(34.0658862423307,14.2092225347123,14.6036824431284)) ;
#13430=CARTESIAN_POINT('Ctrl Pts',(34.0395562744413,14.7425990198672,14.0335422105128)) ;
#13431=CARTESIAN_POINT('Ctrl Pts',(34.,14.9939502140824,13.6640481390428)) ;
#13432=CARTESIAN_POINT('Ctrl Pts',(34.,15.1033511399737,13.4700501879138)) ;
#13433=CARTESIAN_POINT('Ctrl Pts',(33.9,13.420929587643,15.0162467966317)) ;
#13434=CARTESIAN_POINT('Ctrl Pts',(33.9,13.7051591439483,14.8559617191631)) ;
#13435=CARTESIAN_POINT('Ctrl Pts',(33.9439241615538,14.1443846747721,14.5298295225732)) ;
#13436=CARTESIAN_POINT('Ctrl Pts',(33.9263708496276,14.6646071935385,13.971765895988)) ;
#13437=CARTESIAN_POINT('Ctrl Pts',(33.9,14.9093900783193,13.6104159585132)) ;
#13438=CARTESIAN_POINT('Ctrl Pts',(33.9,15.0162467966317,13.4209295876429)) ;
#13439=CARTESIAN_POINT('Ctrl Pts',(33.8,13.3718089873721,14.9291424532898)) ;
#13440=CARTESIAN_POINT('Ctrl Pts',(33.8,13.6492711732893,14.7726736871894)) ;
#13441=CARTESIAN_POINT('Ctrl Pts',(33.8219620807769,14.0795468148318,14.455976602018)) ;
#13442=CARTESIAN_POINT('Ctrl Pts',(33.8131854248138,14.5866153672098,13.9099895814631)) ;
#13443=CARTESIAN_POINT('Ctrl Pts',(33.8,14.8248299425562,13.5567837779836)) ;
#13444=CARTESIAN_POINT('Ctrl Pts',(33.8,14.9291424532898,13.3718089873721)) ;
#13445=CARTESIAN_POINT('Ctrl Pts',(33.7,13.3226883871013,14.8420381099478)) ;
#13446=CARTESIAN_POINT('Ctrl Pts',(33.7,13.5933832026303,14.6893856552157)) ;
#13447=CARTESIAN_POINT('Ctrl Pts',(33.7,14.0147089548915,14.3821236814628)) ;
#13448=CARTESIAN_POINT('Ctrl Pts',(33.7,14.5086235408811,13.8482132669383)) ;
#13449=CARTESIAN_POINT('Ctrl Pts',(33.7,14.7402698067931,13.503151597454)) ;
#13450=CARTESIAN_POINT('Ctrl Pts',(33.7,14.8420381099478,13.3226883871013)) ;
#13451=CARTESIAN_POINT('Ctrl Pts',(33.7,13.3226883871013,14.8420381099478)) ;
#13452=CARTESIAN_POINT('Ctrl Pts',(33.7,13.5933832026303,14.6893856552157)) ;
#13453=CARTESIAN_POINT('Ctrl Pts',(33.7,14.0147089548915,14.3821236814628)) ;
#13454=CARTESIAN_POINT('Ctrl Pts',(33.7,14.5086235408811,13.8482132669383)) ;
#13455=CARTESIAN_POINT('Ctrl Pts',(33.7,14.7402698067931,13.503151597454)) ;
#13456=CARTESIAN_POINT('Ctrl Pts',(33.7,14.8420381099478,13.3226883871013)) ;
#13457=CARTESIAN_POINT('Origin',(34.,11.3578643762691,11.357864376269)) ;
#13458=CARTESIAN_POINT('',(29.6,11.3578643762691,15.357864376269)) ;
#13459=CARTESIAN_POINT('',(34.,11.3578643762691,15.357864376269)) ;
#13460=CARTESIAN_POINT('Origin',(29.6,11.3578643762691,11.357864376269)) ;
#13461=CARTESIAN_POINT('Origin',(29.6,11.3578643762691,11.357864376269)) ;
#13462=CARTESIAN_POINT('',(29.6,11.3578643762691,13.607864376269)) ;
#13463=CARTESIAN_POINT('Origin',(29.6,11.3578643762691,11.357864376269)) ;
#13464=CARTESIAN_POINT('Origin',(29.6,39.642135623731,11.3578643762691)) ;
#13465=CARTESIAN_POINT('',(29.6,39.642135623731,13.607864376269)) ;
#13466=CARTESIAN_POINT('Origin',(29.6,39.642135623731,11.3578643762691)) ;
#13467=CARTESIAN_POINT('Origin',(29.6,39.642135623731,39.642135623731)) ;
#13468=CARTESIAN_POINT('',(29.6,39.642135623731,41.892135623731)) ;
#13469=CARTESIAN_POINT('Origin',(29.6,39.642135623731,39.642135623731)) ;
#13470=CARTESIAN_POINT('Origin',(29.6,11.357864376269,39.642135623731)) ;
#13471=CARTESIAN_POINT('',(29.6,11.357864376269,41.892135623731)) ;
#13472=CARTESIAN_POINT('Origin',(29.6,11.357864376269,39.642135623731)) ;
#13473=CARTESIAN_POINT('Origin',(34.,11.3578643762691,11.357864376269)) ;
#13474=CARTESIAN_POINT('',(27.,11.3578643762691,13.607864376269)) ;
#13475=CARTESIAN_POINT('',(34.,11.3578643762691,13.607864376269)) ;
#13476=CARTESIAN_POINT('Origin',(27.,11.3578643762691,11.357864376269)) ;
#13477=CARTESIAN_POINT('Origin',(34.,39.642135623731,11.3578643762691)) ;
#13478=CARTESIAN_POINT('',(27.,39.642135623731,13.607864376269)) ;
#13479=CARTESIAN_POINT('',(34.,39.642135623731,13.607864376269)) ;
#13480=CARTESIAN_POINT('Origin',(27.,39.642135623731,11.3578643762691)) ;
#13481=CARTESIAN_POINT('Origin',(34.,39.642135623731,39.642135623731)) ;
#13482=CARTESIAN_POINT('',(27.,39.642135623731,41.892135623731)) ;
#13483=CARTESIAN_POINT('',(34.,39.642135623731,41.892135623731)) ;
#13484=CARTESIAN_POINT('Origin',(27.,39.642135623731,39.642135623731)) ;
#13485=CARTESIAN_POINT('Origin',(34.,11.357864376269,39.642135623731)) ;
#13486=CARTESIAN_POINT('',(27.,11.357864376269,41.892135623731)) ;
#13487=CARTESIAN_POINT('',(34.,11.357864376269,41.892135623731)) ;
#13488=CARTESIAN_POINT('Origin',(27.,11.357864376269,39.642135623731)) ;
#13489=CARTESIAN_POINT('Origin',(32.1,19.8431457505076,19.8431457505076)) ;
#13490=CARTESIAN_POINT('',(32.1,20.6453165160457,18.4012643188649)) ;
#13491=CARTESIAN_POINT('',(71.9,20.6453165160457,18.4012643188649)) ;
#13492=CARTESIAN_POINT('',(32.1,20.6453165160457,18.4012643188649)) ;
#13493=CARTESIAN_POINT('',(32.1,18.4012643188649,20.6453165160456)) ;
#13494=CARTESIAN_POINT('Origin',(32.1,19.8431457505076,19.8431457505076)) ;
#13495=CARTESIAN_POINT('',(71.9,18.4012643188649,20.6453165160456)) ;
#13496=CARTESIAN_POINT('',(32.1,18.4012643188649,20.6453165160456)) ;
#13497=CARTESIAN_POINT('Origin',(71.9,19.8431457505076,19.8431457505076)) ;
#13498=CARTESIAN_POINT('Origin',(32.1,31.1568542494924,19.8431457505076)) ;
#13499=CARTESIAN_POINT('',(32.1,32.5987356811351,20.6453165160457)) ;
#13500=CARTESIAN_POINT('',(71.9,32.5987356811351,20.6453165160457)) ;
#13501=CARTESIAN_POINT('',(32.1,32.5987356811351,20.6453165160457)) ;
#13502=CARTESIAN_POINT('',(32.1,30.3546834839544,18.4012643188649)) ;
#13503=CARTESIAN_POINT('Origin',(32.1,31.1568542494924,19.8431457505076)) ;
#13504=CARTESIAN_POINT('',(71.9,30.3546834839544,18.4012643188649)) ;
#13505=CARTESIAN_POINT('',(32.1,30.3546834839544,18.4012643188649)) ;
#13506=CARTESIAN_POINT('Origin',(71.9,31.1568542494924,19.8431457505076)) ;
#13507=CARTESIAN_POINT('Origin',(32.1,31.1568542494924,31.1568542494924)) ;
#13508=CARTESIAN_POINT('',(71.9,32.5987356811351,30.3546834839544)) ;
#13509=CARTESIAN_POINT('',(32.1,32.5987356811351,30.3546834839544)) ;
#13510=CARTESIAN_POINT('',(32.1,32.5987356811351,30.3546834839544)) ;
#13511=CARTESIAN_POINT('',(71.9,30.3546834839544,32.5987356811351)) ;
#13512=CARTESIAN_POINT('Origin',(71.9,31.1568542494924,31.1568542494924)) ;
#13513=CARTESIAN_POINT('',(32.1,30.3546834839544,32.5987356811351)) ;
#13514=CARTESIAN_POINT('',(32.1,30.3546834839544,32.5987356811351)) ;
#13515=CARTESIAN_POINT('Origin',(32.1,31.1568542494924,31.1568542494924)) ;
#13516=CARTESIAN_POINT('Origin',(32.1,19.8431457505076,31.1568542494924)) ;
#13517=CARTESIAN_POINT('',(71.9,20.6453165160456,32.5987356811351)) ;
#13518=CARTESIAN_POINT('',(32.1,20.6453165160456,32.5987356811351)) ;
#13519=CARTESIAN_POINT('',(32.1,20.6453165160456,32.5987356811351)) ;
#13520=CARTESIAN_POINT('',(71.9,18.4012643188649,30.3546834839544)) ;
#13521=CARTESIAN_POINT('Origin',(71.9,19.8431457505076,31.1568542494924)) ;
#13522=CARTESIAN_POINT('',(32.1,18.4012643188649,30.3546834839544)) ;
#13523=CARTESIAN_POINT('',(32.1,18.4012643188649,30.3546834839544)) ;
#13524=CARTESIAN_POINT('Origin',(32.1,19.8431457505076,31.1568542494924)) ;
#13525=CARTESIAN_POINT('Origin',(71.9,34.1,25.5)) ;
#13526=CARTESIAN_POINT('',(71.9,13.5,25.5)) ;
#13527=CARTESIAN_POINT('Origin',(71.9,25.5,25.5)) ;
#13528=CARTESIAN_POINT('Origin',(71.9,25.5,25.5)) ;
#13529=CARTESIAN_POINT('Origin',(71.9,25.5,25.5)) ;
#13530=CARTESIAN_POINT('Origin',(71.9,25.5,25.5)) ;
#13531=CARTESIAN_POINT('Origin',(71.9,25.5,25.5)) ;
#13532=CARTESIAN_POINT('Origin',(52.,25.5,25.5)) ;
#13533=CARTESIAN_POINT('Origin',(32.1,25.5,25.5)) ;
#13534=CARTESIAN_POINT('Origin',(52.,25.5,25.5)) ;
#13535=CARTESIAN_POINT('Origin',(32.1,25.5,25.5)) ;
#13536=CARTESIAN_POINT('Origin',(52.,25.5,25.5)) ;
#13537=CARTESIAN_POINT('Origin',(32.1,25.5,25.5)) ;
#13538=CARTESIAN_POINT('Origin',(52.,25.5,25.5)) ;
#13539=CARTESIAN_POINT('Origin',(32.1,25.5,25.5)) ;
#13540=CARTESIAN_POINT('Origin',(34.,41.,25.5)) ;
#13541=CARTESIAN_POINT('',(34.,0.500000000000001,25.5)) ;
#13542=CARTESIAN_POINT('Origin',(34.,25.5,25.5)) ;
#13543=CARTESIAN_POINT('Origin',(55.25,25.5,25.5)) ;
#13544=CARTESIAN_POINT('',(55.25,10.,25.5)) ;
#13545=CARTESIAN_POINT('Origin',(74.9,38.1,25.5)) ;
#13546=CARTESIAN_POINT('',(74.9,12.9,25.5)) ;
#13547=CARTESIAN_POINT('Origin',(74.9,25.5,25.5)) ;
#13548=CARTESIAN_POINT('',(74.9,13.5,25.5)) ;
#13549=CARTESIAN_POINT('Origin',(74.9,25.5,25.5)) ;
#13550=CARTESIAN_POINT('Origin',(75.55,25.5,25.5)) ;
#13551=CARTESIAN_POINT('',(76.2,12.9,25.5)) ;
#13552=CARTESIAN_POINT('',(75.55,12.9,25.5)) ;
#13553=CARTESIAN_POINT('Origin',(76.2,25.5,25.5)) ;
#13554=CARTESIAN_POINT('Origin',(76.2,37.4,25.5)) ;
#13555=CARTESIAN_POINT('',(76.2,13.5,25.5)) ;
#13556=CARTESIAN_POINT('Origin',(76.2,25.5,25.5)) ;
#13557=CARTESIAN_POINT('Origin',(74.45,25.5,25.5)) ;
#13558=CARTESIAN_POINT('',(77.,13.5,25.5)) ;
#13559=CARTESIAN_POINT('Origin',(77.,25.5,25.5)) ;
#13560=CARTESIAN_POINT('',(74.45,13.5,25.5)) ;
#13561=CARTESIAN_POINT('Origin',(27.8,38.1,25.5)) ;
#13562=CARTESIAN_POINT('',(27.8,12.9,25.5)) ;
#13563=CARTESIAN_POINT('Origin',(27.8,25.5,25.5)) ;
#13564=CARTESIAN_POINT('',(27.8,13.5,25.5)) ;
#13565=CARTESIAN_POINT('Origin',(27.8,25.5,25.5)) ;
#13566=CARTESIAN_POINT('Origin',(28.45,25.5,25.5)) ;
#13567=CARTESIAN_POINT('',(29.1,12.9,25.5)) ;
#13568=CARTESIAN_POINT('',(28.45,12.9,25.5)) ;
#13569=CARTESIAN_POINT('Origin',(29.1,25.5,25.5)) ;
#13570=CARTESIAN_POINT('Origin',(29.1,37.4,25.5)) ;
#13571=CARTESIAN_POINT('',(29.1,13.5,25.5)) ;
#13572=CARTESIAN_POINT('Origin',(29.1,25.5,25.5)) ;
#13573=CARTESIAN_POINT('Origin',(29.55,25.5,25.5)) ;
#13574=CARTESIAN_POINT('',(32.1,13.5,25.5)) ;
#13575=CARTESIAN_POINT('Origin',(32.1,25.5,25.5)) ;
#13576=CARTESIAN_POINT('',(29.55,13.5,25.5)) ;
#13577=CARTESIAN_POINT('Origin',(32.1,37.5,25.5)) ;
#13578=CARTESIAN_POINT('Origin',(29.55,25.5,25.5)) ;
#13579=CARTESIAN_POINT('',(27.,13.5,25.5)) ;
#13580=CARTESIAN_POINT('',(29.55,13.5,25.5)) ;
#13581=CARTESIAN_POINT('Origin',(27.,25.5,25.5)) ;
#13582=CARTESIAN_POINT('Origin',(27.,50.5,25.5)) ;
#13583=CARTESIAN_POINT('',(27.,0.500000000000003,25.5)) ;
#13584=CARTESIAN_POINT('Origin',(27.,25.5,25.5)) ;
#13585=CARTESIAN_POINT('Origin',(27.25,25.5,25.5)) ;
#13586=CARTESIAN_POINT('',(27.5,2.53269627492614E-15,25.5)) ;
#13587=CARTESIAN_POINT('Origin',(27.5,25.5,25.5)) ;
#13588=CARTESIAN_POINT('',(27.25,0.250000000000004,25.5)) ;
#13589=CARTESIAN_POINT('Origin',(30.5,25.5,25.5)) ;
#13590=CARTESIAN_POINT('',(33.5,0.,25.5)) ;
#13591=CARTESIAN_POINT('Origin',(33.5,25.5,25.5)) ;
#13592=CARTESIAN_POINT('',(30.5,0.,25.5)) ;
#13593=CARTESIAN_POINT('Origin',(33.75,25.5,25.5)) ;
#13594=CARTESIAN_POINT('',(33.75,0.250000000000004,25.5)) ;
#13595=CARTESIAN_POINT('Origin',(76.75,25.5,25.5)) ;
#13596=CARTESIAN_POINT('',(77.,10.5,25.5)) ;
#13597=CARTESIAN_POINT('Origin',(77.,25.5,25.5)) ;
#13598=CARTESIAN_POINT('',(76.75,10.25,25.5)) ;
#13599=CARTESIAN_POINT('Origin',(77.,37.5,25.5)) ;
#13600=CARTESIAN_POINT('Origin',(74.45,25.5,25.5)) ;
#13601=CARTESIAN_POINT('',(74.45,13.5,25.5)) ;
#16927=UNCERTAINTY_MEASURE_WITH_UNIT(LENGTH_MEASURE(0.01),#16943,
'DISTANCE_ACCURACY_VALUE',
'Maximum model space distance between geometric entities at asserted c
onnectivities') ;
#16933=UNCERTAINTY_MEASURE_WITH_UNIT(LENGTH_MEASURE(0.01),#16943,
'DISTANCE_ACCURACY_VALUE',
'Maximum model space distance between geometric entities at asserted c
onnectivities') ;
#16936=(
GEOMETRIC_REPRESENTATION_CONTEXT(3)
GLOBAL_UNCERTAINTY_ASSIGNED_CONTEXT((#16927))
GLOBAL_UNIT_ASSIGNED_CONTEXT((#16943,#16945,#16946))
REPRESENTATION_CONTEXT('','3D')
) ;
#16942=(
GEOMETRIC_REPRESENTATION_CONTEXT(3)
GLOBAL_UNCERTAINTY_ASSIGNED_CONTEXT((#16933))
GLOBAL_UNIT_ASSIGNED_CONTEXT((#16943,#16945,#16946))
REPRESENTATION_CONTEXT('','3D')
) ;
#16943=(
LENGTH_UNIT()
NAMED_UNIT(*)
SI_UNIT(.MILLI.,.METRE.)
) ;
#16945=(
NAMED_UNIT(*)
PLANE_ANGLE_UNIT()
SI_UNIT($,.RADIAN.)
) ;
#16946=(
NAMED_UNIT(*)
SI_UNIT($,.STERADIAN.)
SOLID_ANGLE_UNIT()
) ;
#16949=SHAPE_DEFINITION_REPRESENTATION(#16957,#17020) ;
#16957=PRODUCT_DEFINITION_SHAPE('',$,#17029) ;
#17020=SHAPE_REPRESENTATION('',(#8345),#16936) ;
#17026=PRODUCT_DEFINITION_CONTEXT('part definition',#17052,'design') ;
#17029=PRODUCT_DEFINITION('Ball Spline Nut Outer Sleeve Round Flange BSLM16',
'Ball Spline Nut Outer Sleeve Round Flange BSLM16',#17037,#17026) ;
#17037=PRODUCT_DEFINITION_FORMATION('',$,#17056) ;
#17052=APPLICATION_CONTEXT(
'Core Data for Automotive Mechanical Design Process') ;
#17053=PRODUCT_CONTEXT('part definition',#17052,'mechanical') ;
#17056=PRODUCT('Ball Spline Nut Outer Sleeve Round Flange BSLM16',
'Ball Spline Nut Outer Sleeve Round Flange BSLM16',$,(#17053)) ;
#17064=PRESENTATION_STYLE_ASSIGNMENT((#17072)) ;
#17072=SURFACE_STYLE_USAGE(.BOTH.,#17080) ;
#17080=SURFACE_SIDE_STYLE('',(#17088)) ;
#17088=SURFACE_STYLE_FILL_AREA(#17096) ;
#17096=FILL_AREA_STYLE(
'MAS-257 Metallic Sheet - Ball Spline Nut Outer Sleeve Round Flang',(#17104)) ;
#17104=FILL_AREA_STYLE_COLOUR(
'MAS-257 Metallic Sheet - Ball Spline Nut Outer Sleeve Round Flang',#17112) ;
#17112=COLOUR_RGB(
'MAS-257 Metallic Sheet - Ball Spline Nut Outer Sleeve Round Flang', 0.31764706, 0.68627451, 0.89019608) ;
ENDSEC;
END-ISO-10303-21;
